ISO-10303-21;
HEADER;
/* Generated by software containing ST-Developer
 * from STEP Tools, Inc. (www.steptools.com) 
 */

FILE_DESCRIPTION(
/* description */ (''),
/* implementation_level */ '2;1');

FILE_NAME(
/* name */ 'Screw_01.step',
/* time_stamp */ '2026-10-04T22:56:18-07:00',
/* author */ (''),
/* organization */ (''),
/* preprocessor_version */ 'ST-DEVELOPER v20.2',
/* originating_system */ 'Autodesk Translation Framework v15.15.0.0',
/* authorisation */ '');

FILE_SCHEMA (('AUTOMOTIVE_DESIGN { 1 0 10303 214 3 1 1 }'));
ENDSEC;

DATA;
#10=MECHANICAL_DESIGN_GEOMETRIC_PRESENTATION_REPRESENTATION('',(#195),#14544);
#43=CONICAL_SURFACE('',#2029,3.34979916874976,1.09810780243133);
#51=B_SPLINE_SURFACE_WITH_KNOTS('',3,3,((#7599,#7600,#7601,#7602,#7603,
#7604,#7605,#7606,#7607,#7608,#7609,#7610,#7611,#7612,#7613,#7614,#7615,
#7616,#7617,#7618,#7619,#7620,#7621,#7622,#7623,#7624,#7625,#7626,#7627,
#7628,#7629,#7630,#7631,#7632,#7633,#7634,#7635,#7636,#7637,#7638,#7639,
#7640,#7641,#7642,#7643,#7644,#7645,#7646,#7647,#7648,#7649,#7650,#7651,
#7652,#7653,#7654,#7655,#7656,#7657,#7658,#7659,#7660,#7661,#7662,#7663,
#7664,#7665,#7666,#7667,#7668,#7669,#7670,#7671,#7672,#7673,#7674,#7675,
#7676),(#7677,#7678,#7679,#7680,#7681,#7682,#7683,#7684,#7685,#7686,#7687,
#7688,#7689,#7690,#7691,#7692,#7693,#7694,#7695,#7696,#7697,#7698,#7699,
#7700,#7701,#7702,#7703,#7704,#7705,#7706,#7707,#7708,#7709,#7710,#7711,
#7712,#7713,#7714,#7715,#7716,#7717,#7718,#7719,#7720,#7721,#7722,#7723,
#7724,#7725,#7726,#7727,#7728,#7729,#7730,#7731,#7732,#7733,#7734,#7735,
#7736,#7737,#7738,#7739,#7740,#7741,#7742,#7743,#7744,#7745,#7746,#7747,
#7748,#7749,#7750,#7751,#7752,#7753,#7754),(#7755,#7756,#7757,#7758,#7759,
#7760,#7761,#7762,#7763,#7764,#7765,#7766,#7767,#7768,#7769,#7770,#7771,
#7772,#7773,#7774,#7775,#7776,#7777,#7778,#7779,#7780,#7781,#7782,#7783,
#7784,#7785,#7786,#7787,#7788,#7789,#7790,#7791,#7792,#7793,#7794,#7795,
#7796,#7797,#7798,#7799,#7800,#7801,#7802,#7803,#7804,#7805,#7806,#7807,
#7808,#7809,#7810,#7811,#7812,#7813,#7814,#7815,#7816,#7817,#7818,#7819,
#7820,#7821,#7822,#7823,#7824,#7825,#7826,#7827,#7828,#7829,#7830,#7831,
#7832),(#7833,#7834,#7835,#7836,#7837,#7838,#7839,#7840,#7841,#7842,#7843,
#7844,#7845,#7846,#7847,#7848,#7849,#7850,#7851,#7852,#7853,#7854,#7855,
#7856,#7857,#7858,#7859,#7860,#7861,#7862,#7863,#7864,#7865,#7866,#7867,
#7868,#7869,#7870,#7871,#7872,#7873,#7874,#7875,#7876,#7877,#7878,#7879,
#7880,#7881,#7882,#7883,#7884,#7885,#7886,#7887,#7888,#7889,#7890,#7891,
#7892,#7893,#7894,#7895,#7896,#7897,#7898,#7899,#7900,#7901,#7902,#7903,
#7904,#7905,#7906,#7907,#7908,#7909,#7910)),.UNSPECIFIED.,.F.,.F.,.F.,(4,
4),(4,1,1,1,1,1,1,1,1,1,1,1,1,1,1,1,1,1,1,1,1,1,1,1,1,1,1,1,1,1,1,1,1,1,
1,1,1,1,1,1,1,1,1,1,1,1,1,1,1,1,1,1,1,1,1,1,1,1,1,1,1,1,1,1,1,1,1,1,1,1,
1,1,1,1,1,4),(-0.000270112238314874,0.0397652738162967),(8.3062683528249,
9.29465849132061,10.2830486298163,11.271438768312,12.2598289068078,13.2482190453035,
14.2366091837992,15.2249993222949,16.2133894607906,17.2017795992863,18.190169737782,
19.1785598762778,20.1669500147735,21.1553401532692,22.1437302917649,23.1321204302606,
24.1205105687563,25.108900707252,26.0972908457478,27.0856809842435,28.0740711227392,
29.0624612612349,30.0508513997306,31.0392415382263,32.027631676722,33.0160218152178,
34.0044119537135,34.9928020922092,35.9811922307049,36.9695823692006,37.9579725076963,
38.946362646192,39.9347527846878,40.9231429231835,41.9115330616792,42.8999232001749,
43.8883133386706,44.8767034771663,45.865093615662,46.8534837541578,47.8418738926535,
48.8302640311492,49.8186541696449,50.8070443081406,51.7954344466363,52.783824585132,
53.7722147236278,54.7606048621235,55.7489950006192,56.7373851391149,57.7257752776106,
58.7141654161063,59.702555554602,60.6909456930978,61.6793358315935,62.6677259700892,
63.6561161085849,64.6445062470806,65.6328963855763,66.621286524072,67.6096766625678,
68.5980668010635,69.5864569395592,70.5748470780549,71.5632372165506,72.5516273550463,
73.5400174935421,74.5284076320378,75.5167977705335,76.5051879090292,77.4935780475249,
78.4819681860206,79.4703583245163,80.458748463012,81.4471386015078,82.4357988522418),
 .UNSPECIFIED.);
#52=B_SPLINE_SURFACE_WITH_KNOTS('',3,3,((#8072,#8073,#8074,#8075,#8076,
#8077,#8078,#8079,#8080,#8081,#8082,#8083,#8084,#8085,#8086,#8087,#8088,
#8089,#8090,#8091,#8092,#8093,#8094,#8095,#8096,#8097,#8098,#8099,#8100,
#8101,#8102,#8103,#8104,#8105,#8106,#8107,#8108,#8109,#8110,#8111,#8112,
#8113,#8114,#8115,#8116,#8117,#8118,#8119,#8120,#8121,#8122,#8123,#8124,
#8125,#8126,#8127,#8128,#8129,#8130,#8131,#8132,#8133,#8134,#8135,#8136,
#8137,#8138,#8139,#8140,#8141,#8142,#8143,#8144,#8145,#8146,#8147,#8148,
#8149),(#8150,#8151,#8152,#8153,#8154,#8155,#8156,#8157,#8158,#8159,#8160,
#8161,#8162,#8163,#8164,#8165,#8166,#8167,#8168,#8169,#8170,#8171,#8172,
#8173,#8174,#8175,#8176,#8177,#8178,#8179,#8180,#8181,#8182,#8183,#8184,
#8185,#8186,#8187,#8188,#8189,#8190,#8191,#8192,#8193,#8194,#8195,#8196,
#8197,#8198,#8199,#8200,#8201,#8202,#8203,#8204,#8205,#8206,#8207,#8208,
#8209,#8210,#8211,#8212,#8213,#8214,#8215,#8216,#8217,#8218,#8219,#8220,
#8221,#8222,#8223,#8224,#8225,#8226,#8227),(#8228,#8229,#8230,#8231,#8232,
#8233,#8234,#8235,#8236,#8237,#8238,#8239,#8240,#8241,#8242,#8243,#8244,
#8245,#8246,#8247,#8248,#8249,#8250,#8251,#8252,#8253,#8254,#8255,#8256,
#8257,#8258,#8259,#8260,#8261,#8262,#8263,#8264,#8265,#8266,#8267,#8268,
#8269,#8270,#8271,#8272,#8273,#8274,#8275,#8276,#8277,#8278,#8279,#8280,
#8281,#8282,#8283,#8284,#8285,#8286,#8287,#8288,#8289,#8290,#8291,#8292,
#8293,#8294,#8295,#8296,#8297,#8298,#8299,#8300,#8301,#8302,#8303,#8304,
#8305),(#8306,#8307,#8308,#8309,#8310,#8311,#8312,#8313,#8314,#8315,#8316,
#8317,#8318,#8319,#8320,#8321,#8322,#8323,#8324,#8325,#8326,#8327,#8328,
#8329,#8330,#8331,#8332,#8333,#8334,#8335,#8336,#8337,#8338,#8339,#8340,
#8341,#8342,#8343,#8344,#8345,#8346,#8347,#8348,#8349,#8350,#8351,#8352,
#8353,#8354,#8355,#8356,#8357,#8358,#8359,#8360,#8361,#8362,#8363,#8364,
#8365,#8366,#8367,#8368,#8369,#8370,#8371,#8372,#8373,#8374,#8375,#8376,
#8377,#8378,#8379,#8380,#8381,#8382,#8383)),.UNSPECIFIED.,.F.,.F.,.F.,(4,
4),(4,1,1,1,1,1,1,1,1,1,1,1,1,1,1,1,1,1,1,1,1,1,1,1,1,1,1,1,1,1,1,1,1,1,
1,1,1,1,1,1,1,1,1,1,1,1,1,1,1,1,1,1,1,1,1,1,1,1,1,1,1,1,1,1,1,1,1,1,1,1,
1,1,1,1,1,4),(-0.000234520548766864,0.0397897202828816),(11.6153673532494,
12.6040275861021,13.5924177245978,14.5808078630935,15.5691980015892,16.5575881400849,
17.5459782785806,18.5343684170764,19.5227585555721,20.5111486940678,21.4995388325635,
22.4879289710592,23.4763191095549,24.4647092480506,25.4530993865464,26.4414895250421,
27.4298796635378,28.4182698020335,29.4066599405292,30.3950500790249,31.3834402175206,
32.3718303560164,33.3602204945121,34.3486106330078,35.3370007715035,36.3253909099992,
37.3137810484949,38.3021711869906,39.2905613254864,40.2789514639821,41.2673416024778,
42.2557317409735,43.2441218794692,44.2325120179649,45.2209021564607,46.2092922949564,
47.1976824334521,48.1860725719478,49.1744627104435,50.1628528489392,51.1512429874349,
52.1396331259307,53.1280232644264,54.1164134029221,55.1048035414178,56.0931936799135,
57.0815838184092,58.0699739569049,59.0583640954007,60.0467542338964,61.0351443723921,
62.0235345108878,63.0119246493835,64.0003147878792,64.988704926375,65.9770950648707,
66.9654852033664,67.9538753418621,68.9422654803578,69.9306556188535,70.9190457573492,
71.907435895845,72.8958260343407,73.8842161728364,74.8726063113321,75.8609964498278,
76.8493865883235,77.8377767268192,78.8261668653149,79.8145570038107,80.8029471423064,
81.7913372808021,82.7797274192978,83.7681175577935,84.7565076962892,85.7449775254208),
 .UNSPECIFIED.);
#55=B_SPLINE_CURVE_WITH_KNOTS('',3,(#2735,#2736,#2737,#2738,#2739,#2740,
#2741,#2742,#2743,#2744,#2745,#2746,#2747,#2748,#2749,#2750,#2751,#2752,
#2753,#2754,#2755,#2756,#2757,#2758,#2759,#2760,#2761,#2762,#2763,#2764,
#2765,#2766,#2767,#2768,#2769,#2770,#2771,#2772,#2773,#2774,#2775,#2776,
#2777,#2778,#2779,#2780,#2781,#2782,#2783,#2784,#2785,#2786,#2787,#2788,
#2789,#2790,#2791,#2792,#2793,#2794,#2795,#2796,#2797,#2798,#2799,#2800,
#2801,#2802,#2803,#2804,#2805,#2806,#2807,#2808,#2809,#2810,#2811,#2812,
#2813,#2814,#2815,#2816,#2817,#2818,#2819,#2820,#2821,#2822,#2823,#2824,
#2825,#2826,#2827,#2828,#2829,#2830,#2831,#2832,#2833,#2834,#2835,#2836,
#2837,#2838,#2839,#2840,#2841,#2842,#2843,#2844,#2845,#2846,#2847,#2848,
#2849,#2850,#2851,#2852,#2853,#2854,#2855,#2856,#2857,#2858,#2859,#2860,
#2861,#2862,#2863,#2864),.UNSPECIFIED.,.F.,.F.,(4,3,3,3,3,3,3,3,3,3,3,3,
3,3,3,3,3,3,3,3,3,3,3,3,3,3,3,3,3,3,3,3,3,3,3,3,3,3,3,3,3,3,3,4),(10.3759830427441,
10.4901328275944,10.6041362297079,10.7180425069784,10.8319007590481,10.945840293292,
11.059816326816,11.1740039201576,11.271438768312,11.3871452657409,11.5026525812533,
11.6180501086129,11.7333845017257,11.8487023154049,11.9641311047711,12.0796198011564,
12.1953197159756,12.2598289068078,12.3751876429801,12.4903373625612,12.605371537628,
12.7203375249411,12.8352825749272,12.9503349124734,13.0654445419192,13.1807657388827,
13.2482190453035,13.3637725587923,13.4791207741952,13.5943555713228,13.7095239270441,
13.8246727146767,13.9399292713301,14.0552436848736,14.1707681415781,14.2366091837992,
14.3521052552483,14.4674378367289,14.5826541109109,14.6978010922988,14.8129875625007,
14.9281889246498,15.0435538422179,15.1339731442208),.UNSPECIFIED.);
#56=B_SPLINE_CURVE_WITH_KNOTS('',3,(#2867,#2868,#2869,#2870,#2871,#2872,
#2873,#2874,#2875,#2876,#2877,#2878,#2879,#2880,#2881,#2882,#2883,#2884,
#2885,#2886,#2887,#2888,#2889,#2890,#2891,#2892,#2893,#2894,#2895,#2896,
#2897,#2898,#2899,#2900,#2901,#2902,#2903,#2904,#2905,#2906,#2907,#2908,
#2909,#2910,#2911,#2912,#2913,#2914,#2915,#2916,#2917,#2918,#2919,#2920,
#2921,#2922,#2923,#2924,#2925,#2926,#2927,#2928,#2929,#2930,#2931,#2932,
#2933,#2934,#2935,#2936,#2937,#2938,#2939,#2940,#2941,#2942,#2943,#2944,
#2945,#2946,#2947,#2948,#2949,#2950,#2951,#2952,#2953,#2954,#2955,#2956,
#2957,#2958,#2959,#2960,#2961,#2962,#2963),.UNSPECIFIED.,.F.,.F.,(4,3,3,
3,3,3,3,3,3,3,3,3,3,3,3,3,3,3,3,3,3,3,3,3,3,3,3,3,3,3,3,3,4),(11.6156374476063,
11.7391862149183,11.8573028306364,11.9753941171691,12.0934978467133,12.2116517975586,
12.329985894632,12.4484221855639,12.5670917656992,12.6040275861021,12.7183681437411,
12.8324766304615,12.9464559897273,13.0603553078476,13.1742235395948,13.2881915462384,
13.4022107702393,13.5164447310029,13.5924177245978,13.7081224421998,13.8236218489584,
13.9390076808891,14.0543266075558,14.1696251946564,14.2850291383448,14.4004897681705,
14.5161568443809,14.5808078630935,14.6965062137723,14.8120136139633,14.9274078470399,
15.0427609094787,15.1341554268676),.UNSPECIFIED.);
#57=B_SPLINE_CURVE_WITH_KNOTS('',3,(#2969,#2970,#2971,#2972,#2973,#2974,
#2975,#2976,#2977,#2978,#2979,#2980,#2981,#2982,#2983,#2984,#2985,#2986,
#2987,#2988,#2989,#2990,#2991,#2992,#2993,#2994,#2995,#2996,#2997,#2998,
#2999,#3000,#3001,#3002,#3003,#3004,#3005,#3006,#3007,#3008,#3009,#3010,
#3011,#3012,#3013,#3014,#3015,#3016,#3017,#3018,#3019,#3020,#3021,#3022,
#3023,#3024,#3025,#3026,#3027,#3028,#3029,#3030,#3031,#3032,#3033,#3034,
#3035,#3036,#3037,#3038,#3039,#3040,#3041,#3042,#3043,#3044,#3045,#3046,
#3047,#3048,#3049,#3050,#3051,#3052,#3053,#3054,#3055,#3056,#3057,#3058,
#3059,#3060,#3061,#3062,#3063,#3064,#3065,#3066,#3067,#3068,#3069,#3070,
#3071,#3072,#3073,#3074,#3075,#3076,#3077,#3078,#3079,#3080,#3081,#3082,
#3083,#3084,#3085,#3086,#3087,#3088,#3089,#3090,#3091,#3092,#3093,#3094,
#3095,#3096,#3097,#3098,#3099,#3100,#3101,#3102,#3103,#3104,#3105,#3106,
#3107,#3108,#3109,#3110,#3111,#3112,#3113,#3114,#3115,#3116,#3117,#3118,
#3119,#3120,#3121,#3122,#3123,#3124,#3125,#3126,#3127,#3128,#3129,#3130),
 .UNSPECIFIED.,.F.,.F.,(4,2,2,2,2,2,2,2,2,2,2,2,2,2,2,2,2,2,2,2,2,2,2,2,
2,2,2,2,2,2,2,2,2,2,2,2,2,2,2,2,2,2,2,2,2,2,2,2,2,2,2,2,2,2,2,2,2,2,2,2,
2,2,2,2,2,2,2,2,2,2,2,2,2,2,2,2,2,2,2,2,4),(-0.782733604482233,-0.770157826719555,
-0.75276206461562,-0.749117370176853,-0.746928419369716,-0.744809097682532,
-0.741494339600281,-0.729784458095009,-0.699450263751413,-0.687219107000443,
-0.682196332555423,-0.678553517357403,-0.674699027671161,-0.668554315985148,
-0.643216717155835,-0.618451838435992,-0.614233101788583,-0.611898861798471,
-0.60985120678557,-0.606936417014568,-0.599096973822123,-0.585625401079225,
-0.554603092751879,-0.548267267232944,-0.544373902366787,-0.54074736296389,
-0.535831177246758,-0.52348909216597,-0.502676938067557,-0.482047164365493,
-0.478333961048462,-0.476130270859124,-0.474021706684097,-0.470760189917674,
-0.459690893796215,-0.433537235515639,-0.417340314888203,-0.411904812651969,
-0.40856057787087,-0.404881436392131,-0.399643933838947,-0.384522469156377,
-0.351092146048453,-0.344691775828512,-0.342166120108992,-0.340124695693966,
-0.337840686644481,-0.333745862398689,-0.328456060128697,-0.315438052231705,
-0.283483619822755,-0.277271769532392,-0.27340351470766,-0.269766608754107,
-0.26478253529075,-0.251911110080875,-0.23086309942583,-0.21262219916004,
-0.208132631152173,-0.20574057158714,-0.203910420600591,-0.201234128576658,
-0.195031417186624,-0.155419068666847,-0.144854541725996,-0.14013624586591,
-0.136525144863413,-0.132582005105212,-0.126004554399748,-0.105669836784276,
-0.0827148084467963,-0.07441218539548,-0.0713588103952259,-0.069309766435704,
-0.0670468362556635,-0.0630459662546947,-0.0419052067838259,-0.0135949473602621,
-0.00699940792823476,-0.00321792908897172,-0.000389459724301548),
 .UNSPECIFIED.);
#58=B_SPLINE_CURVE_WITH_KNOTS('',3,(#3131,#3132,#3133,#3134,#3135,#3136,
#3137,#3138,#3139,#3140,#3141,#3142,#3143,#3144,#3145,#3146),
 .UNSPECIFIED.,.F.,.F.,(4,3,3,3,3,4),(15.1339731442208,15.2249993222949,
15.3467969573775,15.4683336435129,15.5895226840091,15.707963267538),
 .UNSPECIFIED.);
#59=B_SPLINE_CURVE_WITH_KNOTS('',3,(#3148,#3149,#3150,#3151,#3152,#3153,
#3154,#3155,#3156,#3157,#3158,#3159,#3160,#3161,#3162,#3163),
 .UNSPECIFIED.,.F.,.F.,(4,3,3,3,3,4),(15.1341554268676,15.2495770896519,
15.3650499947019,15.4807417632621,15.5691980015892,15.7079632679489),
 .UNSPECIFIED.);
#60=B_SPLINE_CURVE_WITH_KNOTS('',3,(#3164,#3165,#3166,#3167,#3168,#3169,
#3170,#3171,#3172),.UNSPECIFIED.,.F.,.F.,(4,1,1,1,1,1,4),(15.7079705185665,
16.5575881400849,17.5459782785806,18.5343684170764,19.5227585555721,20.5111486940678,
21.4170854462023),.UNSPECIFIED.);
#61=B_SPLINE_CURVE_WITH_KNOTS('',3,(#3177,#3178,#3179,#3180,#3181,#3182,
#3183,#3184,#3185,#3186,#3187,#3188,#3189,#3190,#3191,#3192,#3193,#3194,
#3195,#3196,#3197,#3198,#3199,#3200,#3201,#3202,#3203,#3204,#3205,#3206,
#3207,#3208,#3209,#3210,#3211,#3212,#3213,#3214,#3215,#3216,#3217,#3218,
#3219,#3220,#3221,#3222,#3223,#3224,#3225,#3226,#3227,#3228,#3229,#3230,
#3231,#3232,#3233,#3234,#3235,#3236,#3237,#3238,#3239,#3240,#3241,#3242,
#3243,#3244,#3245,#3246,#3247,#3248,#3249,#3250,#3251,#3252,#3253,#3254,
#3255,#3256,#3257,#3258,#3259,#3260,#3261,#3262,#3263,#3264,#3265,#3266,
#3267,#3268,#3269,#3270,#3271,#3272,#3273,#3274,#3275,#3276,#3277,#3278,
#3279,#3280,#3281,#3282,#3283,#3284,#3285,#3286,#3287,#3288,#3289,#3290,
#3291,#3292,#3293,#3294,#3295,#3296,#3297,#3298,#3299,#3300,#3301,#3302,
#3303,#3304,#3305,#3306,#3307,#3308,#3309,#3310,#3311,#3312,#3313,#3314,
#3315,#3316,#3317,#3318,#3319,#3320,#3321,#3322,#3323,#3324,#3325,#3326,
#3327,#3328,#3329,#3330,#3331,#3332,#3333,#3334,#3335,#3336,#3337,#3338,
#3339,#3340,#3341,#3342,#3343,#3344,#3345,#3346,#3347,#3348,#3349,#3350,
#3351,#3352,#3353,#3354,#3355,#3356,#3357,#3358,#3359,#3360,#3361,#3362,
#3363,#3364,#3365,#3366,#3367,#3368),.UNSPECIFIED.,.F.,.F.,(4,2,2,2,2,2,
2,2,2,2,2,2,2,2,2,2,2,2,2,2,2,2,2,2,2,2,2,2,2,2,2,2,2,2,2,2,2,2,2,2,2,2,
2,2,2,2,2,2,2,2,2,2,2,2,2,2,2,2,2,2,2,2,2,2,2,2,2,2,2,2,2,2,2,2,2,2,2,2,
2,2,2,2,2,2,2,2,2,2,2,2,2,2,2,2,2,4),(-1.64352268459931,-1.63476883123318,
-1.63402567322011,-1.63342722906353,-1.63292767441782,-1.63249448823608,
-1.63210359140578,-1.63173566873332,-1.62780587104402,-1.62419491063142,
-1.61945946059501,-1.60875406191175,-1.5692722504643,-1.5630868427994,-1.56041499772771,
-1.55858668142764,-1.55619511324214,-1.55170442358894,-1.53342756718608,
-1.51705128748056,-1.50592128959387,-1.49762536274893,-1.49334906035993,
-1.4897823637737,-1.48548962780102,-1.47736787756967,-1.44698876904348,
-1.43527580264051,-1.42809762035076,-1.42527413818368,-1.42323930798832,
-1.42085734706968,-1.41641262574429,-1.39903345895037,-1.37692223120475,
-1.36418266009999,-1.35921637524091,-1.35558312958256,-1.35171026497336,
-1.34547166682427,-1.31371775484136,-1.30060020677027,-1.2928893692202,
-1.28999220021456,-1.2879476520995,-1.28560577432011,-1.28134973805828,
-1.25735089556425,-1.23089283838892,-1.22498034484753,-1.22117299188316,
-1.21754720293339,-1.21320927324726,-1.20251111723102,-1.16307507571946,
-1.15689929284964,-1.15422874640166,-1.15240033106973,-1.15000720512386,
-1.14551018571139,-1.12715260273344,-1.11038923180556,-1.09423498228552,
-1.08889918402023,-1.08520242147841,-1.08143559157495,-1.07573053130373,
-1.05538329047308,-1.02661649144373,-1.02116808771719,-1.01862165983652,
-1.01680350549185,-1.01431190689201,-1.00916448883525,-0.983352029504981,
-0.96760342616325,-0.957126394053837,-0.952478022594186,-0.948887423589241,
-0.944871769636762,-0.937927475085164,-0.90016904700671,-0.887657233503014,
-0.884281596906025,-0.882149647187371,-0.879975814846629,-0.876402543393401,
-0.861433002233763,-0.827960396031091,-0.820971161790752,-0.816561960136959,
-0.812991188864477,-0.80881638959142,-0.801062101183388,-0.785939975109009,
-0.782733604482233),.UNSPECIFIED.);
#62=B_SPLINE_CURVE_WITH_KNOTS('',3,(#3370,#3371,#3372,#3373,#3374),
 .UNSPECIFIED.,.F.,.F.,(4,1,4),(21.4170854462023,21.4995388325635,21.9911484110583),
 .UNSPECIFIED.);
#63=B_SPLINE_CURVE_WITH_KNOTS('',3,(#3375,#3376,#3377,#3378,#3379,#3380,
#3381,#3382,#3383,#3384,#3385,#3386,#3387,#3388,#3389,#3390,#3391,#3392,
#3393,#3394,#3395,#3396,#3397,#3398,#3399,#3400,#3401,#3402,#3403,#3404,
#3405,#3406,#3407,#3408,#3409,#3410,#3411,#3412,#3413,#3414,#3415,#3416,
#3417,#3418,#3419,#3420,#3421,#3422,#3423,#3424,#3425,#3426,#3427,#3428,
#3429,#3430,#3431,#3432,#3433,#3434,#3435,#3436,#3437,#3438,#3439,#3440,
#3441,#3442,#3443,#3444,#3445,#3446,#3447,#3448,#3449,#3450,#3451,#3452,
#3453,#3454,#3455,#3456,#3457,#3458,#3459,#3460,#3461,#3462,#3463,#3464,
#3465,#3466,#3467,#3468,#3469,#3470,#3471,#3472,#3473,#3474,#3475,#3476,
#3477,#3478,#3479,#3480,#3481,#3482,#3483,#3484,#3485,#3486,#3487,#3488,
#3489,#3490,#3491,#3492,#3493,#3494,#3495,#3496,#3497,#3498,#3499,#3500,
#3501,#3502,#3503,#3504,#3505,#3506,#3507,#3508,#3509,#3510,#3511,#3512,
#3513,#3514,#3515,#3516,#3517,#3518,#3519,#3520,#3521,#3522,#3523,#3524,
#3525,#3526,#3527,#3528,#3529,#3530,#3531,#3532,#3533,#3534,#3535,#3536,
#3537,#3538,#3539,#3540),.UNSPECIFIED.,.F.,.F.,(4,2,2,2,2,2,2,2,2,2,2,2,
2,2,2,2,2,2,2,2,2,2,2,2,2,2,2,2,2,2,2,2,2,2,2,2,2,2,2,2,2,2,2,2,2,2,2,2,
2,2,2,2,2,2,2,2,2,2,2,2,2,2,2,2,2,2,2,2,2,2,2,2,2,2,2,2,2,2,2,2,2,2,4),
(-1.72167836190146,-1.71993697657055,-1.71759155374419,-1.71275393978564,
-1.69882493517257,-1.66371621695858,-1.65747769739599,-1.6547979341954,
-1.65296929384515,-1.65058468672109,-1.64612528794294,-1.62511269287794,
-1.60556984059511,-1.59365078975702,-1.58879339412367,-1.58517730292486,
-1.58126424068391,-1.57482320787054,-1.5446452837465,-1.53072619827246,
-1.5227305689983,-1.51979650989599,-1.51774702764271,-1.51542452751536,
-1.51125629876888,-1.48585371079696,-1.46889497034311,-1.45792728782081,
-1.45320590782008,-1.44960839891158,-1.44563451111625,-1.43889109860587,
-1.41339125332872,-1.39655335652045,-1.38762130909995,-1.38457395257359,
-1.38250630070754,-1.38023319674731,-1.37618651598821,-1.34924651957977,
-1.3330791763852,-1.32571908232761,-1.31959747558421,-1.31574921255501,
-1.31210671097212,-1.3070753685696,-1.29477440026756,-1.26451274654844,
-1.25281244979044,-1.24949948968538,-1.24738135437933,-1.24519366027113,
-1.24155138653956,-1.22417074368823,-1.20840430116804,-1.19554919003907,
-1.18638082906214,-1.18194887606309,-1.17837865509488,-1.17422580645375,
-1.16679565946455,-1.12996502559649,-1.11753613239243,-1.1141675860736,
-1.11203782863533,-1.10986385442139,-1.10628663816915,-1.09120189733225,
-1.06618465948351,-1.05265511829926,-1.04759291403465,-1.04394490788819,
-1.04010573458198,-1.0340315116068,-1.00113166622705,-0.988561855242318,
-0.983380941651227,-0.979350457118574,-0.977080447749138,-0.975034464511672,
-0.972486208839398,-0.965923306996879,-0.939600795071122),.UNSPECIFIED.);
#64=B_SPLINE_CURVE_WITH_KNOTS('',3,(#3546,#3547,#3548,#3549,#3550,#3551,
#3552,#3553,#3554,#3555,#3556,#3557,#3558,#3559,#3560,#3561,#3562,#3563,
#3564,#3565,#3566,#3567,#3568,#3569,#3570,#3571,#3572,#3573,#3574,#3575,
#3576,#3577,#3578,#3579,#3580,#3581,#3582,#3583,#3584,#3585,#3586,#3587,
#3588,#3589,#3590,#3591,#3592,#3593,#3594,#3595,#3596,#3597,#3598,#3599,
#3600,#3601,#3602,#3603,#3604,#3605,#3606,#3607,#3608,#3609,#3610,#3611,
#3612,#3613,#3614,#3615,#3616,#3617,#3618,#3619,#3620,#3621,#3622,#3623,
#3624,#3625,#3626,#3627,#3628,#3629,#3630,#3631,#3632,#3633,#3634,#3635,
#3636,#3637,#3638,#3639,#3640,#3641,#3642,#3643,#3644,#3645,#3646,#3647,
#3648,#3649,#3650,#3651,#3652,#3653,#3654,#3655,#3656,#3657,#3658,#3659,
#3660,#3661,#3662,#3663,#3664,#3665,#3666,#3667,#3668,#3669,#3670,#3671,
#3672,#3673,#3674,#3675,#3676,#3677,#3678,#3679,#3680,#3681,#3682,#3683,
#3684,#3685,#3686,#3687,#3688,#3689,#3690,#3691,#3692,#3693,#3694,#3695,
#3696,#3697,#3698,#3699,#3700,#3701,#3702,#3703,#3704,#3705,#3706,#3707),
 .UNSPECIFIED.,.F.,.F.,(4,2,2,2,2,2,2,2,2,2,2,2,2,2,2,2,2,2,2,2,2,2,2,2,
2,2,2,2,2,2,2,2,2,2,2,2,2,2,2,2,2,2,2,2,2,2,2,2,2,2,2,2,2,2,2,2,2,2,2,2,
2,2,2,2,2,2,2,2,2,2,2,2,2,2,2,2,2,2,2,2,4),(-0.782696160082662,-0.781075359436944,
-0.77328328598361,-0.759943173937005,-0.728660283751481,-0.722359348904134,
-0.718473432435426,-0.714844722566713,-0.709911259337837,-0.697433398901302,
-0.676189046787961,-0.657661695477911,-0.653151516600006,-0.650755543412031,
-0.64892740805726,-0.646260580729097,-0.640108143481001,-0.600792497984823,
-0.590002994722619,-0.585651102005755,-0.582021754183454,-0.578219105711645,
-0.57233195335054,-0.565342597230487,-0.550560881162287,-0.527434583566802,
-0.519350947839438,-0.516327317227424,-0.514283286352171,-0.512006654137859,
-0.507946245131807,-0.502715089205647,-0.489938841318079,-0.457512448786117,
-0.451372549004067,-0.447519497986136,-0.443876944512898,-0.438852758095078,
-0.425649222564851,-0.406155914027626,-0.386778717188384,-0.382304629054381,
-0.37991643578708,-0.378087344850847,-0.375410016595597,-0.369191515686781,
-0.334159908112979,-0.320176506576414,-0.314947068059239,-0.31130634470972,
-0.307522347694134,-0.301727987493547,-0.277429585680445,-0.250569432024096,
-0.246508918257079,-0.244232316155977,-0.242164751680355,-0.239122043078044,
-0.230237091346038,-0.21356032098588,-0.187860668751238,-0.181119888635252,
-0.177145423124215,-0.173546012975649,-0.168820063054617,-0.157830956802909,
-0.140820171809713,-0.115418730256182,-0.111223191176004,-0.108918504830981,
-0.106861841514575,-0.10388561497163,-0.0955600489989513,-0.0806694248799056,
-0.0522417527946656,-0.0456226622466711,-0.0416726117827746,-0.038066367541658,
-0.0332884890336368,-0.0279803390021662,-0.000387520461421266),
 .UNSPECIFIED.);
#65=B_SPLINE_CURVE_WITH_KNOTS('',3,(#3708,#3709,#3710,#3711,#3712,#3713,
#3714,#3715,#3716,#3717,#3718,#3719,#3720,#3721,#3722,#3723,#3724,#3725,
#3726,#3727,#3728,#3729),.UNSPECIFIED.,.F.,.F.,(4,2,2,2,2,2,2,2,2,2,4),
(-1.72194463547043,-1.70657072393317,-1.70042690145371,-1.69777394834495,
-1.69578717472258,-1.69396043674524,-1.69156103513742,-1.68703187060117,
-1.66702483672176,-1.64687581390891,-1.64352268459931),.UNSPECIFIED.);
#66=B_SPLINE_CURVE_WITH_KNOTS('',3,(#3730,#3731,#3732,#3733,#3734,#3735,
#3736,#3737,#3738,#3739,#3740,#3741,#3742,#3743,#3744,#3745,#3746,#3747,
#3748,#3749,#3750,#3751,#3752,#3753,#3754,#3755,#3756,#3757,#3758,#3759,
#3760,#3761,#3762,#3763,#3764,#3765,#3766,#3767,#3768,#3769,#3770,#3771,
#3772,#3773,#3774,#3775,#3776,#3777,#3778,#3779,#3780,#3781,#3782,#3783,
#3784,#3785,#3786,#3787,#3788,#3789,#3790,#3791,#3792,#3793,#3794,#3795,
#3796,#3797,#3798,#3799,#3800,#3801,#3802,#3803,#3804,#3805,#3806,#3807,
#3808,#3809,#3810,#3811,#3812,#3813,#3814,#3815,#3816,#3817,#3818,#3819,
#3820,#3821,#3822,#3823,#3824,#3825,#3826,#3827,#3828,#3829,#3830,#3831,
#3832,#3833,#3834,#3835,#3836,#3837,#3838,#3839,#3840,#3841,#3842,#3843,
#3844,#3845,#3846,#3847,#3848,#3849,#3850,#3851,#3852,#3853,#3854,#3855,
#3856,#3857,#3858,#3859,#3860,#3861,#3862,#3863,#3864,#3865,#3866,#3867,
#3868,#3869,#3870,#3871,#3872,#3873,#3874,#3875,#3876,#3877,#3878,#3879,
#3880,#3881,#3882,#3883,#3884,#3885,#3886,#3887,#3888,#3889,#3890,#3891,
#3892,#3893,#3894,#3895,#3896,#3897,#3898,#3899,#3900,#3901,#3902,#3903,
#3904,#3905,#3906,#3907,#3908,#3909,#3910,#3911,#3912,#3913,#3914,#3915,
#3916,#3917,#3918,#3919,#3920,#3921,#3922,#3923,#3924,#3925),
 .UNSPECIFIED.,.F.,.F.,(4,2,2,2,2,2,2,2,2,2,2,2,2,2,2,2,2,2,2,2,2,2,2,2,
2,2,2,2,2,2,2,2,2,2,2,2,2,2,2,2,2,2,2,2,2,2,2,2,2,2,2,2,2,2,2,2,2,2,2,2,
2,2,2,2,2,2,2,2,2,2,2,2,2,2,2,2,2,2,2,2,2,2,2,2,2,2,2,2,2,2,2,2,2,2,2,2,
2,4),(-0.939600795071122,-0.932717148076296,-0.917632823774098,-0.9124005620682,
-0.908723319768595,-0.905379625484532,-0.899942432619131,-0.883717300430899,
-0.860937298427964,-0.847041736435776,-0.843517470395148,-0.841354761086481,
-0.839214912310399,-0.835798343305456,-0.822668703892458,-0.80575122815367,
-0.783436435022837,-0.777665319611758,-0.773886343430266,-0.770200819731045,
-0.764922551296239,-0.749376473166826,-0.721630035673222,-0.711176169236045,
-0.70789057995898,-0.705986402194631,-0.703851850256852,-0.700460890191082,
-0.687713974493037,-0.655791590508192,-0.645358358723685,-0.640767424507792,
-0.637175608797507,-0.633173640104625,-0.626292979332825,-0.617689148495527,
-0.596017374181675,-0.57803188698761,-0.573559118290177,-0.5711714763914,
-0.56934276614162,-0.566666047165555,-0.560449441082152,-0.525430769435245,
-0.511429584698833,-0.506199184352612,-0.502558836983457,-0.498776154320935,
-0.492985828748129,-0.468822278209715,-0.441775527532032,-0.437737050858496,
-0.435465320637159,-0.433396271425122,-0.430343182663081,-0.421364327021702,
-0.404369052008774,-0.379111419379661,-0.372364948337714,-0.368389832518859,
-0.364791513619253,-0.360069520952884,-0.349103523026432,-0.332151101588875,
-0.306687660057606,-0.302520813698895,-0.300198277096951,-0.298148246382424,
-0.295212728180463,-0.287207763946105,-0.273264386051648,-0.243145515932078,
-0.236697957531038,-0.232783084112019,-0.229166675364196,-0.224310979526816,
-0.212410122899578,-0.192924298824382,-0.171802139490986,-0.167329524256459,
-0.164941787808227,-0.163112898266531,-0.160435775156034,-0.154217572548377,
-0.11919175918273,-0.105194031282819,-0.0999635744661058,-0.0963229798264828,
-0.0925398662353551,-0.0921654860774136,-0.0918035472410569,-0.0914351641230606,
-0.0910427653025588,-0.0906068878656257,-0.0901031203839437,-0.08949837617733,
-0.0793554662889542,-0.0788478650889102),.UNSPECIFIED.);
#67=B_SPLINE_CURVE_WITH_KNOTS('',3,(#3930,#3931,#3932,#3933,#3934,#3935,
#3936,#3937,#3938,#3939,#3940,#3941,#3942,#3943,#3944,#3945,#3946,#3947,
#3948,#3949,#3950,#3951,#3952,#3953,#3954,#3955,#3956,#3957,#3958,#3959,
#3960,#3961,#3962,#3963,#3964,#3965,#3966,#3967,#3968,#3969,#3970,#3971,
#3972,#3973,#3974,#3975,#3976,#3977,#3978,#3979,#3980,#3981,#3982,#3983,
#3984,#3985,#3986,#3987,#3988,#3989,#3990,#3991,#3992,#3993,#3994,#3995,
#3996,#3997,#3998,#3999,#4000,#4001,#4002,#4003,#4004,#4005,#4006,#4007,
#4008,#4009,#4010,#4011,#4012,#4013,#4014,#4015,#4016,#4017,#4018,#4019,
#4020,#4021,#4022,#4023,#4024,#4025,#4026,#4027,#4028,#4029,#4030,#4031,
#4032,#4033,#4034,#4035,#4036,#4037,#4038,#4039,#4040,#4041,#4042,#4043,
#4044,#4045,#4046,#4047,#4048,#4049,#4050,#4051,#4052,#4053,#4054,#4055,
#4056,#4057,#4058,#4059,#4060,#4061,#4062,#4063,#4064,#4065,#4066,#4067,
#4068,#4069,#4070,#4071,#4072,#4073,#4074,#4075,#4076,#4077,#4078,#4079,
#4080,#4081,#4082,#4083,#4084,#4085,#4086,#4087,#4088,#4089,#4090,#4091,
#4092,#4093,#4094,#4095,#4096,#4097,#4098,#4099,#4100,#4101,#4102,#4103,
#4104,#4105,#4106,#4107,#4108,#4109),.UNSPECIFIED.,.F.,.F.,(4,2,2,2,2,2,
2,2,2,2,2,2,2,2,2,2,2,2,2,2,2,2,2,2,2,2,2,2,2,2,2,2,2,2,2,2,2,2,2,2,2,2,
2,2,2,2,2,2,2,2,2,2,2,2,2,2,2,2,2,2,2,2,2,2,2,2,2,2,2,2,2,2,2,2,2,2,2,2,
2,2,2,2,2,2,2,2,2,2,2,4),(-1.64346459097191,-1.64299413827663,-1.60796975239201,
-1.6017559312754,-1.59907926671871,-1.5972502157541,-1.59486139517667,-1.59038465729976,
-1.56963813329225,-1.54992778993481,-1.53795045785992,-1.53308401710661,
-1.5294655530535,-1.52555400213521,-1.51912511836203,-1.48882360767624,
-1.47496353663432,-1.46698761973969,-1.46405548679376,-1.46200570953533,
-1.45968076959513,-1.45550398171545,-1.4252496372731,-1.40838548913298,
-1.40056168432393,-1.39637401719785,-1.39280457146821,-1.38841267239701,
-1.38148422401653,-1.3504592528106,-1.3385868028233,-1.33134573927208,-1.32851313448038,
-1.32647704048686,-1.32410000184642,-1.31967922697425,-1.29884880166951,
-1.27913162015462,-1.26715197464246,-1.26228522492473,-1.25866672120616,
-1.25475530651898,-1.24832707393271,-1.21802031498721,-1.20416306979233,
-1.19618814522604,-1.19325614366897,-1.1912063888698,-1.18888139248743,
-1.1847043319608,-1.15938494526366,-1.142376348639,-1.13138780338708,-1.12666202358827,
-1.12306261093225,-1.11908800218368,-1.11234672668275,-1.08657737364282,
-1.06992745641147,-1.06105017813285,-1.05800822450704,-1.05594078084827,
-1.05366381075885,-1.04960170177527,-1.02277818054436,-0.998474338397782,
-0.992680506752823,-0.988896508027428,-0.985255508738456,-0.980025222524119,
-0.966039063831574,-0.9309824122132,-0.924760376413454,-0.922082302038895,
-0.920253017744464,-0.917864948848926,-0.913392116657112,-0.89399184135791,
-0.874466378027543,-0.861324738321179,-0.856307941661326,-0.852666281657645,
-0.848810171301246,-0.842656515975083,-0.817047434013356,-0.792599030371879,
-0.788367002157873,-0.786030038314498,-0.783983588999409,-0.782696160082662),
 .UNSPECIFIED.);
#68=B_SPLINE_CURVE_WITH_KNOTS('',3,(#4111,#4112,#4113,#4114,#4115,#4116,
#4117,#4118,#4119,#4120,#4121,#4122,#4123,#4124,#4125,#4126,#4127,#4128,
#4129,#4130),.UNSPECIFIED.,.F.,.F.,(4,2,2,2,2,2,2,2,2,4),(-0.0788478650889102,
-0.0642475044479353,-0.0404188851012244,-0.0332561931473402,-0.0303676396375803,
-0.0283245362340553,-0.0259788937490618,-0.0234388254342997,-0.0172068433153215,
-0.000387300569270395),.UNSPECIFIED.);
#69=B_SPLINE_CURVE_WITH_KNOTS('',3,(#4131,#4132,#4133,#4134,#4135,#4136,
#4137,#4138,#4139,#4140,#4141,#4142,#4143,#4144,#4145,#4146,#4147,#4148,
#4149,#4150,#4151,#4152,#4153,#4154,#4155,#4156,#4157,#4158,#4159,#4160,
#4161,#4162,#4163,#4164,#4165,#4166,#4167,#4168,#4169,#4170,#4171,#4172,
#4173,#4174,#4175,#4176,#4177,#4178,#4179,#4180,#4181,#4182,#4183,#4184,
#4185,#4186,#4187,#4188,#4189,#4190,#4191,#4192,#4193,#4194,#4195,#4196,
#4197,#4198,#4199,#4200,#4201,#4202,#4203,#4204,#4205,#4206,#4207,#4208,
#4209,#4210,#4211,#4212,#4213,#4214,#4215,#4216,#4217,#4218,#4219,#4220,
#4221,#4222,#4223,#4224,#4225,#4226,#4227,#4228,#4229,#4230,#4231,#4232,
#4233,#4234,#4235,#4236,#4237,#4238,#4239,#4240,#4241,#4242,#4243,#4244,
#4245,#4246,#4247,#4248,#4249,#4250,#4251,#4252,#4253,#4254,#4255,#4256,
#4257,#4258,#4259,#4260,#4261,#4262,#4263,#4264,#4265,#4266,#4267,#4268,
#4269,#4270,#4271,#4272,#4273,#4274,#4275,#4276,#4277,#4278,#4279,#4280,
#4281,#4282,#4283,#4284,#4285,#4286,#4287,#4288,#4289,#4290),
 .UNSPECIFIED.,.F.,.F.,(4,2,2,2,2,2,2,2,2,2,2,2,2,2,2,2,2,2,2,2,2,2,2,2,
2,2,2,2,2,2,2,2,2,2,2,2,2,2,2,2,2,2,2,2,2,2,2,2,2,2,2,2,2,2,2,2,2,2,2,2,
2,2,2,2,2,2,2,2,2,2,2,2,2,2,2,2,2,2,2,4),(-1.72212022081959,-1.69533255126009,
-1.69016620326192,-1.68548487803012,-1.68189175424043,-1.67789649965908,
-1.67104880052373,-1.64319535086452,-1.62817535772164,-1.61980786069624,
-1.61682697356166,-1.61477011898971,-1.61246876126964,-1.608287201836,-1.58276749554589,
-1.56583942628212,-1.55488319703798,-1.55016308540602,-1.54656530829544,
-1.54258989694887,-1.53584074254029,-1.51074305238622,-1.49361456735207,
-1.48459693358426,-1.48153955145949,-1.47946991782762,-1.47720016742003,
-1.47317058363322,-1.44607880187779,-1.4219757593487,-1.41618827508326,
-1.41240633530046,-1.40876588353763,-1.40353390814182,-1.38951623832309,
-1.35448975970563,-1.34827376895779,-1.34559715869928,-1.34376851903516,
-1.34138088223878,-1.33690805107266,-1.31755743222477,-1.29687415221088,
-1.28457549796112,-1.2796667260237,-1.27604277973669,-1.27214958370109,
-1.26580819035222,-1.23481396078216,-1.22131195958812,-1.21346267796392,
-1.21054746122841,-1.20850060609653,-1.20616853471792,-1.20195704402135,
-1.17711230455999,-1.15983401972054,-1.14874058829289,-1.14399999259999,
-1.14039947759935,-1.1364337461265,-1.1297333389673,-1.10254495760731,-1.08022989891291,
-1.0762296836793,-1.07396592620081,-1.07191704560627,-1.06886284387474,
-1.06054663348016,-1.03762421930456,-1.01561681822763,-1.00990048309864,
-1.00613206715272,-1.00248089192403,-0.997190584484555,-0.982741672931519,
-0.954828205269458,-0.94346779079941,-0.940181863111125,-0.939838537595481),
 .UNSPECIFIED.);
#70=B_SPLINE_CURVE_WITH_KNOTS('',3,(#4296,#4297,#4298,#4299,#4300,#4301,
#4302,#4303,#4304,#4305,#4306,#4307,#4308,#4309,#4310,#4311,#4312,#4313,
#4314,#4315,#4316,#4317,#4318,#4319,#4320,#4321,#4322,#4323,#4324,#4325,
#4326,#4327,#4328,#4329,#4330,#4331,#4332,#4333,#4334,#4335,#4336,#4337,
#4338,#4339,#4340,#4341,#4342,#4343,#4344,#4345,#4346,#4347,#4348,#4349,
#4350,#4351,#4352,#4353,#4354,#4355,#4356,#4357,#4358,#4359,#4360,#4361,
#4362,#4363,#4364,#4365,#4366,#4367,#4368,#4369,#4370,#4371,#4372,#4373,
#4374,#4375,#4376,#4377,#4378,#4379,#4380,#4381,#4382,#4383,#4384,#4385,
#4386,#4387,#4388,#4389,#4390,#4391,#4392,#4393,#4394,#4395,#4396,#4397,
#4398,#4399,#4400,#4401,#4402,#4403,#4404,#4405,#4406,#4407,#4408,#4409,
#4410,#4411,#4412,#4413,#4414,#4415,#4416,#4417,#4418,#4419,#4420,#4421,
#4422,#4423,#4424,#4425,#4426,#4427,#4428,#4429,#4430,#4431,#4432,#4433,
#4434,#4435,#4436,#4437,#4438,#4439,#4440,#4441,#4442,#4443,#4444,#4445,
#4446,#4447,#4448,#4449,#4450,#4451,#4452,#4453,#4454,#4455,#4456,#4457,
#4458,#4459,#4460,#4461),.UNSPECIFIED.,.F.,.F.,(4,2,2,2,2,2,2,2,2,2,2,2,
2,2,2,2,2,2,2,2,2,2,2,2,2,2,2,2,2,2,2,2,2,2,2,2,2,2,2,2,2,2,2,2,2,2,2,2,
2,2,2,2,2,2,2,2,2,2,2,2,2,2,2,2,2,2,2,2,2,2,2,2,2,2,2,2,2,2,2,2,2,2,4),
(-0.782502334421087,-0.767045137430122,-0.760820555065709,-0.756950338592601,
-0.753315532356511,-0.748340657637774,-0.735536528532295,-0.7146968730885,
-0.696198018516441,-0.691690477241836,-0.689295216228231,-0.687467210754608,
-0.684800027855247,-0.678644291391059,-0.639314047563905,-0.628542905584255,
-0.624194064720761,-0.620565714899577,-0.616762507239646,-0.610871077341131,
-0.584435900353066,-0.560325930300542,-0.556076684174118,-0.553736228853726,
-0.551691167046597,-0.548790976551945,-0.541057453264677,-0.527878239987123,
-0.496281099015622,-0.490024303065802,-0.486147684762659,-0.482515864686925,
-0.477559436979493,-0.464899611680007,-0.443058784216286,-0.425296645812249,
-0.420834926944211,-0.418449329304707,-0.416619786211475,-0.413938572024984,
-0.407696069476743,-0.372570046453006,-0.358693356814788,-0.353473085588776,
-0.349833950363349,-0.346047584087344,-0.340241238759429,-0.315445020904246,
-0.289242090673591,-0.285104823812511,-0.282812264812267,-0.280751252339647,
-0.27774749274177,-0.269194581030825,-0.253599217452694,-0.226310490821413,
-0.219616565852772,-0.215651556287467,-0.212049716427345,-0.207304402611245,
-0.196184105704066,-0.178836600102776,-0.154079317473949,-0.149861090993263,
-0.147527220035567,-0.145480106097394,-0.142566312897634,-0.134730784227824,
-0.121268670610156,-0.0902322400924257,-0.0838995623626038,-0.0800074554591401,
-0.076381670872289,-0.0714658787049653,-0.0591209858206712,-0.0337276219199564,
-0.0175107458707944,-0.0138931708560644,-0.0117101342163253,-0.0098247471181441,
-0.00768948435977741,-0.00452472033345642,-0.000387015215521824),
 .UNSPECIFIED.);
#71=B_SPLINE_CURVE_WITH_KNOTS('',3,(#4462,#4463,#4464,#4465,#4466,#4467,
#4468,#4469,#4470,#4471,#4472,#4473,#4474,#4475,#4476,#4477),
 .UNSPECIFIED.,.F.,.F.,(4,2,2,2,2,2,2,4),(-1.72208794112375,-1.69961702131751,
-1.67546164729257,-1.66967193793774,-1.66588887582809,-1.66224752994355,
-1.65701451805733,-1.64346459097191),.UNSPECIFIED.);
#72=B_SPLINE_CURVE_WITH_KNOTS('',3,(#4478,#4479,#4480,#4481,#4482,#4483,
#4484,#4485,#4486,#4487,#4488,#4489,#4490,#4491,#4492,#4493,#4494,#4495,
#4496,#4497,#4498,#4499,#4500,#4501,#4502,#4503,#4504,#4505,#4506,#4507,
#4508,#4509,#4510,#4511,#4512,#4513,#4514,#4515,#4516,#4517,#4518,#4519,
#4520,#4521,#4522,#4523,#4524,#4525,#4526,#4527,#4528,#4529,#4530,#4531,
#4532,#4533,#4534,#4535,#4536,#4537,#4538,#4539,#4540,#4541,#4542,#4543,
#4544,#4545,#4546,#4547,#4548,#4549,#4550,#4551,#4552,#4553,#4554,#4555,
#4556,#4557,#4558,#4559,#4560,#4561,#4562,#4563,#4564,#4565,#4566,#4567,
#4568,#4569,#4570,#4571,#4572,#4573,#4574,#4575,#4576,#4577,#4578,#4579,
#4580,#4581,#4582,#4583,#4584,#4585,#4586,#4587,#4588,#4589,#4590,#4591,
#4592,#4593,#4594,#4595,#4596,#4597,#4598,#4599,#4600,#4601,#4602,#4603,
#4604,#4605,#4606,#4607,#4608,#4609,#4610,#4611,#4612,#4613,#4614,#4615,
#4616,#4617,#4618,#4619,#4620,#4621,#4622,#4623,#4624,#4625,#4626,#4627,
#4628,#4629,#4630,#4631,#4632,#4633,#4634,#4635,#4636,#4637,#4638,#4639,
#4640,#4641,#4642,#4643,#4644,#4645,#4646,#4647,#4648,#4649,#4650,#4651,
#4652,#4653,#4654,#4655,#4656,#4657),.UNSPECIFIED.,.F.,.F.,(4,2,2,2,2,2,
2,2,2,2,2,2,2,2,2,2,2,2,2,2,2,2,2,2,2,2,2,2,2,2,2,2,2,2,2,2,2,2,2,2,2,2,
2,2,2,2,2,2,2,2,2,2,2,2,2,2,2,2,2,2,2,2,2,2,2,2,2,2,2,2,2,2,2,2,2,2,2,2,
2,2,2,2,2,2,2,2,2,2,2,4),(-0.939838537595481,-0.938068797775664,-0.936145440061214,
-0.932756964776017,-0.92121159401672,-0.893145310333023,-0.878928004304586,
-0.873786974217987,-0.870125352159042,-0.866763503213755,-0.861221197153815,
-0.842434949502465,-0.827724190822388,-0.810285819065485,-0.805837941971229,
-0.803455451934922,-0.801420979433844,-0.7985992975301,-0.791432461321423,
-0.779749286419483,-0.749483422745094,-0.741276929095984,-0.736967781883236,
-0.733401271993392,-0.729141678050981,-0.720934899560516,-0.709972122574217,
-0.69341145547469,-0.674979783703478,-0.670477739758828,-0.6680838892394,
-0.666256103659589,-0.663588218243026,-0.657426430809991,-0.618074466313829,
-0.607320212510232,-0.60297435246546,-0.599347192523239,-0.595543931751392,
-0.589649763658981,-0.563038803090738,-0.539140753286892,-0.534870759234907,
-0.532526113872392,-0.530482759766023,-0.527592431394132,-0.519930340622053,
-0.506946582747292,-0.474944196487876,-0.468743476837958,-0.464878666674533,
-0.461242709787195,-0.456256322976876,-0.443355305630278,-0.422210296904462,
-0.404094785254174,-0.399614521128156,-0.397225295663127,-0.395396838270499,
-0.392722422317909,-0.386520084878706,-0.346968952183938,-0.336339042098344,
-0.331616227157014,-0.328007256916538,-0.324072138519676,-0.31752248052578,
-0.297371999190207,-0.274791687277466,-0.266029135469896,-0.262918384678814,
-0.260859806833145,-0.258617255382973,-0.254717078326282,-0.233608482817605,
-0.204869286252108,-0.198278878746309,-0.194335669425123,-0.190729386192128,
-0.185942115507579,-0.174525341677054,-0.156391882314086,-0.133075844426758,
-0.128718098421515,-0.126354903223532,-0.124316577615172,-0.121461996238531,
-0.11405990954294,-0.101769993493656,-0.079052177473784),.UNSPECIFIED.);
#73=B_SPLINE_CURVE_WITH_KNOTS('',3,(#4662,#4663,#4664,#4665,#4666,#4667,
#4668,#4669,#4670,#4671,#4672,#4673,#4674,#4675,#4676,#4677,#4678,#4679,
#4680,#4681,#4682,#4683,#4684,#4685,#4686,#4687,#4688,#4689,#4690,#4691,
#4692,#4693,#4694,#4695,#4696,#4697,#4698,#4699,#4700,#4701,#4702,#4703,
#4704,#4705,#4706,#4707,#4708,#4709,#4710,#4711,#4712,#4713,#4714,#4715,
#4716,#4717,#4718,#4719,#4720,#4721,#4722,#4723,#4724,#4725,#4726,#4727,
#4728,#4729,#4730,#4731,#4732,#4733,#4734,#4735,#4736,#4737,#4738,#4739,
#4740,#4741,#4742,#4743,#4744,#4745,#4746,#4747,#4748,#4749,#4750,#4751,
#4752,#4753,#4754,#4755,#4756,#4757,#4758,#4759,#4760,#4761,#4762,#4763,
#4764,#4765,#4766,#4767,#4768,#4769,#4770,#4771,#4772,#4773,#4774,#4775,
#4776,#4777,#4778,#4779,#4780,#4781,#4782,#4783,#4784,#4785,#4786,#4787,
#4788,#4789,#4790,#4791,#4792,#4793,#4794,#4795,#4796,#4797,#4798,#4799,
#4800,#4801,#4802,#4803,#4804,#4805,#4806,#4807,#4808,#4809,#4810,#4811,
#4812,#4813,#4814,#4815,#4816,#4817,#4818,#4819,#4820,#4821,#4822,#4823,
#4824,#4825,#4826,#4827,#4828,#4829,#4830,#4831,#4832,#4833,#4834,#4835,
#4836,#4837,#4838,#4839,#4840,#4841,#4842,#4843,#4844,#4845),
 .UNSPECIFIED.,.F.,.F.,(4,2,2,2,2,2,2,2,2,2,2,2,2,2,2,2,2,2,2,2,2,2,2,2,
2,2,2,2,2,2,2,2,2,2,2,2,2,2,2,2,2,2,2,2,2,2,2,2,2,2,2,2,2,2,2,2,2,2,2,2,
2,2,2,2,2,2,2,2,2,2,2,2,2,2,2,2,2,2,2,2,2,2,2,2,2,2,2,2,2,2,2,4),(-1.64297773443279,
-1.64004297846864,-1.63736524041581,-1.63553677967994,-1.63315064508125,
-1.62868346378423,-1.61077294092021,-1.58951056936148,-1.57657617060184,
-1.57158667665708,-1.56795085702201,-1.56408830249779,-1.55789591873041,
-1.52584075523492,-1.51288115910944,-1.50522919089457,-1.50234061161371,
-1.50029788278035,-1.49795303213325,-1.4936806392777,-1.46985579832729,
-1.45199849669385,-1.44068579653118,-1.43591394403918,-1.43230994527066,
-1.42836010309057,-1.42173585057647,-1.39339076853442,-1.37196237222845,
-1.36805141050512,-1.36580669791819,-1.36374935765044,-1.36064508749538,
-1.35193258783187,-1.32934059477822,-1.30919179992477,-1.30264298564033,
-1.29870819515655,-1.29509932434392,-1.29037628677091,-1.27992407545554,
-1.24748833893756,-1.23551372973242,-1.23217916097273,-1.23005644605728,
-1.2278739478477,-1.22425667230072,-1.20814517415559,-1.18397167511406,
-1.17065875800202,-1.16562247331685,-1.16197872269448,-1.15813114870345,
-1.15201503415923,-1.11941795249295,-1.10671426468329,-1.10150099922408,
-1.0974516555762,-1.0951777226073,-1.09313335842651,-1.09010535364877,-1.08198499486996,
-1.05891403633355,-1.04415768158023,-1.03717629397825,-1.03129407456293,
-1.02749306514734,-1.02386417573296,-1.01951146533365,-1.00871276681361,
-0.969394484886577,-0.963242986690139,-0.960576607405278,-0.95874884174587,
-0.956353365951283,-0.951844283119531,-0.933327549125823,-0.916567056098586,
-0.900565618543884,-0.8952442532579,-0.891550456425138,-0.887780882267833,
-0.882060112836508,-0.86097354370312,-0.831179280780422,-0.8269165479703,
-0.824573143044055,-0.822528794713476,-0.819634103208903,-0.811942321610842,
-0.79887808948178,-0.782502334421087),.UNSPECIFIED.);
#74=B_SPLINE_CURVE_WITH_KNOTS('',3,(#4847,#4848,#4849,#4850,#4851,#4852,
#4853,#4854,#4855,#4856,#4857,#4858,#4859,#4860,#4861,#4862),
 .UNSPECIFIED.,.F.,.F.,(4,2,2,2,2,2,2,4),(-0.079052177473784,-0.0689809976460656,
-0.0626536956613715,-0.0587636537041857,-0.0551390412965591,-0.050223731628864,
-0.0378738902713093,-0.000387745880559849),.UNSPECIFIED.);
#75=B_SPLINE_CURVE_WITH_KNOTS('',3,(#4863,#4864,#4865,#4866,#4867,#4868,
#4869,#4870,#4871,#4872,#4873,#4874,#4875,#4876,#4877,#4878,#4879,#4880,
#4881,#4882,#4883,#4884,#4885,#4886,#4887,#4888,#4889,#4890,#4891,#4892,
#4893,#4894,#4895,#4896,#4897,#4898,#4899,#4900,#4901,#4902,#4903,#4904,
#4905,#4906,#4907,#4908,#4909,#4910,#4911,#4912,#4913,#4914,#4915,#4916,
#4917,#4918,#4919,#4920,#4921,#4922,#4923,#4924,#4925,#4926,#4927,#4928,
#4929,#4930,#4931,#4932,#4933,#4934,#4935,#4936,#4937,#4938,#4939,#4940,
#4941,#4942,#4943,#4944,#4945,#4946,#4947,#4948,#4949,#4950,#4951,#4952,
#4953,#4954,#4955,#4956,#4957,#4958,#4959,#4960,#4961,#4962,#4963,#4964,
#4965,#4966,#4967,#4968,#4969,#4970,#4971,#4972,#4973,#4974,#4975,#4976,
#4977,#4978,#4979,#4980,#4981,#4982,#4983,#4984,#4985,#4986,#4987,#4988,
#4989,#4990,#4991,#4992,#4993,#4994,#4995,#4996,#4997,#4998,#4999,#5000,
#5001,#5002,#5003,#5004,#5005,#5006,#5007,#5008,#5009,#5010,#5011,#5012,
#5013,#5014,#5015,#5016,#5017,#5018,#5019,#5020,#5021,#5022,#5023,#5024,
#5025,#5026,#5027,#5028,#5029,#5030,#5031,#5032),.UNSPECIFIED.,.F.,.F.,
(4,2,2,2,2,2,2,2,2,2,2,2,2,2,2,2,2,2,2,2,2,2,2,2,2,2,2,2,2,2,2,2,2,2,2,
2,2,2,2,2,2,2,2,2,2,2,2,2,2,2,2,2,2,2,2,2,2,2,2,2,2,2,2,2,2,2,2,2,2,2,2,
2,2,2,2,2,2,2,2,2,2,2,2,2,4),(-1.72202346959793,-1.71870018917094,-1.71591322745448,
-1.7137717851489,-1.71189119546824,-1.70971791514103,-1.70614322261802,
-1.69104856008632,-1.66138713746971,-1.65436780756703,-1.64846163132073,
-1.64465642502085,-1.64103140026988,-1.63669289250378,-1.62598523221138,
-1.58656459426751,-1.58039020467346,-1.57772042206146,-1.57589261844911,
-1.57350052300544,-1.56900615173947,-1.55067513426042,-1.53420116499451,
-1.52315305398727,-1.51490055503334,-1.5106327586612,-1.5070666719527,-1.50276688016783,
-1.49460698831665,-1.46426952076207,-1.45256578852821,-1.44539135107234,
-1.44256868709891,-1.44053426948862,-1.43815268817646,-1.433708588999,-1.41274055928829,
-1.39314353539268,-1.38120527695429,-1.37634492977801,-1.37272814275904,
-1.36881576233835,-1.36237934197206,-1.33214526514168,-1.31824831572467,
-1.31025989639583,-1.30732661631416,-1.30527710798275,-1.30295384133811,
-1.29878306781289,-1.27339646693931,-1.25642332096652,-1.24544916521034,
-1.24072627291106,-1.23712804079784,-1.23315377705416,-1.22641079352668,
-1.20080262310378,-1.18403711853035,-1.17512584778449,-1.17208047826183,
-1.17001286668314,-1.16773829430545,-1.16368587832871,-1.13678362319376,
-1.11253716635762,-1.10674568648551,-1.10296285987455,-1.09932277953469,
-1.09409352460756,-1.08010956202237,-1.04505169166033,-1.03882770328252,
-1.03614973459047,-1.03432088144703,-1.0319339998225,-1.02746502477973,
-1.00785201787439,-0.987346036116553,-0.975104496453811,-0.970203164133492,
-0.966580221846493,-0.962683928260761,-0.956327698005292,-0.939927914600591),
 .UNSPECIFIED.);
#76=B_SPLINE_CURVE_WITH_KNOTS('',3,(#5038,#5039,#5040,#5041,#5042,#5043,
#5044,#5045,#5046,#5047,#5048,#5049,#5050,#5051,#5052,#5053,#5054,#5055,
#5056,#5057,#5058,#5059,#5060,#5061,#5062,#5063,#5064,#5065,#5066,#5067,
#5068,#5069,#5070,#5071,#5072,#5073,#5074,#5075,#5076,#5077,#5078,#5079,
#5080,#5081,#5082,#5083,#5084,#5085,#5086,#5087,#5088,#5089,#5090,#5091,
#5092,#5093,#5094,#5095,#5096,#5097,#5098,#5099,#5100,#5101,#5102,#5103,
#5104,#5105,#5106,#5107,#5108,#5109,#5110,#5111,#5112,#5113,#5114,#5115,
#5116,#5117,#5118,#5119,#5120,#5121,#5122,#5123,#5124,#5125,#5126,#5127,
#5128,#5129,#5130,#5131,#5132,#5133,#5134,#5135,#5136,#5137,#5138,#5139,
#5140,#5141,#5142,#5143,#5144,#5145,#5146,#5147,#5148,#5149,#5150,#5151,
#5152,#5153,#5154,#5155,#5156,#5157,#5158,#5159,#5160,#5161,#5162,#5163,
#5164,#5165,#5166,#5167,#5168,#5169,#5170,#5171,#5172,#5173,#5174,#5175,
#5176,#5177,#5178,#5179,#5180,#5181,#5182,#5183,#5184,#5185,#5186,#5187,
#5188,#5189,#5190,#5191,#5192,#5193,#5194,#5195,#5196,#5197,#5198,#5199),
 .UNSPECIFIED.,.F.,.F.,(4,2,2,2,2,2,2,2,2,2,2,2,2,2,2,2,2,2,2,2,2,2,2,2,
2,2,2,2,2,2,2,2,2,2,2,2,2,2,2,2,2,2,2,2,2,2,2,2,2,2,2,2,2,2,2,2,2,2,2,2,
2,2,2,2,2,2,2,2,2,2,2,2,2,2,2,2,2,2,2,2,4),(-0.782686723559536,-0.776829908385411,
-0.759694909346261,-0.734557343110431,-0.730361867686715,-0.728032581521128,
-0.725983481676664,-0.723058616281106,-0.715141620403665,-0.701451820327158,
-0.670845737253636,-0.664455565957333,-0.660551250214299,-0.656928984029553,
-0.652041174517008,-0.639912390951821,-0.619755546974085,-0.59969774299674,
-0.595168709446075,-0.59276859020319,-0.590940797163087,-0.588279083002747,
-0.582159300687959,-0.542994182076116,-0.532060526505425,-0.527686745055492,
-0.524051907850687,-0.520256669090037,-0.514408754673189,-0.507481153357872,
-0.492921967070446,-0.464062707929007,-0.459637131773207,-0.457258779161931,
-0.455222391313416,-0.452390588694543,-0.445157569901286,-0.433307848590126,
-0.402366183445107,-0.395384280391682,-0.390976944941689,-0.387406028922544,
-0.38322918423663,-0.375465214483068,-0.36010030753842,-0.335487379845948,
-0.326223078674156,-0.323051662153072,-0.320981173404627,-0.318757117138205,
-0.314947944026571,-0.310141239047756,-0.299043161632813,-0.264788713760983,
-0.258261368828698,-0.254329590727207,-0.250717305906561,-0.245897130031362,
-0.234258739925162,-0.215521604929568,-0.193128150007976,-0.188753124981894,
-0.186385553465706,-0.184346916354634,-0.181496453706521,-0.174130198356016,
-0.161936407667949,-0.129559513557705,-0.122930531688521,-0.11897822899014,
-0.115372169487496,-0.110597877453516,-0.0992818286751014,-0.0814224240349977,
-0.0575323651140709,-0.0532602224953532,-0.0509145690988358,-0.0488703999603477,
-0.0459788792694939,-0.0383129958008827,-0.000387729151872138),
 .UNSPECIFIED.);
#77=B_SPLINE_CURVE_WITH_KNOTS('',3,(#5200,#5201,#5202,#5203,#5204,#5205,
#5206,#5207,#5208,#5209,#5210,#5211,#5212,#5213,#5214,#5215,#5216,#5217,
#5218,#5219),.UNSPECIFIED.,.F.,.F.,(4,2,2,2,2,2,2,2,2,4),(-1.7216012596671,
-1.71550655685447,-1.71067082519282,-1.70705039597375,-1.70367348907421,
-1.69990717799663,-1.69419743381424,-1.67243675688787,-1.64626826175847,
-1.64297773443279),.UNSPECIFIED.);
#78=B_SPLINE_CURVE_WITH_KNOTS('',3,(#5220,#5221,#5222,#5223,#5224,#5225,
#5226,#5227,#5228,#5229,#5230,#5231,#5232,#5233,#5234,#5235,#5236,#5237,
#5238,#5239,#5240,#5241,#5242,#5243,#5244,#5245,#5246,#5247,#5248,#5249,
#5250,#5251,#5252,#5253,#5254,#5255,#5256,#5257,#5258,#5259,#5260,#5261,
#5262,#5263,#5264,#5265,#5266,#5267,#5268,#5269,#5270,#5271,#5272,#5273,
#5274,#5275,#5276,#5277,#5278,#5279,#5280,#5281,#5282,#5283,#5284,#5285,
#5286,#5287,#5288,#5289,#5290,#5291,#5292,#5293,#5294,#5295,#5296,#5297,
#5298,#5299,#5300,#5301,#5302,#5303,#5304,#5305,#5306,#5307,#5308,#5309,
#5310,#5311,#5312,#5313,#5314,#5315,#5316,#5317,#5318,#5319,#5320,#5321,
#5322,#5323,#5324,#5325,#5326,#5327,#5328,#5329,#5330,#5331,#5332,#5333,
#5334,#5335,#5336,#5337,#5338,#5339,#5340,#5341,#5342,#5343,#5344,#5345,
#5346,#5347,#5348,#5349,#5350,#5351,#5352,#5353,#5354,#5355,#5356,#5357,
#5358,#5359,#5360,#5361,#5362,#5363,#5364,#5365,#5366,#5367,#5368,#5369,
#5370,#5371,#5372,#5373,#5374,#5375,#5376,#5377,#5378,#5379,#5380,#5381,
#5382,#5383,#5384,#5385,#5386,#5387,#5388,#5389,#5390,#5391,#5392,#5393,
#5394,#5395,#5396,#5397,#5398,#5399),.UNSPECIFIED.,.F.,.F.,(4,2,2,2,2,2,
2,2,2,2,2,2,2,2,2,2,2,2,2,2,2,2,2,2,2,2,2,2,2,2,2,2,2,2,2,2,2,2,2,2,2,2,
2,2,2,2,2,2,2,2,2,2,2,2,2,2,2,2,2,2,2,2,2,2,2,2,2,2,2,2,2,2,2,2,2,2,2,2,
2,2,2,2,2,2,2,2,2,2,2,4),(-0.939927914600591,-0.923554267701752,-0.911263480236345,
-0.906151124386267,-0.902160808727174,-0.899899068576791,-0.897849160525681,
-0.895284635018434,-0.888528660992351,-0.861444729901312,-0.841498237755948,
-0.835805365716651,-0.832041454714497,-0.828343759470433,-0.822999889948548,
-0.806753459006284,-0.790151906013408,-0.771714213525448,-0.767211576534864,
-0.764817540605371,-0.762989691557827,-0.760321816451003,-0.754160522112188,
-0.714810511893886,-0.704052537395685,-0.69970600330477,-0.69607857650783,
-0.69227534293082,-0.686381870447858,-0.659822843986647,-0.635855765468199,
-0.631593179933376,-0.629250061396491,-0.62720617584421,-0.624312555995763,
-0.616626522513446,-0.603577728127068,-0.571706183948792,-0.565486635879485,
-0.561617914336139,-0.55798347915703,-0.553007531340048,-0.540190887178216,
-0.519312299844477,-0.500856611132237,-0.496352703931226,-0.493958460860715,
-0.492130734998392,-0.489463410509781,-0.483305077279369,-0.443969649384891,
-0.433200361860738,-0.428852240868508,-0.425224551848086,-0.421422145459688,
-0.41553229912841,-0.389160708630153,-0.364969131690273,-0.360725430270745,
-0.358386419990707,-0.356341495739722,-0.353440089561388,-0.345695155792632,
-0.332484176260121,-0.300944076448628,-0.294679124014928,-0.290801335785631,
-0.28717102974285,-0.282220894810267,-0.269606293613773,-0.247915109770964,
-0.22995397359159,-0.225482475353296,-0.223095079153693,-0.221266294767036,
-0.218589120229558,-0.212369847080465,-0.177340680088108,-0.163350705858965,
-0.158121205009425,-0.154480976403562,-0.150697992740656,-0.144906326348576,
-0.120694903844777,-0.0937113529293291,-0.0896652440295716,-0.0873919005455655,
-0.0853235244697597,-0.0822744434035082,-0.0790377234486064),
 .UNSPECIFIED.);
#79=B_SPLINE_CURVE_WITH_KNOTS('',3,(#5404,#5405,#5406,#5407,#5408,#5409,
#5410,#5411,#5412,#5413,#5414,#5415,#5416,#5417,#5418,#5419,#5420,#5421,
#5422,#5423,#5424,#5425,#5426,#5427,#5428,#5429,#5430,#5431,#5432,#5433,
#5434,#5435,#5436,#5437,#5438,#5439,#5440,#5441,#5442,#5443,#5444,#5445,
#5446,#5447,#5448,#5449,#5450,#5451,#5452,#5453,#5454,#5455,#5456,#5457,
#5458,#5459,#5460,#5461,#5462,#5463,#5464,#5465,#5466,#5467,#5468,#5469,
#5470,#5471,#5472,#5473,#5474,#5475,#5476,#5477,#5478,#5479,#5480,#5481,
#5482,#5483,#5484,#5485,#5486,#5487,#5488,#5489,#5490,#5491,#5492,#5493,
#5494,#5495,#5496,#5497,#5498,#5499,#5500,#5501,#5502,#5503,#5504,#5505,
#5506,#5507,#5508,#5509,#5510,#5511,#5512,#5513,#5514,#5515,#5516,#5517,
#5518,#5519,#5520,#5521,#5522,#5523,#5524,#5525,#5526,#5527,#5528,#5529,
#5530,#5531,#5532,#5533,#5534,#5535,#5536,#5537,#5538,#5539,#5540,#5541,
#5542,#5543,#5544,#5545,#5546,#5547,#5548,#5549,#5550,#5551,#5552,#5553,
#5554,#5555,#5556,#5557,#5558,#5559,#5560,#5561,#5562,#5563,#5564,#5565,
#5566,#5567,#5568,#5569,#5570,#5571,#5572,#5573,#5574,#5575,#5576,#5577,
#5578,#5579,#5580,#5581,#5582,#5583,#5584,#5585),.UNSPECIFIED.,.F.,.F.,
(4,2,2,2,2,2,2,2,2,2,2,2,2,2,2,2,2,2,2,2,2,2,2,2,2,2,2,2,2,2,2,2,2,2,2,
2,2,2,2,2,2,2,2,2,2,2,2,2,2,2,2,2,2,2,2,2,2,2,2,2,2,2,2,2,2,2,2,2,2,2,2,
2,2,2,2,2,2,2,2,2,2,2,2,2,2,2,2,2,2,2,4),(-1.64347692384346,-1.62647809996023,
-1.61519114415661,-1.61042132461924,-1.60681599358851,-1.60286189606256,
-1.59622352561842,-1.56799895904397,-1.55296545702111,-1.54459279077102,
-1.54161057888925,-1.53955290587183,-1.53725064258264,-1.53306729168193,
-1.50730452913988,-1.48519766988736,-1.47777616399101,-1.47366614387183,
-1.47009017055522,-1.46559487452762,-1.45829221621878,-1.42776139810831,
-1.41601010631762,-1.40881638020244,-1.40599037167774,-1.40395495039513,
-1.40157378419175,-1.39713398687239,-1.37630457460847,-1.35660549186341,
-1.34463156987632,-1.33976533813434,-1.33614667502193,-1.33223457484849,
-1.32580399123308,-1.29550999255385,-1.28164359657382,-1.27366522418574,
-1.27073262439214,-1.26868265014921,-1.26635763912456,-1.2621810428845,
-1.23685037511258,-1.21984546503079,-1.20885802194901,-1.20413215610088,
-1.20053248952346,-1.1965574136866,-1.18981486861127,-1.16409070196488,
-1.1474060751908,-1.13851813470799,-1.13547479302475,-1.13340698664667,
-1.13113028681442,-1.12707002523676,-1.10022602928524,-1.07593398004563,
-1.07014003585567,-1.06635580272923,-1.06271446363032,-1.05748348543213,
-1.04349301673887,-1.00843634258165,-1.00221452490058,-0.999536351783928,
-0.997706933977108,-0.995318595178487,-0.990845031998848,-0.971471413028527,
-0.951982264612179,-0.938789164943159,-0.933765807222672,-0.930122869243032,
-0.926268514868687,-0.92012460735921,-0.887685197354395,-0.874893619944347,
-0.869658103041326,-0.865595303780987,-0.863317917160893,-0.861273638061288,
-0.858250270910351,-0.8495357104705,-0.833424756299311,-0.806900675158636,
-0.800175522456143,-0.796203645093578,-0.792602586738466,-0.787868619119288,
-0.782686723559536),.UNSPECIFIED.);
#80=B_SPLINE_CURVE_WITH_KNOTS('',3,(#5587,#5588,#5589,#5590,#5591,#5592,
#5593,#5594,#5595,#5596,#5597,#5598,#5599,#5600,#5601,#5602,#5603,#5604,
#5605,#5606),.UNSPECIFIED.,.F.,.F.,(4,2,2,2,2,2,2,2,2,4),(-0.0790377234486064,
-0.0733310779424561,-0.0519587194341138,-0.0310138573416728,-0.0242790937925843,
-0.0203062843425282,-0.0168350967339937,-0.0133427717109691,-0.00781598579281862,
-0.0003870511716117),.UNSPECIFIED.);
#81=B_SPLINE_CURVE_WITH_KNOTS('',3,(#5607,#5608,#5609,#5610,#5611,#5612,
#5613,#5614,#5615,#5616,#5617,#5618,#5619,#5620,#5621,#5622,#5623,#5624,
#5625,#5626,#5627,#5628,#5629,#5630,#5631,#5632,#5633,#5634,#5635,#5636,
#5637,#5638,#5639,#5640,#5641,#5642,#5643,#5644,#5645,#5646,#5647,#5648,
#5649,#5650,#5651,#5652,#5653,#5654,#5655,#5656,#5657,#5658,#5659,#5660,
#5661,#5662,#5663,#5664,#5665,#5666,#5667,#5668,#5669,#5670,#5671,#5672,
#5673,#5674,#5675,#5676,#5677,#5678,#5679,#5680,#5681,#5682,#5683,#5684,
#5685,#5686,#5687,#5688,#5689,#5690,#5691,#5692,#5693,#5694,#5695,#5696,
#5697,#5698,#5699,#5700,#5701,#5702,#5703,#5704,#5705,#5706,#5707,#5708,
#5709,#5710,#5711,#5712,#5713,#5714,#5715,#5716,#5717,#5718,#5719,#5720,
#5721,#5722,#5723,#5724,#5725,#5726,#5727,#5728,#5729,#5730,#5731,#5732,
#5733,#5734,#5735,#5736,#5737,#5738,#5739,#5740,#5741,#5742,#5743,#5744,
#5745,#5746,#5747,#5748,#5749,#5750,#5751,#5752,#5753,#5754,#5755,#5756,
#5757,#5758,#5759,#5760,#5761,#5762,#5763,#5764,#5765,#5766,#5767,#5768),
 .UNSPECIFIED.,.F.,.F.,(4,2,2,2,2,2,2,2,2,2,2,2,2,2,2,2,2,2,2,2,2,2,2,2,
2,2,2,2,2,2,2,2,2,2,2,2,2,2,2,2,2,2,2,2,2,2,2,2,2,2,2,2,2,2,2,2,2,2,2,2,
2,2,2,2,2,2,2,2,2,2,2,2,2,2,2,2,2,2,2,2,4),(-1.72190052015242,-1.7008417553696,
-1.67959684492697,-1.67569206404128,-1.6734487908009,-1.67139110028624,
-1.66828400795561,-1.65954762801523,-1.63696924262774,-1.62239240996895,
-1.6124236064941,-1.60785759134824,-1.60427728045063,-1.60021747719425,
-1.593234689959,-1.56143533771465,-1.54937567616379,-1.54206258327152,-1.53922055996786,
-1.53718403671187,-1.53481422723463,-1.53042470441813,-1.50743773593717,
-1.48914697124183,-1.47767246073601,-1.47287730510484,-1.46927016858056,
-1.46533092948403,-1.45875935533647,-1.42979099186425,-1.40901528198744,
-1.40502214366069,-1.40276013650602,-1.40071104751257,-1.39765395885015,
-1.38931286139406,-1.36641605531578,-1.35172163584231,-1.34475752822906,
-1.33888643933257,-1.33508796435709,-1.33145829623413,-1.32710082120996,
-1.31626833493528,-1.27698090133382,-1.27083455163844,-1.26816919426628,
-1.26634174274867,-1.26394622361528,-1.25943612937136,-1.2409066312412,
-1.22400969584118,-1.20812458662231,-1.20281426740824,-1.19912282053708,
-1.19579244388631,-1.19043602103518,-1.17513555137222,-1.14806746104473,
-1.13684265131668,-1.13356817698875,-1.13145744408986,-1.12925859429158,
-1.12556550075609,-1.10527641878139,-1.08422458841688,-1.07180817690105,
-1.06688369388516,-1.06325716571645,-1.05936953824415,-1.05305664542918,
-1.02184004167219,-1.00844868028128,-1.00063872648701,-0.997728541971604,
-0.995682297284709,-0.993347454769666,-0.989123585235036,-0.964517292391267,
-0.947095091498651,-0.939896813873088),.UNSPECIFIED.);
#82=B_SPLINE_CURVE_WITH_KNOTS('',3,(#5774,#5775,#5776,#5777,#5778,#5779,
#5780,#5781,#5782,#5783,#5784,#5785,#5786,#5787,#5788,#5789,#5790,#5791,
#5792,#5793,#5794,#5795,#5796,#5797,#5798,#5799,#5800,#5801,#5802,#5803,
#5804,#5805,#5806,#5807,#5808,#5809,#5810,#5811,#5812,#5813,#5814,#5815,
#5816,#5817,#5818,#5819,#5820,#5821,#5822,#5823,#5824,#5825,#5826,#5827,
#5828,#5829,#5830,#5831,#5832,#5833,#5834,#5835,#5836,#5837,#5838,#5839,
#5840,#5841,#5842,#5843,#5844,#5845,#5846,#5847,#5848,#5849,#5850,#5851,
#5852,#5853,#5854,#5855,#5856,#5857,#5858,#5859,#5860,#5861,#5862,#5863,
#5864,#5865,#5866,#5867,#5868,#5869,#5870,#5871,#5872,#5873,#5874,#5875,
#5876,#5877,#5878,#5879,#5880,#5881,#5882,#5883,#5884,#5885,#5886,#5887,
#5888,#5889,#5890,#5891,#5892,#5893,#5894,#5895,#5896,#5897,#5898,#5899,
#5900,#5901,#5902,#5903,#5904,#5905,#5906,#5907,#5908,#5909,#5910,#5911,
#5912,#5913,#5914,#5915,#5916,#5917,#5918,#5919,#5920,#5921,#5922,#5923,
#5924,#5925,#5926,#5927,#5928,#5929,#5930,#5931,#5932,#5933,#5934,#5935,
#5936,#5937,#5938,#5939,#5940,#5941,#5942,#5943),.UNSPECIFIED.,.F.,.F.,
(4,2,2,2,2,2,2,2,2,2,2,2,2,2,2,2,2,2,2,2,2,2,2,2,2,2,2,2,2,2,2,2,2,2,2,
2,2,2,2,2,2,2,2,2,2,2,2,2,2,2,2,2,2,2,2,2,2,2,2,2,2,2,2,2,2,2,2,2,2,2,2,
2,2,2,2,2,2,2,2,2,2,2,2,2,4),(-0.782599245859888,-0.771916842875543,-0.768391423183112,
-0.766228283301738,-0.764087894668306,-0.760670671928447,-0.747540096293486,
-0.730623483154982,-0.708310536159541,-0.702538578495944,-0.698758569476279,
-0.695071619029943,-0.689790445592084,-0.674224150558897,-0.647851420333512,
-0.636273406736027,-0.632881734529875,-0.630957404873542,-0.628844178174779,
-0.625559134319365,-0.614211710202638,-0.586364196575075,-0.57187831405912,
-0.566584986678905,-0.562932722225909,-0.559163930256809,-0.553448506717713,
-0.531494501426773,-0.508671845943224,-0.500210245250518,-0.497136751173071,
-0.49508424883467,-0.492826991589006,-0.488859202040587,-0.483785807980474,
-0.471650989715129,-0.439521106204485,-0.432714938328506,-0.42872740732765,
-0.42513134972042,-0.420431868479238,-0.409618826514158,-0.393050433566889,
-0.366862294429662,-0.362723062780961,-0.360430053398802,-0.358369095119043,
-0.355366090293615,-0.346820294776242,-0.331247934685562,-0.303921333544282,
-0.297228910757118,-0.293264060986159,-0.289661921055439,-0.284915551415741,
-0.2737891873953,-0.256426444227997,-0.231693102888949,-0.227473457318857,
-0.225139198332099,-0.223092057284232,-0.220178629888363,-0.212346522643491,
-0.198894354670003,-0.167835990360443,-0.161505766506546,-0.15761404881174,
-0.153987900294494,-0.149070474775887,-0.136714204326878,-0.115854771085359,
-0.0952920913959404,-0.0915829562950598,-0.0893803621176636,-0.0872712977028124,
-0.0840071172452614,-0.0729063668309943,-0.0570412553575325,-0.0334066342075332,
-0.0265621740533172,-0.0225666130179622,-0.0190836151482547,-0.0155992334828168,
-0.00934406409815735,-0.000389160665116305),.UNSPECIFIED.);
#83=B_SPLINE_CURVE_WITH_KNOTS('',3,(#5944,#5945,#5946,#5947,#5948,#5949,
#5950,#5951,#5952,#5953,#5954,#5955,#5956,#5957,#5958,#5959,#5960,#5961),
 .UNSPECIFIED.,.F.,.F.,(4,2,2,2,2,2,2,2,4),(-1.72199006678857,-1.68750856578881,
-1.67979846079402,-1.67690108887121,-1.67485624629048,-1.67251384604177,
-1.6682564786429,-1.64426046576741,-1.64347692384346),.UNSPECIFIED.);
#84=B_SPLINE_CURVE_WITH_KNOTS('',3,(#5962,#5963,#5964,#5965,#5966,#5967,
#5968,#5969,#5970,#5971,#5972,#5973,#5974,#5975,#5976,#5977,#5978,#5979,
#5980,#5981,#5982,#5983,#5984,#5985,#5986,#5987,#5988,#5989,#5990,#5991,
#5992,#5993,#5994,#5995,#5996,#5997,#5998,#5999,#6000,#6001,#6002,#6003,
#6004,#6005,#6006,#6007,#6008,#6009,#6010,#6011,#6012,#6013,#6014,#6015,
#6016,#6017,#6018,#6019,#6020,#6021,#6022,#6023,#6024,#6025,#6026,#6027,
#6028,#6029,#6030,#6031,#6032,#6033,#6034,#6035,#6036,#6037,#6038,#6039,
#6040,#6041,#6042,#6043,#6044,#6045,#6046,#6047,#6048,#6049,#6050,#6051,
#6052,#6053,#6054,#6055,#6056,#6057,#6058,#6059,#6060,#6061,#6062,#6063,
#6064,#6065,#6066,#6067,#6068,#6069,#6070,#6071,#6072,#6073,#6074,#6075,
#6076,#6077,#6078,#6079,#6080,#6081,#6082,#6083,#6084,#6085,#6086,#6087,
#6088,#6089,#6090,#6091,#6092,#6093,#6094,#6095,#6096,#6097,#6098,#6099,
#6100,#6101,#6102,#6103,#6104,#6105,#6106,#6107,#6108,#6109,#6110,#6111,
#6112,#6113,#6114,#6115,#6116,#6117,#6118,#6119,#6120,#6121,#6122,#6123,
#6124,#6125,#6126,#6127,#6128,#6129,#6130,#6131,#6132,#6133,#6134,#6135,
#6136,#6137,#6138,#6139,#6140,#6141,#6142,#6143,#6144,#6145),
 .UNSPECIFIED.,.F.,.F.,(4,2,2,2,2,2,2,2,2,2,2,2,2,2,2,2,2,2,2,2,2,2,2,2,
2,2,2,2,2,2,2,2,2,2,2,2,2,2,2,2,2,2,2,2,2,2,2,2,2,2,2,2,2,2,2,2,2,2,2,2,
2,2,2,2,2,2,2,2,2,2,2,2,2,2,2,2,2,2,2,2,2,2,2,2,2,2,2,2,2,2,2,4),(-0.939896813873088,
-0.935945765197772,-0.931196725373738,-0.927594901368007,-0.923632744081659,
-0.916951051952594,-0.883448209138369,-0.867924648794366,-0.863619616212537,
-0.861292650799981,-0.859243809631339,-0.856317031658491,-0.848380786607831,
-0.834634699293341,-0.80413816353932,-0.79773557353793,-0.793829612153776,
-0.790209681130236,-0.785331084733207,-0.773263442024674,-0.753287587011472,
-0.732833061505069,-0.728386045506471,-0.726003594598022,-0.723968866668277,
-0.721146442191349,-0.713975648992959,-0.702283096907898,-0.671981201787048,
-0.663801840651034,-0.659497744422515,-0.655930940832998,-0.651665680332589,
-0.6434299070133,-0.63241295311361,-0.615882015096843,-0.597508309993198,
-0.593010316610334,-0.590617171529793,-0.588789050269151,-0.586119522556112,
-0.579948687960363,-0.540551986561062,-0.529833547112135,-0.525492806904551,
-0.521866569818422,-0.518060792777725,-0.512155294028801,-0.485106365917026,
-0.46182425897503,-0.457459482560063,-0.455094485793467,-0.453056031751265,
-0.45020319552216,-0.442816439523984,-0.430568141988818,-0.397961777612341,
-0.391499097539396,-0.387581134943543,-0.383965731841133,-0.379117307673376,
-0.367269696507562,-0.347938108162909,-0.326458349631957,-0.322063205476426,
-0.319691782589373,-0.317654823899299,-0.314813570848215,-0.307509462242839,
-0.295475799115584,-0.263776247764284,-0.256722849091742,-0.252647477038307,
-0.249426223290332,-0.245062685346377,-0.236287190473465,-0.224226337874599,
-0.208827257830432,-0.191157403554994,-0.18669978746137,-0.184315207104427,
-0.182485759572001,-0.179803891306055,-0.173556442487766,-0.138414739590681,
-0.124544267041282,-0.119326986104001,-0.115688662530475,-0.111902118200791,
-0.106093473042144,-0.0811916551463075,-0.0789957478678517),
 .UNSPECIFIED.);
#85=B_SPLINE_CURVE_WITH_KNOTS('',3,(#6150,#6151,#6152,#6153,#6154,#6155,
#6156,#6157,#6158,#6159,#6160,#6161,#6162,#6163,#6164,#6165,#6166,#6167,
#6168,#6169,#6170,#6171,#6172,#6173,#6174,#6175,#6176,#6177,#6178,#6179,
#6180,#6181,#6182,#6183,#6184,#6185,#6186,#6187,#6188,#6189,#6190,#6191,
#6192,#6193,#6194,#6195,#6196,#6197,#6198,#6199,#6200,#6201,#6202,#6203,
#6204,#6205,#6206,#6207,#6208,#6209,#6210,#6211,#6212,#6213,#6214,#6215,
#6216,#6217,#6218,#6219,#6220,#6221,#6222,#6223,#6224,#6225,#6226,#6227,
#6228,#6229,#6230,#6231,#6232,#6233,#6234,#6235,#6236,#6237,#6238,#6239,
#6240,#6241,#6242,#6243,#6244,#6245,#6246,#6247,#6248,#6249,#6250,#6251,
#6252,#6253,#6254,#6255,#6256,#6257,#6258,#6259,#6260,#6261,#6262,#6263,
#6264,#6265,#6266,#6267,#6268,#6269,#6270,#6271,#6272,#6273,#6274,#6275,
#6276,#6277,#6278,#6279,#6280,#6281,#6282,#6283,#6284,#6285,#6286,#6287,
#6288,#6289,#6290,#6291,#6292,#6293,#6294,#6295,#6296,#6297,#6298,#6299,
#6300,#6301,#6302,#6303,#6304,#6305,#6306,#6307,#6308,#6309,#6310,#6311,
#6312,#6313,#6314,#6315,#6316,#6317,#6318,#6319,#6320,#6321,#6322,#6323,
#6324,#6325),.UNSPECIFIED.,.F.,.F.,(4,2,2,2,2,2,2,2,2,2,2,2,2,2,2,2,2,2,
2,2,2,2,2,2,2,2,2,2,2,2,2,2,2,2,2,2,2,2,2,2,2,2,2,2,2,2,2,2,2,2,2,2,2,2,
2,2,2,2,2,2,2,2,2,2,2,2,2,2,2,2,2,2,2,2,2,2,2,2,2,2,2,2,2,2,2,2,2,4),(-1.6432613616363,
-1.64161314158455,-1.63517065096013,-1.60035856750064,-1.58937151171928,
-1.58249256221114,-1.57972586961991,-1.57772343305823,-1.5753312885874,
-1.57084086371976,-1.55256684156769,-1.53154503040702,-1.51867274857762,
-1.51368160165886,-1.51003665769862,-1.50615656624993,-1.49991602379275,
-1.46836947911062,-1.45527948874169,-1.44757813600774,-1.44467514664117,
-1.44262403943427,-1.44027334731779,-1.43598400490242,-1.41227202807211,
-1.38547443452719,-1.37963909308575,-1.37584654743783,-1.372210344127,-1.36783009767956,
-1.35685020234345,-1.31769060898488,-1.31155745259713,-1.30889466424372,
-1.30706835165882,-1.30467412953405,-1.30016449476984,-1.28162684568544,
-1.26041571902772,-1.24795152497195,-1.24302348340268,-1.23939905236228,
-1.23551818339787,-1.22922717130057,-1.19785438429616,-1.18453439255849,
-1.17675119962063,-1.17384617561964,-1.17180159898918,-1.1694651807813,
-1.16523553718916,-1.14077067859652,-1.12326672460158,-1.11208500468429,
-1.10732972618432,-1.10372542174437,-1.0997625818622,-1.09308431529482,
-1.0655092196304,-1.0501006604258,-1.04160731553292,-1.03860962029435,-1.03654884428248,
-1.03425237835456,-1.03009686526669,-1.00408785176088,-0.9791741946859,
-0.973366700081466,-0.969580258348652,-0.965941500253462,-0.960722629720811,
-0.946865847082279,-0.911692371408435,-0.905437735994771,-0.90275472786554,
-0.900925220596629,-0.898541510757078,-0.894087837670476,-0.876489006982961,
-0.861280684840634,-0.843337904312691,-0.837733808194014,-0.834361243892084,
-0.830708020484245,-0.825617005449271,-0.811845733161868,-0.78583367335449,
-0.782599245859888),.UNSPECIFIED.);
#86=B_SPLINE_CURVE_WITH_KNOTS('',3,(#6327,#6328,#6329,#6330,#6331,#6332,
#6333,#6334,#6335,#6336,#6337,#6338,#6339,#6340,#6341,#6342),
 .UNSPECIFIED.,.F.,.F.,(4,2,2,2,2,2,2,4),(-0.0789957478678517,-0.0551148295329374,
-0.0509626629422434,-0.0486671676406389,-0.0466076700700712,-0.0436120653051043,
-0.0351252602160147,-0.000467694393496468),.UNSPECIFIED.);
#87=B_SPLINE_CURVE_WITH_KNOTS('',3,(#6343,#6344,#6345,#6346,#6347,#6348,
#6349,#6350,#6351,#6352,#6353,#6354,#6355,#6356,#6357,#6358,#6359,#6360,
#6361,#6362,#6363,#6364,#6365,#6366,#6367,#6368,#6369,#6370,#6371,#6372,
#6373,#6374,#6375,#6376,#6377,#6378,#6379,#6380,#6381,#6382,#6383,#6384,
#6385,#6386,#6387,#6388,#6389,#6390,#6391,#6392,#6393,#6394,#6395,#6396,
#6397,#6398,#6399,#6400,#6401,#6402,#6403,#6404,#6405,#6406,#6407,#6408,
#6409,#6410,#6411,#6412,#6413,#6414,#6415,#6416,#6417,#6418,#6419,#6420,
#6421,#6422,#6423,#6424,#6425,#6426,#6427,#6428,#6429,#6430,#6431,#6432,
#6433,#6434,#6435,#6436,#6437,#6438,#6439,#6440,#6441,#6442,#6443,#6444,
#6445,#6446,#6447,#6448,#6449,#6450,#6451,#6452,#6453,#6454,#6455,#6456,
#6457,#6458,#6459,#6460,#6461,#6462,#6463,#6464,#6465,#6466,#6467,#6468,
#6469,#6470,#6471,#6472,#6473,#6474,#6475,#6476,#6477,#6478,#6479,#6480,
#6481,#6482,#6483,#6484,#6485,#6486,#6487,#6488,#6489,#6490,#6491,#6492,
#6493,#6494,#6495,#6496,#6497,#6498,#6499,#6500,#6501,#6502,#6503,#6504,
#6505,#6506,#6507,#6508,#6509,#6510),.UNSPECIFIED.,.F.,.F.,(4,2,2,2,2,2,
2,2,2,2,2,2,2,2,2,2,2,2,2,2,2,2,2,2,2,2,2,2,2,2,2,2,2,2,2,2,2,2,2,2,2,2,
2,2,2,2,2,2,2,2,2,2,2,2,2,2,2,2,2,2,2,2,2,2,2,2,2,2,2,2,2,2,2,2,2,2,2,2,
2,2,2,2,2,4),(0.782675134033573,0.782757485927756,0.79475868109047,0.798176777831719,
0.800104431433756,0.802211228332774,0.805465846820559,0.816456368900843,
0.842152606133684,0.858697906830614,0.864240310369191,0.867603266628399,
0.871266977594691,0.876412828561605,0.890664055646709,0.918913849486384,
0.930243122109789,0.933609935042696,0.935530065740048,0.937648381135311,
0.940958897741722,0.952617221264153,0.982558786625348,0.995139239295908,
1.00021136792272,1.00382517622462,1.00765269196997,1.0136675642461,1.03885136040049,
1.06405934903704,1.06824645506887,1.07057318495682,1.07262140621808,1.07554680049778,
1.08347506120726,1.09720008463773,1.12776711776842,1.13416346016404,1.13806759007756,
1.14168703025469,1.14656681390693,1.15864939288267,1.17867289197161,1.19898414322743,
1.20345332047464,1.20584010470427,1.20766893530967,1.21034680925492,1.2165696116661,
1.25162358005158,1.26561408639473,1.27084423366087,1.27448474097013,1.27826786510143,
1.2840595405384,1.30830424262765,1.33520506211329,1.33925760994492,1.34153239052917,
1.34360017810509,1.34664599470362,1.35556049046178,1.37233653973675,1.39793017143743,
1.40467342657647,1.40864778588906,1.41224606448015,1.41696895461105,1.42794269808721,
1.44491431607832,1.4703072739279,1.4744777338303,1.47680092931909,1.47885045329991,
1.481783835504,1.48977297224307,1.51117459842206,1.53323974042741,1.54002851148807,
1.5440120563922,1.54748826067801,1.55097547824573,1.55683902380664,1.56494898091576),
 .UNSPECIFIED.);
#88=B_SPLINE_CURVE_WITH_KNOTS('',3,(#6514,#6515,#6516,#6517,#6518,#6519),
 .UNSPECIFIED.,.F.,.F.,(4,1,1,4),(-4.09232582034257,-3.95356055398286,-2.96517041548714,
-2.06969806661986),.UNSPECIFIED.);
#89=B_SPLINE_CURVE_WITH_KNOTS('',3,(#6523,#6524,#6525,#6526,#6527),
 .UNSPECIFIED.,.F.,.F.,(4,1,4),(0.,0.988390138495704,1.11850960794437),
 .UNSPECIFIED.);
#90=B_SPLINE_CURVE_WITH_KNOTS('',3,(#6529,#6530,#6531,#6532,#6533,#6534,
#6535,#6536,#6537,#6538,#6539,#6540,#6541,#6542,#6543,#6544,#6545,#6546,
#6547,#6548,#6549,#6550,#6551,#6552,#6553,#6554,#6555,#6556,#6557,#6558,
#6559,#6560,#6561,#6562,#6563,#6564,#6565,#6566,#6567,#6568,#6569,#6570,
#6571,#6572,#6573,#6574,#6575,#6576,#6577,#6578,#6579,#6580,#6581,#6582,
#6583,#6584,#6585,#6586,#6587,#6588,#6589,#6590,#6591,#6592,#6593,#6594,
#6595,#6596,#6597,#6598,#6599,#6600,#6601,#6602,#6603,#6604,#6605,#6606,
#6607,#6608,#6609,#6610,#6611,#6612,#6613,#6614,#6615,#6616,#6617,#6618,
#6619,#6620,#6621,#6622,#6623,#6624,#6625,#6626,#6627,#6628,#6629,#6630,
#6631,#6632,#6633,#6634,#6635,#6636,#6637,#6638,#6639,#6640,#6641,#6642,
#6643,#6644,#6645,#6646,#6647,#6648,#6649,#6650,#6651,#6652,#6653,#6654,
#6655,#6656,#6657,#6658,#6659,#6660,#6661,#6662,#6663,#6664,#6665,#6666,
#6667,#6668,#6669,#6670,#6671,#6672,#6673,#6674,#6675,#6676,#6677,#6678,
#6679,#6680,#6681,#6682,#6683,#6684,#6685,#6686,#6687,#6688,#6689,#6690,
#6691,#6692,#6693,#6694,#6695,#6696,#6697,#6698,#6699,#6700,#6701,#6702,
#6703),.UNSPECIFIED.,.F.,.F.,(4,3,3,3,3,3,3,3,3,3,3,3,3,3,3,3,3,3,3,3,3,
3,3,3,3,3,3,3,3,3,3,3,3,3,3,3,3,3,3,3,3,3,3,3,3,3,3,3,3,3,3,3,3,3,3,3,3,
3,4),(1.11850960794437,1.22579344157525,1.33223603590235,1.43859406334533,
1.54491030815538,1.65287780036439,1.75930425580786,1.86804226639964,1.97678027699142,
2.08619472520565,2.19606668649083,2.30518861914641,2.41424528619025,2.52327607349202,
2.6337496589908,2.74291250415898,2.85404145982306,2.96517041548714,3.07458685153405,
3.18445856434015,3.29359150555844,3.4026625541112,3.51171108558613,3.62217345268532,
3.73136219092843,3.84246137245565,3.95356055398286,4.06264813384511,4.1725609536743,
4.2813505245247,4.39007374209031,4.49877057062825,4.60956560109083,4.71839716172489,
4.83017392710173,4.94195069247857,5.05122246113134,5.16111225736171,5.27009152387901,
5.37900596450968,5.48789522451555,5.59850662613023,5.70753138898118,5.81893610997773,
5.93034083097429,6.03959681195816,6.14948858164714,6.25845280370696,6.36735252397173,
6.47622741436736,6.58685330314302,6.69586473711608,6.80729785329305,6.91873096947001,
7.0394719557711,7.15440370853321,7.26911755665986,7.38356740485535,7.40169491467437),
 .UNSPECIFIED.);
#91=B_SPLINE_CURVE_WITH_KNOTS('',3,(#6705,#6706,#6707,#6708,#6709,#6710,
#6711,#6712,#6713,#6714,#6715,#6716,#6717,#6718,#6719,#6720,#6721,#6722,
#6723,#6724,#6725,#6726,#6727,#6728,#6729,#6730,#6731,#6732,#6733,#6734,
#6735,#6736,#6737,#6738,#6739,#6740,#6741,#6742,#6743,#6744,#6745,#6746,
#6747,#6748,#6749,#6750,#6751,#6752,#6753,#6754,#6755,#6756,#6757,#6758,
#6759,#6760,#6761,#6762,#6763,#6764,#6765,#6766,#6767,#6768,#6769,#6770,
#6771,#6772,#6773,#6774,#6775,#6776,#6777,#6778,#6779,#6780,#6781,#6782,
#6783,#6784,#6785,#6786,#6787,#6788,#6789,#6790,#6791,#6792,#6793,#6794,
#6795,#6796,#6797,#6798,#6799,#6800,#6801,#6802,#6803,#6804,#6805,#6806,
#6807,#6808,#6809,#6810,#6811,#6812,#6813,#6814,#6815,#6816,#6817,#6818,
#6819,#6820,#6821,#6822,#6823,#6824,#6825,#6826,#6827,#6828,#6829,#6830,
#6831,#6832,#6833,#6834,#6835,#6836,#6837,#6838,#6839,#6840,#6841,#6842,
#6843,#6844,#6845,#6846,#6847,#6848,#6849,#6850,#6851,#6852,#6853,#6854,
#6855,#6856,#6857,#6858,#6859,#6860,#6861,#6862,#6863,#6864,#6865,#6866,
#6867,#6868,#6869,#6870,#6871,#6872,#6873,#6874,#6875,#6876,#6877,#6878,
#6879),.UNSPECIFIED.,.F.,.F.,(4,3,3,3,3,3,3,3,3,3,3,3,3,3,3,3,3,3,3,3,3,
3,3,3,3,3,3,3,3,3,3,3,3,3,3,3,3,3,3,3,3,3,3,3,3,3,3,3,3,3,3,3,3,3,3,3,3,
3,4),(7.40169491512396,7.51508585839002,7.62876448289629,7.74259833580656,
7.85672333604955,7.90712110796573,8.01636379034547,8.12625722235997,8.23520710733033,
8.34409214137705,8.45295202069422,8.56359182713602,8.67258761935882,8.78404943291013,
8.89551124646144,9.0047489895559,9.11464303898106,9.2235879892422,9.33246810470449,
9.44132309010251,9.55196766381617,9.66095868084071,9.77243003289893,9.88390138495715,
9.99313410876066,10.1030287855972,10.2119684564921,10.3208432100475,10.4296927599658,
10.5403424508376,10.6493279132887,10.7608097183708,10.8722915234529,10.9815285124691,
11.091422656154,11.200366741289,11.3092459523339,11.4180999954536,11.5287454120773,
11.6377354037949,11.7492085328717,11.8606816619486,11.9699175713013,12.0798118499442,
12.1887548410624,12.2976329558757,12.4064859024314,12.5171323769346,12.6261212841214,
12.7375965422828,12.8490718004443,12.9566773999038,13.0641381618935,13.1714962465973,
13.2787936552669,13.3861279145202,13.4934766413414,13.6009727981548,13.6848802223035),
 .UNSPECIFIED.);
#92=B_SPLINE_CURVE_WITH_KNOTS('',3,(#6881,#6882,#6883,#6884,#6885,#6886,
#6887,#6888,#6889,#6890,#6891),.UNSPECIFIED.,.F.,.F.,(4,1,1,1,1,1,1,1,4),
(13.6848802223035,13.83746193894,14.8258520774357,15.8142422159314,16.8026323544271,
17.7910224929229,18.7794126314186,19.7678027699143,19.9680655294831),
 .UNSPECIFIED.);
#93=B_SPLINE_CURVE_WITH_KNOTS('',3,(#6893,#6894,#6895,#6896,#6897,#6898,
#6899,#6900,#6901,#6902),.UNSPECIFIED.,.F.,.F.,(4,1,1,1,1,1,1,4),(19.9680655294831,
20.75619290841,21.7445830469057,22.7329731854014,23.7213633238971,24.7097534623929,
25.6981436008886,26.2512508366627),.UNSPECIFIED.);
#94=B_SPLINE_CURVE_WITH_KNOTS('',3,(#6904,#6905,#6906,#6907,#6908,#6909,
#6910,#6911,#6912,#6913),.UNSPECIFIED.,.F.,.F.,(4,1,1,1,1,1,1,4),(26.2512508366627,
26.6865337393843,27.67492387788,28.6633140163757,29.6517041548714,30.6400942933671,
31.6284844318629,32.5344361438423),.UNSPECIFIED.);
#95=B_SPLINE_CURVE_WITH_KNOTS('',3,(#6915,#6916,#6917,#6918,#6919,#6920,
#6921,#6922,#6923,#6924,#6925),.UNSPECIFIED.,.F.,.F.,(4,1,1,1,1,1,1,1,4),
(32.5344361438423,32.6168745703586,33.6052647088543,34.59365484735,35.5820449858457,
36.5704351243414,37.5588252628371,38.5472154013329,38.8176214510219),
 .UNSPECIFIED.);
#96=B_SPLINE_CURVE_WITH_KNOTS('',3,(#6927,#6928,#6929,#6930,#6931,#6932,
#6933,#6934,#6935,#6936),.UNSPECIFIED.,.F.,.F.,(4,1,1,1,1,1,1,4),(38.8176214510219,
39.5356055398286,40.5239956783243,41.51238581682,42.5007759553157,43.4891660938114,
44.4775562323071,45.1008067582015),.UNSPECIFIED.);
#97=B_SPLINE_CURVE_WITH_KNOTS('',3,(#6938,#6939,#6940,#6941,#6942,#6943,
#6944,#6945,#6946,#6947),.UNSPECIFIED.,.F.,.F.,(4,1,1,1,1,1,1,4),(45.1008067582015,
45.4659463708029,46.4543365092986,47.4427266477943,48.43111678629,49.4195069247857,
50.4078970632814,51.3839920653811),.UNSPECIFIED.);
#98=B_SPLINE_CURVE_WITH_KNOTS('',3,(#6949,#6950,#6951,#6952,#6953,#6954,
#6955,#6956,#6957,#6958,#6959,#6960),.UNSPECIFIED.,.F.,.F.,(4,2,1,1,1,1,
1,1,4),(51.3839920653811,51.3962872017771,52.3846773402729,53.3730674787686,
54.3614576172643,55.34984775576,56.3382378942557,57.3266280327514,57.6671773725607),
 .UNSPECIFIED.);
#99=B_SPLINE_CURVE_WITH_KNOTS('',3,(#6962,#6963,#6964,#6965,#6966,#6967,
#6968,#6969,#6970,#6971),.UNSPECIFIED.,.F.,.F.,(4,1,1,1,1,1,1,4),(57.6671773725607,
58.3150181712471,59.3034083097429,60.2917984482386,61.2801885867343,62.26857872523,
63.2569688637257,63.9503626797403),.UNSPECIFIED.);
#100=B_SPLINE_CURVE_WITH_KNOTS('',3,(#6973,#6974,#6975,#6976,#6977,#6978,
#6979,#6980,#6981,#6982,#6983),.UNSPECIFIED.,.F.,.F.,(4,1,1,1,1,1,1,1,4),
(63.9503626797403,64.2453590022215,65.2337491407172,66.2221392792129,67.2105294177086,
68.1989195562043,69.1873096947,70.1756998331957,70.2335479869199),
 .UNSPECIFIED.);
#101=B_SPLINE_CURVE_WITH_KNOTS('',3,(#6985,#6986,#6987,#6988,#6989),
 .UNSPECIFIED.,.F.,.F.,(4,1,4),(70.2335479869199,71.1640899716914,72.0600176124814),
 .UNSPECIFIED.);
#102=B_SPLINE_CURVE_WITH_KNOTS('',3,(#6993,#6994,#6995,#6996,#6997,#6998,
#6999,#7000,#7001,#7002,#7003,#7004,#7005,#7006,#7007,#7008,#7009,#7010,
#7011,#7012,#7013,#7014,#7015,#7016,#7017,#7018,#7019,#7020),
 .UNSPECIFIED.,.F.,.F.,(4,3,3,3,3,3,3,3,3,4),(-74.1292603871786,-74.014023363696,
-73.9035575273749,-73.7931227076102,-73.6826829382937,-73.5722022608866,
-73.4615630851229,-73.3508315426675,-73.2398888203009,-73.2073641993181),
 .UNSPECIFIED.);
#103=B_SPLINE_CURVE_WITH_KNOTS('',3,(#7022,#7023,#7024,#7025,#7026,#7027,
#7028,#7029,#7030,#7031,#7032),.UNSPECIFIED.,.F.,.F.,(4,1,1,1,1,1,1,1,4),
(-73.2073641993181,-73.1408702486829,-72.1524801101872,-71.1640899716915,
-70.1756998331958,-69.1873096947,-68.1989195562043,-67.2105294177086,-66.9241788921385),
 .UNSPECIFIED.);
#104=B_SPLINE_CURVE_WITH_KNOTS('',3,(#7034,#7035,#7036,#7037,#7038,#7039,
#7040,#7041,#7042,#7043),.UNSPECIFIED.,.F.,.F.,(4,1,1,1,1,1,1,4),(-66.9241788921385,
-66.2221392792129,-65.2337491407172,-64.2453590022215,-63.2569688637258,
-62.26857872523,-61.2801885867343,-60.6409935849589),.UNSPECIFIED.);
#105=B_SPLINE_CURVE_WITH_KNOTS('',3,(#7045,#7046,#7047,#7048,#7049,#7050,
#7051,#7052,#7053,#7054,#7055),.UNSPECIFIED.,.F.,.F.,(4,1,1,1,1,1,1,1,4),
(-60.6409935849589,-60.2917984482386,-59.3034083097429,-58.3150181712472,
-57.3266280327515,-56.3382378942557,-55.34984775576,-54.3614576172643,-54.3578082777793),
 .UNSPECIFIED.);
#106=B_SPLINE_CURVE_WITH_KNOTS('',3,(#7057,#7058,#7059,#7060,#7061,#7062,
#7063,#7064,#7065,#7066),.UNSPECIFIED.,.F.,.F.,(4,1,1,1,1,1,1,4),(-54.3578082777793,
-53.3730674787686,-52.3846773402729,-51.3962872017772,-50.4078970632814,
-49.4195069247857,-48.43111678629,-48.0746229705997),.UNSPECIFIED.);
#107=B_SPLINE_CURVE_WITH_KNOTS('',3,(#7068,#7069,#7070,#7071,#7072,#7073,
#7074,#7075,#7076,#7077),.UNSPECIFIED.,.F.,.F.,(4,1,1,1,1,1,1,4),(-48.0746229705997,
-47.4427266477943,-46.4543365092986,-45.4659463708029,-44.4775562323072,
-43.4891660938114,-42.5007759553157,-41.7914376634201),.UNSPECIFIED.);
#108=B_SPLINE_CURVE_WITH_KNOTS('',3,(#7079,#7080,#7081,#7082,#7083,#7084,
#7085,#7086,#7087,#7088,#7089),.UNSPECIFIED.,.F.,.F.,(4,1,1,1,1,1,1,1,4),
(-41.7914376634201,-41.51238581682,-40.5239956783243,-39.5356055398286,
-38.5472154013329,-37.5588252628372,-36.5704351243414,-35.5820449858457,
-35.5082523562405),.UNSPECIFIED.);
#109=B_SPLINE_CURVE_WITH_KNOTS('',3,(#7091,#7092,#7093,#7094,#7095,#7096,
#7097,#7098,#7099,#7100),.UNSPECIFIED.,.F.,.F.,(4,1,1,1,1,1,1,4),(-35.5082523562405,
-34.59365484735,-33.6052647088543,-32.6168745703586,-31.6284844318629,-30.6400942933672,
-29.6517041548714,-29.2250670490609),.UNSPECIFIED.);
#110=B_SPLINE_CURVE_WITH_KNOTS('',3,(#7102,#7103,#7104,#7105,#7106,#7107,
#7108,#7109,#7110,#7111),.UNSPECIFIED.,.F.,.F.,(4,1,1,1,1,1,1,4),(-29.2250670490609,
-28.6633140163757,-27.67492387788,-26.6865337393843,-25.6981436008886,-24.7097534623929,
-23.7213633238972,-22.9418817418813),.UNSPECIFIED.);
#111=B_SPLINE_CURVE_WITH_KNOTS('',3,(#7113,#7114,#7115,#7116,#7117,#7118,
#7119,#7120,#7121,#7122,#7123),.UNSPECIFIED.,.F.,.F.,(4,1,1,1,1,1,1,1,4),
(-22.9418817418813,-22.7329731854014,-21.7445830469057,-20.75619290841,
-19.7678027699143,-18.7794126314186,-17.7910224929229,-16.8026323544271,
-16.6586964347017),.UNSPECIFIED.);
#112=B_SPLINE_CURVE_WITH_KNOTS('',3,(#7125,#7126,#7127,#7128,#7129,#7130,
#7131,#7132,#7133,#7134),.UNSPECIFIED.,.F.,.F.,(4,1,1,1,1,1,1,4),(-16.6586964347017,
-15.8142422159314,-14.8258520774357,-13.83746193894,-12.8490718004443,-11.8606816619486,
-10.8722915234529,-10.3755111275222),.UNSPECIFIED.);
#113=B_SPLINE_CURVE_WITH_KNOTS('',3,(#7135,#7136,#7137,#7138,#7139,#7140,
#7141,#7142,#7143,#7144,#7145,#7146,#7147,#7148,#7149,#7150,#7151,#7152,
#7153,#7154,#7155,#7156,#7157,#7158,#7159,#7160,#7161,#7162,#7163,#7164,
#7165,#7166,#7167,#7168,#7169,#7170,#7171,#7172,#7173,#7174,#7175,#7176,
#7177,#7178,#7179,#7180,#7181,#7182,#7183,#7184,#7185,#7186,#7187,#7188,
#7189,#7190,#7191,#7192,#7193,#7194,#7195,#7196,#7197,#7198,#7199,#7200,
#7201,#7202,#7203,#7204,#7205,#7206,#7207,#7208,#7209,#7210,#7211,#7212,
#7213,#7214,#7215,#7216,#7217,#7218,#7219,#7220,#7221,#7222,#7223,#7224,
#7225,#7226,#7227,#7228,#7229,#7230,#7231,#7232,#7233,#7234,#7235,#7236,
#7237,#7238,#7239,#7240,#7241,#7242,#7243,#7244,#7245,#7246,#7247,#7248,
#7249,#7250,#7251,#7252,#7253,#7254,#7255,#7256,#7257,#7258,#7259,#7260,
#7261,#7262,#7263,#7264,#7265,#7266,#7267,#7268,#7269,#7270,#7271,#7272,
#7273,#7274,#7275,#7276,#7277,#7278,#7279,#7280,#7281,#7282,#7283,#7284,
#7285,#7286,#7287,#7288,#7289,#7290,#7291,#7292,#7293,#7294,#7295,#7296,
#7297,#7298,#7299,#7300,#7301,#7302,#7303,#7304,#7305,#7306,#7307,#7308,
#7309),.UNSPECIFIED.,.F.,.F.,(4,3,3,3,3,3,3,3,3,3,3,3,3,3,3,3,3,3,3,3,3,
3,3,3,3,3,3,3,3,3,3,3,3,3,3,3,3,3,3,3,3,3,3,3,3,3,3,3,3,3,3,3,3,3,3,3,3,
3,4),(-10.3755111025761,-10.2614689943702,-10.1471056802317,-10.0325664532904,
-9.91772759343654,-9.88390138495715,-9.77466328603903,-9.66476928109183,
-9.55582418286387,-9.446943997502,-9.33808902015295,-9.22744457673007,-9.11845375896544,
-9.00698250271344,-8.89551124646144,-8.78626851305079,-8.67637508741516,
-8.56742517260818,-8.45854011672707,-8.34968022359019,-8.23904044468407,
-8.13004465846976,-8.01858288321774,-7.90712110796572,-7.79790831958831,
-7.68801115082352,-7.57909129493945,-7.47023625590901,-7.36140628774901,
-7.25073745817926,-7.14177102748603,-7.03025099847802,-6.91873096947,-6.80947225831212,
-6.69958082989489,-6.59061547220279,-6.48171521526574,-6.37284038625179,
-6.26221549743242,-6.15320559159024,-6.04177321128226,-5.93034083097429,
-5.82106975234147,-5.71117986985861,-5.60220084897479,-5.49328648723783,
-5.38439713975623,-5.27378552793682,-5.16476027045818,-5.05335548146837,
-4.94195069247857,-4.83445286275916,-4.72709981013473,-4.61984927129259,
-4.51265914426547,-4.40542736627408,-4.29818096566019,-4.19077482677967,
-4.09232582034257),.UNSPECIFIED.);
#114=B_SPLINE_CURVE_WITH_KNOTS('',3,(#7312,#7313,#7314,#7315,#7316,#7317,
#7318,#7319,#7320,#7321,#7322,#7323,#7324,#7325,#7326,#7327,#7328,#7329,
#7330,#7331,#7332,#7333,#7334,#7335,#7336,#7337,#7338,#7339,#7340,#7341,
#7342,#7343,#7344,#7345,#7346,#7347,#7348,#7349,#7350,#7351,#7352,#7353,
#7354,#7355,#7356,#7357,#7358,#7359,#7360,#7361,#7362,#7363,#7364,#7365,
#7366,#7367,#7368,#7369,#7370,#7371,#7372,#7373,#7374,#7375,#7376,#7377,
#7378,#7379,#7380,#7381,#7382,#7383,#7384,#7385,#7386,#7387,#7388,#7389,
#7390,#7391,#7392,#7393,#7394,#7395,#7396,#7397,#7398,#7399,#7400,#7401,
#7402,#7403,#7404,#7405,#7406,#7407,#7408,#7409,#7410,#7411,#7412,#7413,
#7414,#7415,#7416,#7417,#7418,#7419,#7420,#7421,#7422,#7423,#7424,#7425,
#7426,#7427,#7428,#7429,#7430,#7431,#7432,#7433,#7434,#7435,#7436,#7437,
#7438,#7439,#7440,#7441,#7442,#7443,#7444,#7445,#7446,#7447,#7448,#7449,
#7450,#7451,#7452,#7453,#7454,#7455,#7456,#7457,#7458,#7459,#7460,#7461,
#7462,#7463,#7464,#7465),.UNSPECIFIED.,.F.,.F.,(4,2,2,2,2,2,2,2,2,2,2,2,
2,2,2,2,2,2,2,2,2,2,2,2,2,2,2,2,2,2,2,2,2,2,2,2,2,2,2,2,2,2,2,2,2,2,2,2,
2,2,2,2,2,2,2,2,2,2,2,2,2,2,2,2,2,2,2,2,2,2,2,2,2,2,2,2,4),(0.0019271125636388,
0.0359882586975409,0.0488495312971493,0.053884776286046,0.0575798993696898,
0.061533608308059,0.0679528681421754,0.09694686298088,0.110574076667147,
0.118468402614831,0.121437295887913,0.123533451649698,0.125924118639411,
0.130471602975681,0.151602133207587,0.170896061494497,0.182719350336417,
0.187575881186773,0.191205611514928,0.195147824979162,0.201672627265219,
0.231619614775219,0.245840725214441,0.251413458609416,0.255672786850559,
0.257990756854425,0.260031973366808,0.262954354156453,0.270390438492984,
0.29405438915914,0.316492447629417,0.322202831441264,0.32595083015959,0.329568877776729,
0.33395574597341,0.345268569245878,0.384140969187585,0.390289845099253,
0.392943121292912,0.39476247355183,0.397149705141244,0.401616678980508,
0.419464108466401,0.44127771261733,0.453941340636418,0.458906304353505,
0.462547142592922,0.466436528546787,0.472723312330512,0.503918813642895,
0.517174552285323,0.524936547689952,0.527847585423213,0.529899856004968,
0.53224623173506,0.536515539926699,0.566259134935688,0.585849849580721,
0.592322830082281,0.596243357140048,0.599858860622756,0.604619302853052,
0.615285948369656,0.654774978012272,0.660979991486942,0.663654313514544,
0.66548177482559,0.667867512905708,0.672337417126603,0.692659143088369,
0.719694546424965,0.727100056009227,0.731203617792598,0.734774906305486,
0.739265237973076,0.748788247652177,0.782675134033573),.UNSPECIFIED.);
#115=B_SPLINE_CURVE_WITH_KNOTS('',3,(#7469,#7470,#7471,#7472,#7473,#7474,
#7475,#7476,#7477,#7478,#7479,#7480,#7481,#7482,#7483,#7484,#7485,#7486,
#7487,#7488,#7489,#7490,#7491,#7492,#7493,#7494,#7495,#7496,#7497,#7498,
#7499,#7500,#7501,#7502,#7503,#7504,#7505,#7506,#7507,#7508,#7509,#7510,
#7511,#7512,#7513,#7514,#7515,#7516,#7517,#7518,#7519,#7520,#7521,#7522,
#7523,#7524,#7525,#7526,#7527,#7528,#7529,#7530,#7531,#7532,#7533,#7534,
#7535,#7536,#7537,#7538,#7539,#7540,#7541,#7542,#7543,#7544,#7545,#7546,
#7547,#7548,#7549,#7550,#7551,#7552,#7553,#7554,#7555,#7556,#7557,#7558,
#7559,#7560,#7561,#7562,#7563,#7564,#7565,#7566,#7567,#7568,#7569,#7570,
#7571,#7572,#7573,#7574),.UNSPECIFIED.,.F.,.F.,(4,3,3,3,3,3,3,3,3,3,3,3,
3,3,3,3,3,3,3,3,3,3,3,3,3,3,3,3,3,3,3,3,3,3,3,4),(78.5398163401459,78.6561340881922,
78.7706355519136,78.8850310411815,78.9993690019213,79.11711633257,79.2315565783168,
79.3509574514166,79.4703583245163,79.5860523177359,79.7015449273291,79.8169263900411,
79.9322433694907,80.0475424284951,80.1629505027753,80.2784173412434,80.3940938012417,
80.458748463012,80.5730139624223,80.6870758225365,80.8010260233051,80.9149135960265,
81.028787466322,81.1427876464366,81.2568539755108,81.3711583644439,81.4471386015078,
81.5706873688198,81.6891165335582,81.8073967935847,81.925566265604,82.0436628949241,
82.1617581236453,82.2798497928827,82.3980223100823,82.4355287400035),
 .UNSPECIFIED.);
#116=B_SPLINE_CURVE_WITH_KNOTS('',3,(#7575,#7576,#7577,#7578,#7579,#7580,
#7581,#7582,#7583,#7584,#7585,#7586,#7587,#7588,#7589,#7590,#7591,#7592,
#7593,#7594,#7595,#7596,#7597,#7598),.UNSPECIFIED.,.F.,.F.,(4,2,2,2,2,2,
2,2,2,2,2,4),(-1.72176609592119,-1.71857158954466,-1.71581859485177,-1.7139477611094,
-1.71180394756969,-1.70832902031807,-1.69506735904276,-1.66549716493993,
-1.65388885134957,-1.64909455131773,-1.64550843441701,-1.6432613616363),
 .UNSPECIFIED.);
#117=B_SPLINE_CURVE_WITH_KNOTS('',3,(#7911,#7912,#7913,#7914,#7915,#7916,
#7917,#7918,#7919,#7920,#7921,#7922,#7923,#7924,#7925,#7926,#7927,#7928,
#7929,#7930,#7931,#7932,#7933,#7934,#7935,#7936,#7937,#7938,#7939,#7940,
#7941,#7942,#7943,#7944,#7945,#7946,#7947,#7948,#7949,#7950,#7951,#7952,
#7953,#7954,#7955,#7956,#7957,#7958,#7959,#7960,#7961,#7962,#7963,#7964,
#7965,#7966,#7967,#7968,#7969,#7970,#7971,#7972,#7973,#7974,#7975,#7976,
#7977,#7978,#7979,#7980,#7981,#7982,#7983,#7984,#7985,#7986,#7987,#7988,
#7989),.UNSPECIFIED.,.F.,.F.,(4,3,3,3,3,3,3,3,3,3,3,3,3,3,3,3,3,3,3,3,3,
3,3,3,3,3,4),(-0.319964203083861,-0.304228037518007,-0.284613148690911,
-0.276871331371113,-0.272257224906624,-0.252969211159584,-0.239387034404623,
-0.231434900380484,-0.227996911242295,-0.209251097418081,-0.190531504790305,
-0.171811912162528,-0.167655673991812,-0.1499077162788,-0.144306654204072,
-0.125663099898434,-0.11745065284486,-0.112094758046013,-0.10874239451909,
-0.0911202044344707,-0.0736624604297992,-0.0563420615200763,-0.0520648001853392,
-0.0351733175045267,-0.0188296765697835,-0.00258365319679502,0.),
 .UNSPECIFIED.);
#118=B_SPLINE_CURVE_WITH_KNOTS('',3,(#7990,#7991,#7992,#7993,#7994,#7995,
#7996,#7997,#7998,#7999,#8000,#8001,#8002,#8003,#8004,#8005,#8006,#8007,
#8008,#8009,#8010,#8011,#8012,#8013,#8014,#8015,#8016,#8017,#8018,#8019,
#8020,#8021,#8022,#8023,#8024,#8025,#8026,#8027,#8028,#8029,#8030,#8031,
#8032,#8033,#8034,#8035,#8036,#8037,#8038,#8039,#8040,#8041,#8042,#8043,
#8044,#8045,#8046,#8047,#8048,#8049,#8050,#8051,#8052,#8053,#8054,#8055,
#8056,#8057,#8058,#8059,#8060,#8061,#8062,#8063,#8064,#8065,#8066,#8067,
#8068,#8069,#8070,#8071),.UNSPECIFIED.,.F.,.F.,(4,3,3,3,3,3,3,3,3,3,3,3,
3,3,3,3,3,3,3,3,3,3,3,3,3,3,3,4),(0.,0.0128150276685244,0.0291235486693142,
0.0458461102161369,0.052840853654919,0.0569615705457033,0.0648285591165465,
0.0821842191184943,0.0998369062260194,0.108571225247779,0.112969449381281,
0.131127949227731,0.149229095291533,0.158622885237427,0.169525023140723,
0.17289105881689,0.190819970311636,0.209351312635224,0.223582858937968,
0.228841969886222,0.234245615182723,0.253464440755347,0.269667484046342,
0.274196754530456,0.277710493273208,0.297309565454661,0.316738144166086,
0.319979638214873),.UNSPECIFIED.);
#119=B_SPLINE_CURVE_WITH_KNOTS('',3,(#8385,#8386,#8387,#8388,#8389,#8390,
#8391,#8392,#8393,#8394,#8395,#8396,#8397,#8398,#8399,#8400,#8401,#8402,
#8403,#8404,#8405,#8406,#8407,#8408,#8409,#8410,#8411,#8412,#8413,#8414,
#8415,#8416,#8417,#8418,#8419,#8420,#8421,#8422,#8423,#8424,#8425,#8426,
#8427,#8428,#8429,#8430,#8431,#8432,#8433,#8434,#8435,#8436,#8437,#8438,
#8439,#8440,#8441,#8442,#8443,#8444,#8445,#8446,#8447,#8448,#8449,#8450,
#8451,#8452,#8453,#8454,#8455,#8456,#8457,#8458,#8459,#8460,#8461,#8462,
#8463,#8464,#8465,#8466,#8467,#8468,#8469,#8470,#8471,#8472),
 .UNSPECIFIED.,.F.,.F.,(4,3,3,3,3,3,3,3,3,3,3,3,3,3,3,3,3,3,3,3,3,3,3,3,
3,3,3,3,3,4),(-0.321499574649745,-0.308639510237196,-0.292262552050655,
-0.285372565290688,-0.282077555907296,-0.265037557387853,-0.252192985904029,
-0.24784545954478,-0.243738192672081,-0.226094652565765,-0.208132202142491,
-0.196707016120459,-0.191486671532126,-0.188416440693185,-0.185204704484879,
-0.166696376310579,-0.162287577878747,-0.144403429113291,-0.13537821479371,
-0.129752321066448,-0.125753449476847,-0.107263748186351,-0.0882397721456158,
-0.0692157961048804,-0.0657197649701159,-0.0625694288177743,-0.0429999128835448,
-0.0235085207817788,-0.00419545160864722,0.),.UNSPECIFIED.);
#120=B_SPLINE_CURVE_WITH_KNOTS('',3,(#8473,#8474,#8475,#8476),
 .UNSPECIFIED.,.F.,.F.,(4,4),(0.,0.0112718986101486),.UNSPECIFIED.);
#121=B_SPLINE_CURVE_WITH_KNOTS('',3,(#8477,#8478,#8479,#8480,#8481,#8482,
#8483,#8484,#8485,#8486,#8487,#8488,#8489,#8490,#8491,#8492,#8493,#8494,
#8495,#8496,#8497,#8498,#8499,#8500,#8501,#8502,#8503,#8504,#8505,#8506,
#8507,#8508,#8509,#8510,#8511,#8512,#8513,#8514,#8515,#8516,#8517,#8518,
#8519,#8520,#8521,#8522,#8523,#8524,#8525,#8526,#8527,#8528,#8529,#8530,
#8531,#8532,#8533,#8534,#8535,#8536,#8537,#8538,#8539,#8540,#8541,#8542,
#8543,#8544,#8545,#8546,#8547,#8548,#8549,#8550,#8551,#8552,#8553,#8554,
#8555,#8556,#8557,#8558),.UNSPECIFIED.,.F.,.F.,(4,3,3,3,3,3,3,3,3,3,3,3,
3,3,3,3,3,3,3,3,3,3,3,3,3,3,3,4),(0.,0.0158313618666332,0.0352739749108183,
0.0549065400622293,0.0614660392741775,0.0648988561933009,0.0684243966151204,
0.0875181682202572,0.107484385696968,0.125932139403052,0.127450603173679,
0.130444599968218,0.148719087235956,0.166424962509677,0.176672078090267,
0.186480980745562,0.190515610764009,0.208325400012171,0.226979737992308,
0.244665188163836,0.245634075972445,0.248879896927083,0.266153517834279,
0.280651005930739,0.284205126944081,0.287929482087063,0.304714528368394,
0.321499574649725),.UNSPECIFIED.);
#172=TOROIDAL_SURFACE('',#2037,3.01701820384648,0.700000000000003);
#179=SHAPE_REPRESENTATION_RELATIONSHIP('SRR','None',#14581,#187);
#187=ADVANCED_BREP_SHAPE_REPRESENTATION('',(#203),#14541);
#195=STYLED_ITEM('',(#14627),#203);
#203=MANIFOLD_SOLID_BREP('Body1',#1831);
#223=LINE('',#2733,#279);
#224=LINE('',#2967,#280);
#225=LINE('',#3176,#281);
#226=LINE('',#3544,#282);
#227=LINE('',#3929,#283);
#228=LINE('',#4294,#284);
#229=LINE('',#4661,#285);
#230=LINE('',#5036,#286);
#231=LINE('',#5403,#287);
#232=LINE('',#5772,#288);
#233=LINE('',#6149,#289);
#234=LINE('',#8569,#290);
#235=LINE('',#8572,#291);
#236=LINE('',#8577,#292);
#237=LINE('',#8584,#293);
#238=LINE('',#8595,#294);
#239=LINE('',#8600,#295);
#279=VECTOR('',#2311,1.366);
#280=VECTOR('',#2316,1.366);
#281=VECTOR('',#2319,1.366);
#282=VECTOR('',#2322,1.366);
#283=VECTOR('',#2325,1.366);
#284=VECTOR('',#2328,1.366);
#285=VECTOR('',#2331,1.366);
#286=VECTOR('',#2334,1.366);
#287=VECTOR('',#2337,1.366);
#288=VECTOR('',#2340,1.366);
#289=VECTOR('',#2343,1.366);
#290=VECTOR('',#2368,3.51922397520286);
#291=VECTOR('',#2371,3.34979916874976);
#292=VECTOR('',#2378,3.18037436229666);
#293=VECTOR('',#2387,3.71701820384649);
#294=VECTOR('',#2402,1.4890246697361);
#295=VECTOR('',#2409,2.72578406873475);
#335=CYLINDRICAL_SURFACE('',#2005,1.366);
#336=CYLINDRICAL_SURFACE('',#2007,1.366);
#337=CYLINDRICAL_SURFACE('',#2008,1.366);
#338=CYLINDRICAL_SURFACE('',#2009,1.366);
#339=CYLINDRICAL_SURFACE('',#2010,1.366);
#340=CYLINDRICAL_SURFACE('',#2011,1.366);
#341=CYLINDRICAL_SURFACE('',#2012,1.366);
#342=CYLINDRICAL_SURFACE('',#2013,1.366);
#343=CYLINDRICAL_SURFACE('',#2014,1.366);
#344=CYLINDRICAL_SURFACE('',#2015,1.366);
#345=CYLINDRICAL_SURFACE('',#2016,1.366);
#346=CYLINDRICAL_SURFACE('',#2017,1.70825);
#347=CYLINDRICAL_SURFACE('',#2020,1.366);
#348=CYLINDRICAL_SURFACE('',#2027,3.51922397520286);
#349=CYLINDRICAL_SURFACE('',#2031,3.18037436229666);
#350=CYLINDRICAL_SURFACE('',#2035,3.71701820384649);
#351=CYLINDRICAL_SURFACE('',#2042,1.4890246697361);
#352=CYLINDRICAL_SURFACE('',#2046,2.72578406873475);
#385=FACE_BOUND('',#574,.T.);
#386=FACE_BOUND('',#579,.T.);
#387=FACE_BOUND('',#583,.T.);
#388=FACE_BOUND('',#586,.T.);
#436=FACE_OUTER_BOUND('',#556,.T.);
#437=FACE_OUTER_BOUND('',#557,.T.);
#438=FACE_OUTER_BOUND('',#558,.T.);
#439=FACE_OUTER_BOUND('',#559,.T.);
#440=FACE_OUTER_BOUND('',#560,.T.);
#441=FACE_OUTER_BOUND('',#561,.T.);
#442=FACE_OUTER_BOUND('',#562,.T.);
#443=FACE_OUTER_BOUND('',#563,.T.);
#444=FACE_OUTER_BOUND('',#564,.T.);
#445=FACE_OUTER_BOUND('',#565,.T.);
#446=FACE_OUTER_BOUND('',#566,.T.);
#447=FACE_OUTER_BOUND('',#567,.T.);
#448=FACE_OUTER_BOUND('',#568,.T.);
#449=FACE_OUTER_BOUND('',#569,.T.);
#450=FACE_OUTER_BOUND('',#570,.T.);
#451=FACE_OUTER_BOUND('',#571,.T.);
#452=FACE_OUTER_BOUND('',#572,.T.);
#453=FACE_OUTER_BOUND('',#573,.T.);
#454=FACE_OUTER_BOUND('',#575,.T.);
#455=FACE_OUTER_BOUND('',#576,.T.);
#456=FACE_OUTER_BOUND('',#577,.T.);
#457=FACE_OUTER_BOUND('',#578,.T.);
#458=FACE_OUTER_BOUND('',#580,.T.);
#459=FACE_OUTER_BOUND('',#581,.T.);
#460=FACE_OUTER_BOUND('',#582,.T.);
#461=FACE_OUTER_BOUND('',#584,.T.);
#462=FACE_OUTER_BOUND('',#585,.T.);
#463=FACE_OUTER_BOUND('',#587,.T.);
#556=EDGE_LOOP('',(#1281,#1282,#1283,#1284));
#557=EDGE_LOOP('',(#1285,#1286,#1287,#1288,#1289,#1290));
#558=EDGE_LOOP('',(#1291,#1292,#1293,#1294,#1295));
#559=EDGE_LOOP('',(#1296,#1297,#1298,#1299,#1300));
#560=EDGE_LOOP('',(#1301,#1302,#1303,#1304,#1305));
#561=EDGE_LOOP('',(#1306,#1307,#1308,#1309,#1310));
#562=EDGE_LOOP('',(#1311,#1312,#1313,#1314,#1315));
#563=EDGE_LOOP('',(#1316,#1317,#1318,#1319,#1320));
#564=EDGE_LOOP('',(#1321,#1322,#1323,#1324,#1325));
#565=EDGE_LOOP('',(#1326,#1327,#1328,#1329,#1330));
#566=EDGE_LOOP('',(#1331,#1332,#1333,#1334,#1335));
#567=EDGE_LOOP('',(#1336,#1337,#1338,#1339,#1340,#1341,#1342,#1343,#1344,
#1345,#1346,#1347,#1348,#1349,#1350,#1351,#1352,#1353,#1354,#1355,#1356,
#1357,#1358,#1359,#1360,#1361,#1362,#1363));
#568=EDGE_LOOP('',(#1364,#1365,#1366,#1367,#1368));
#569=EDGE_LOOP('',(#1369,#1370,#1371,#1372,#1373,#1374,#1375,#1376,#1377,
#1378,#1379,#1380,#1381,#1382,#1383,#1384,#1385,#1386,#1387,#1388,#1389,
#1390,#1391,#1392,#1393,#1394,#1395,#1396,#1397,#1398,#1399,#1400,#1401));
#570=EDGE_LOOP('',(#1402,#1403,#1404,#1405,#1406,#1407,#1408,#1409,#1410,
#1411,#1412,#1413,#1414,#1415,#1416,#1417,#1418,#1419,#1420,#1421,#1422,
#1423,#1424,#1425,#1426,#1427,#1428,#1429,#1430,#1431,#1432,#1433,#1434,
#1435));
#571=EDGE_LOOP('',(#1436));
#572=EDGE_LOOP('',(#1437,#1438,#1439,#1440));
#573=EDGE_LOOP('',(#1441));
#574=EDGE_LOOP('',(#1442,#1443,#1444,#1445,#1446));
#575=EDGE_LOOP('',(#1447,#1448,#1449,#1450));
#576=EDGE_LOOP('',(#1451,#1452,#1453,#1454));
#577=EDGE_LOOP('',(#1455,#1456,#1457,#1458));
#578=EDGE_LOOP('',(#1459));
#579=EDGE_LOOP('',(#1460));
#580=EDGE_LOOP('',(#1461,#1462,#1463,#1464));
#581=EDGE_LOOP('',(#1465,#1466,#1467,#1468));
#582=EDGE_LOOP('',(#1469));
#583=EDGE_LOOP('',(#1470));
#584=EDGE_LOOP('',(#1471,#1472,#1473,#1474));
#585=EDGE_LOOP('',(#1475));
#586=EDGE_LOOP('',(#1476));
#587=EDGE_LOOP('',(#1477,#1478,#1479,#1480));
#676=CIRCLE('',#2006,1.366);
#677=CIRCLE('',#2018,1.70825);
#678=CIRCLE('',#2019,1.70825);
#679=CIRCLE('',#2021,1.366);
#680=CIRCLE('',#2023,2.72578406873475);
#681=CIRCLE('',#2026,3.51922397520286);
#682=CIRCLE('',#2028,3.51922397520286);
#683=CIRCLE('',#2030,3.18037436229666);
#684=CIRCLE('',#2032,3.18037436229666);
#685=CIRCLE('',#2034,3.71701820384649);
#686=CIRCLE('',#2036,3.71701820384649);
#687=CIRCLE('',#2038,3.01701820384649);
#688=CIRCLE('',#2039,0.700000000000003);
#689=CIRCLE('',#2041,1.4890246697361);
#690=CIRCLE('',#2043,1.4890246697361);
#691=CIRCLE('',#2045,2.72578406873475);
#762=VERTEX_POINT('',#2731);
#763=VERTEX_POINT('',#2732);
#764=VERTEX_POINT('',#2734);
#765=VERTEX_POINT('',#2865);
#766=VERTEX_POINT('',#2965);
#767=VERTEX_POINT('',#2966);
#768=VERTEX_POINT('',#2968);
#769=VERTEX_POINT('',#3147);
#770=VERTEX_POINT('',#3174);
#771=VERTEX_POINT('',#3175);
#772=VERTEX_POINT('',#3369);
#773=VERTEX_POINT('',#3542);
#774=VERTEX_POINT('',#3543);
#775=VERTEX_POINT('',#3545);
#776=VERTEX_POINT('',#3927);
#777=VERTEX_POINT('',#3928);
#778=VERTEX_POINT('',#4110);
#779=VERTEX_POINT('',#4292);
#780=VERTEX_POINT('',#4293);
#781=VERTEX_POINT('',#4295);
#782=VERTEX_POINT('',#4659);
#783=VERTEX_POINT('',#4660);
#784=VERTEX_POINT('',#4846);
#785=VERTEX_POINT('',#5034);
#786=VERTEX_POINT('',#5035);
#787=VERTEX_POINT('',#5037);
#788=VERTEX_POINT('',#5401);
#789=VERTEX_POINT('',#5402);
#790=VERTEX_POINT('',#5586);
#791=VERTEX_POINT('',#5770);
#792=VERTEX_POINT('',#5771);
#793=VERTEX_POINT('',#5773);
#794=VERTEX_POINT('',#6147);
#795=VERTEX_POINT('',#6148);
#796=VERTEX_POINT('',#6326);
#797=VERTEX_POINT('',#6512);
#798=VERTEX_POINT('',#6513);
#799=VERTEX_POINT('',#6520);
#800=VERTEX_POINT('',#6522);
#801=VERTEX_POINT('',#6528);
#802=VERTEX_POINT('',#6704);
#803=VERTEX_POINT('',#6880);
#804=VERTEX_POINT('',#6892);
#805=VERTEX_POINT('',#6903);
#806=VERTEX_POINT('',#6914);
#807=VERTEX_POINT('',#6926);
#808=VERTEX_POINT('',#6937);
#809=VERTEX_POINT('',#6948);
#810=VERTEX_POINT('',#6961);
#811=VERTEX_POINT('',#6972);
#812=VERTEX_POINT('',#6984);
#813=VERTEX_POINT('',#6990);
#814=VERTEX_POINT('',#6992);
#815=VERTEX_POINT('',#7021);
#816=VERTEX_POINT('',#7033);
#817=VERTEX_POINT('',#7044);
#818=VERTEX_POINT('',#7056);
#819=VERTEX_POINT('',#7067);
#820=VERTEX_POINT('',#7078);
#821=VERTEX_POINT('',#7090);
#822=VERTEX_POINT('',#7101);
#823=VERTEX_POINT('',#7112);
#824=VERTEX_POINT('',#7124);
#825=VERTEX_POINT('',#7311);
#826=VERTEX_POINT('',#7466);
#827=VERTEX_POINT('',#7468);
#828=VERTEX_POINT('',#8384);
#829=VERTEX_POINT('',#8560);
#830=VERTEX_POINT('',#8564);
#831=VERTEX_POINT('',#8567);
#832=VERTEX_POINT('',#8571);
#833=VERTEX_POINT('',#8575);
#834=VERTEX_POINT('',#8579);
#835=VERTEX_POINT('',#8582);
#836=VERTEX_POINT('',#8586);
#837=VERTEX_POINT('',#8590);
#838=VERTEX_POINT('',#8593);
#839=VERTEX_POINT('',#8597);
#969=EDGE_CURVE('',#762,#763,#223,.T.);
#970=EDGE_CURVE('',#764,#762,#55,.T.);
#971=EDGE_CURVE('',#765,#764,#676,.T.);
#972=EDGE_CURVE('',#765,#763,#56,.T.);
#973=EDGE_CURVE('',#766,#767,#224,.T.);
#974=EDGE_CURVE('',#768,#766,#57,.F.);
#975=EDGE_CURVE('',#762,#768,#58,.T.);
#976=EDGE_CURVE('',#763,#769,#59,.T.);
#977=EDGE_CURVE('',#769,#767,#60,.T.);
#978=EDGE_CURVE('',#770,#771,#225,.T.);
#979=EDGE_CURVE('',#766,#770,#61,.F.);
#980=EDGE_CURVE('',#767,#772,#62,.T.);
#981=EDGE_CURVE('',#772,#771,#63,.T.);
#982=EDGE_CURVE('',#773,#774,#226,.T.);
#983=EDGE_CURVE('',#775,#773,#64,.F.);
#984=EDGE_CURVE('',#770,#775,#65,.F.);
#985=EDGE_CURVE('',#771,#774,#66,.T.);
#986=EDGE_CURVE('',#776,#777,#227,.T.);
#987=EDGE_CURVE('',#773,#776,#67,.F.);
#988=EDGE_CURVE('',#774,#778,#68,.T.);
#989=EDGE_CURVE('',#778,#777,#69,.T.);
#990=EDGE_CURVE('',#779,#780,#228,.T.);
#991=EDGE_CURVE('',#781,#779,#70,.F.);
#992=EDGE_CURVE('',#776,#781,#71,.F.);
#993=EDGE_CURVE('',#777,#780,#72,.T.);
#994=EDGE_CURVE('',#782,#783,#229,.T.);
#995=EDGE_CURVE('',#779,#782,#73,.F.);
#996=EDGE_CURVE('',#780,#784,#74,.T.);
#997=EDGE_CURVE('',#784,#783,#75,.T.);
#998=EDGE_CURVE('',#785,#786,#230,.T.);
#999=EDGE_CURVE('',#787,#785,#76,.F.);
#1000=EDGE_CURVE('',#782,#787,#77,.F.);
#1001=EDGE_CURVE('',#783,#786,#78,.T.);
#1002=EDGE_CURVE('',#788,#789,#231,.T.);
#1003=EDGE_CURVE('',#785,#788,#79,.F.);
#1004=EDGE_CURVE('',#786,#790,#80,.T.);
#1005=EDGE_CURVE('',#790,#789,#81,.T.);
#1006=EDGE_CURVE('',#791,#792,#232,.T.);
#1007=EDGE_CURVE('',#793,#791,#82,.F.);
#1008=EDGE_CURVE('',#788,#793,#83,.F.);
#1009=EDGE_CURVE('',#789,#792,#84,.T.);
#1010=EDGE_CURVE('',#794,#795,#233,.T.);
#1011=EDGE_CURVE('',#791,#794,#85,.F.);
#1012=EDGE_CURVE('',#792,#796,#86,.T.);
#1013=EDGE_CURVE('',#796,#795,#87,.F.);
#1014=EDGE_CURVE('',#797,#798,#88,.T.);
#1015=EDGE_CURVE('',#798,#799,#677,.T.);
#1016=EDGE_CURVE('',#799,#800,#89,.T.);
#1017=EDGE_CURVE('',#800,#801,#90,.T.);
#1018=EDGE_CURVE('',#801,#802,#91,.T.);
#1019=EDGE_CURVE('',#802,#803,#92,.T.);
#1020=EDGE_CURVE('',#803,#804,#93,.T.);
#1021=EDGE_CURVE('',#804,#805,#94,.T.);
#1022=EDGE_CURVE('',#805,#806,#95,.T.);
#1023=EDGE_CURVE('',#806,#807,#96,.T.);
#1024=EDGE_CURVE('',#807,#808,#97,.T.);
#1025=EDGE_CURVE('',#808,#809,#98,.T.);
#1026=EDGE_CURVE('',#809,#810,#99,.T.);
#1027=EDGE_CURVE('',#810,#811,#100,.T.);
#1028=EDGE_CURVE('',#811,#812,#101,.T.);
#1029=EDGE_CURVE('',#813,#812,#678,.T.);
#1030=EDGE_CURVE('',#813,#814,#102,.T.);
#1031=EDGE_CURVE('',#814,#815,#103,.T.);
#1032=EDGE_CURVE('',#815,#816,#104,.T.);
#1033=EDGE_CURVE('',#816,#817,#105,.T.);
#1034=EDGE_CURVE('',#817,#818,#106,.T.);
#1035=EDGE_CURVE('',#818,#819,#107,.T.);
#1036=EDGE_CURVE('',#819,#820,#108,.T.);
#1037=EDGE_CURVE('',#820,#821,#109,.T.);
#1038=EDGE_CURVE('',#821,#822,#110,.T.);
#1039=EDGE_CURVE('',#822,#823,#111,.T.);
#1040=EDGE_CURVE('',#823,#824,#112,.T.);
#1041=EDGE_CURVE('',#824,#797,#113,.T.);
#1042=EDGE_CURVE('',#795,#825,#114,.F.);
#1043=EDGE_CURVE('',#826,#825,#679,.T.);
#1044=EDGE_CURVE('',#827,#826,#115,.T.);
#1045=EDGE_CURVE('',#794,#827,#116,.F.);
#1046=EDGE_CURVE('',#812,#826,#117,.T.);
#1047=EDGE_CURVE('',#764,#799,#118,.T.);
#1048=EDGE_CURVE('',#828,#813,#119,.T.);
#1049=EDGE_CURVE('',#825,#828,#120,.T.);
#1050=EDGE_CURVE('',#798,#765,#121,.T.);
#1051=EDGE_CURVE('',#829,#829,#680,.T.);
#1052=EDGE_CURVE('',#830,#830,#681,.T.);
#1053=EDGE_CURVE('',#831,#831,#682,.T.);
#1054=EDGE_CURVE('',#831,#830,#234,.T.);
#1055=EDGE_CURVE('',#831,#832,#235,.T.);
#1056=EDGE_CURVE('',#832,#832,#683,.T.);
#1057=EDGE_CURVE('',#833,#833,#684,.T.);
#1058=EDGE_CURVE('',#833,#832,#236,.T.);
#1059=EDGE_CURVE('',#834,#834,#685,.T.);
#1060=EDGE_CURVE('',#835,#835,#686,.T.);
#1061=EDGE_CURVE('',#835,#834,#237,.T.);
#1062=EDGE_CURVE('',#836,#836,#687,.T.);
#1063=EDGE_CURVE('',#836,#835,#688,.T.);
#1064=EDGE_CURVE('',#837,#837,#689,.T.);
#1065=EDGE_CURVE('',#838,#838,#690,.T.);
#1066=EDGE_CURVE('',#838,#837,#238,.T.);
#1067=EDGE_CURVE('',#839,#839,#691,.T.);
#1068=EDGE_CURVE('',#829,#839,#239,.T.);
#1281=ORIENTED_EDGE('',*,*,#969,.F.);
#1282=ORIENTED_EDGE('',*,*,#970,.F.);
#1283=ORIENTED_EDGE('',*,*,#971,.F.);
#1284=ORIENTED_EDGE('',*,*,#972,.T.);
#1285=ORIENTED_EDGE('',*,*,#973,.F.);
#1286=ORIENTED_EDGE('',*,*,#974,.F.);
#1287=ORIENTED_EDGE('',*,*,#975,.F.);
#1288=ORIENTED_EDGE('',*,*,#969,.T.);
#1289=ORIENTED_EDGE('',*,*,#976,.T.);
#1290=ORIENTED_EDGE('',*,*,#977,.T.);
#1291=ORIENTED_EDGE('',*,*,#978,.F.);
#1292=ORIENTED_EDGE('',*,*,#979,.F.);
#1293=ORIENTED_EDGE('',*,*,#973,.T.);
#1294=ORIENTED_EDGE('',*,*,#980,.T.);
#1295=ORIENTED_EDGE('',*,*,#981,.T.);
#1296=ORIENTED_EDGE('',*,*,#982,.F.);
#1297=ORIENTED_EDGE('',*,*,#983,.F.);
#1298=ORIENTED_EDGE('',*,*,#984,.F.);
#1299=ORIENTED_EDGE('',*,*,#978,.T.);
#1300=ORIENTED_EDGE('',*,*,#985,.T.);
#1301=ORIENTED_EDGE('',*,*,#986,.F.);
#1302=ORIENTED_EDGE('',*,*,#987,.F.);
#1303=ORIENTED_EDGE('',*,*,#982,.T.);
#1304=ORIENTED_EDGE('',*,*,#988,.T.);
#1305=ORIENTED_EDGE('',*,*,#989,.T.);
#1306=ORIENTED_EDGE('',*,*,#990,.F.);
#1307=ORIENTED_EDGE('',*,*,#991,.F.);
#1308=ORIENTED_EDGE('',*,*,#992,.F.);
#1309=ORIENTED_EDGE('',*,*,#986,.T.);
#1310=ORIENTED_EDGE('',*,*,#993,.T.);
#1311=ORIENTED_EDGE('',*,*,#994,.F.);
#1312=ORIENTED_EDGE('',*,*,#995,.F.);
#1313=ORIENTED_EDGE('',*,*,#990,.T.);
#1314=ORIENTED_EDGE('',*,*,#996,.T.);
#1315=ORIENTED_EDGE('',*,*,#997,.T.);
#1316=ORIENTED_EDGE('',*,*,#998,.F.);
#1317=ORIENTED_EDGE('',*,*,#999,.F.);
#1318=ORIENTED_EDGE('',*,*,#1000,.F.);
#1319=ORIENTED_EDGE('',*,*,#994,.T.);
#1320=ORIENTED_EDGE('',*,*,#1001,.T.);
#1321=ORIENTED_EDGE('',*,*,#1002,.F.);
#1322=ORIENTED_EDGE('',*,*,#1003,.F.);
#1323=ORIENTED_EDGE('',*,*,#998,.T.);
#1324=ORIENTED_EDGE('',*,*,#1004,.T.);
#1325=ORIENTED_EDGE('',*,*,#1005,.T.);
#1326=ORIENTED_EDGE('',*,*,#1006,.F.);
#1327=ORIENTED_EDGE('',*,*,#1007,.F.);
#1328=ORIENTED_EDGE('',*,*,#1008,.F.);
#1329=ORIENTED_EDGE('',*,*,#1002,.T.);
#1330=ORIENTED_EDGE('',*,*,#1009,.T.);
#1331=ORIENTED_EDGE('',*,*,#1010,.F.);
#1332=ORIENTED_EDGE('',*,*,#1011,.F.);
#1333=ORIENTED_EDGE('',*,*,#1006,.T.);
#1334=ORIENTED_EDGE('',*,*,#1012,.T.);
#1335=ORIENTED_EDGE('',*,*,#1013,.T.);
#1336=ORIENTED_EDGE('',*,*,#1014,.T.);
#1337=ORIENTED_EDGE('',*,*,#1015,.T.);
#1338=ORIENTED_EDGE('',*,*,#1016,.T.);
#1339=ORIENTED_EDGE('',*,*,#1017,.T.);
#1340=ORIENTED_EDGE('',*,*,#1018,.T.);
#1341=ORIENTED_EDGE('',*,*,#1019,.T.);
#1342=ORIENTED_EDGE('',*,*,#1020,.T.);
#1343=ORIENTED_EDGE('',*,*,#1021,.T.);
#1344=ORIENTED_EDGE('',*,*,#1022,.T.);
#1345=ORIENTED_EDGE('',*,*,#1023,.T.);
#1346=ORIENTED_EDGE('',*,*,#1024,.T.);
#1347=ORIENTED_EDGE('',*,*,#1025,.T.);
#1348=ORIENTED_EDGE('',*,*,#1026,.T.);
#1349=ORIENTED_EDGE('',*,*,#1027,.T.);
#1350=ORIENTED_EDGE('',*,*,#1028,.T.);
#1351=ORIENTED_EDGE('',*,*,#1029,.F.);
#1352=ORIENTED_EDGE('',*,*,#1030,.T.);
#1353=ORIENTED_EDGE('',*,*,#1031,.T.);
#1354=ORIENTED_EDGE('',*,*,#1032,.T.);
#1355=ORIENTED_EDGE('',*,*,#1033,.T.);
#1356=ORIENTED_EDGE('',*,*,#1034,.T.);
#1357=ORIENTED_EDGE('',*,*,#1035,.T.);
#1358=ORIENTED_EDGE('',*,*,#1036,.T.);
#1359=ORIENTED_EDGE('',*,*,#1037,.T.);
#1360=ORIENTED_EDGE('',*,*,#1038,.T.);
#1361=ORIENTED_EDGE('',*,*,#1039,.T.);
#1362=ORIENTED_EDGE('',*,*,#1040,.T.);
#1363=ORIENTED_EDGE('',*,*,#1041,.T.);
#1364=ORIENTED_EDGE('',*,*,#1010,.T.);
#1365=ORIENTED_EDGE('',*,*,#1042,.T.);
#1366=ORIENTED_EDGE('',*,*,#1043,.F.);
#1367=ORIENTED_EDGE('',*,*,#1044,.F.);
#1368=ORIENTED_EDGE('',*,*,#1045,.F.);
#1369=ORIENTED_EDGE('',*,*,#1046,.F.);
#1370=ORIENTED_EDGE('',*,*,#1028,.F.);
#1371=ORIENTED_EDGE('',*,*,#1027,.F.);
#1372=ORIENTED_EDGE('',*,*,#1026,.F.);
#1373=ORIENTED_EDGE('',*,*,#1025,.F.);
#1374=ORIENTED_EDGE('',*,*,#1024,.F.);
#1375=ORIENTED_EDGE('',*,*,#1023,.F.);
#1376=ORIENTED_EDGE('',*,*,#1022,.F.);
#1377=ORIENTED_EDGE('',*,*,#1021,.F.);
#1378=ORIENTED_EDGE('',*,*,#1020,.F.);
#1379=ORIENTED_EDGE('',*,*,#1019,.F.);
#1380=ORIENTED_EDGE('',*,*,#1018,.F.);
#1381=ORIENTED_EDGE('',*,*,#1017,.F.);
#1382=ORIENTED_EDGE('',*,*,#1016,.F.);
#1383=ORIENTED_EDGE('',*,*,#1047,.F.);
#1384=ORIENTED_EDGE('',*,*,#970,.T.);
#1385=ORIENTED_EDGE('',*,*,#975,.T.);
#1386=ORIENTED_EDGE('',*,*,#974,.T.);
#1387=ORIENTED_EDGE('',*,*,#979,.T.);
#1388=ORIENTED_EDGE('',*,*,#984,.T.);
#1389=ORIENTED_EDGE('',*,*,#983,.T.);
#1390=ORIENTED_EDGE('',*,*,#987,.T.);
#1391=ORIENTED_EDGE('',*,*,#992,.T.);
#1392=ORIENTED_EDGE('',*,*,#991,.T.);
#1393=ORIENTED_EDGE('',*,*,#995,.T.);
#1394=ORIENTED_EDGE('',*,*,#1000,.T.);
#1395=ORIENTED_EDGE('',*,*,#999,.T.);
#1396=ORIENTED_EDGE('',*,*,#1003,.T.);
#1397=ORIENTED_EDGE('',*,*,#1008,.T.);
#1398=ORIENTED_EDGE('',*,*,#1007,.T.);
#1399=ORIENTED_EDGE('',*,*,#1011,.T.);
#1400=ORIENTED_EDGE('',*,*,#1045,.T.);
#1401=ORIENTED_EDGE('',*,*,#1044,.T.);
#1402=ORIENTED_EDGE('',*,*,#1048,.F.);
#1403=ORIENTED_EDGE('',*,*,#1049,.F.);
#1404=ORIENTED_EDGE('',*,*,#1042,.F.);
#1405=ORIENTED_EDGE('',*,*,#1013,.F.);
#1406=ORIENTED_EDGE('',*,*,#1012,.F.);
#1407=ORIENTED_EDGE('',*,*,#1009,.F.);
#1408=ORIENTED_EDGE('',*,*,#1005,.F.);
#1409=ORIENTED_EDGE('',*,*,#1004,.F.);
#1410=ORIENTED_EDGE('',*,*,#1001,.F.);
#1411=ORIENTED_EDGE('',*,*,#997,.F.);
#1412=ORIENTED_EDGE('',*,*,#996,.F.);
#1413=ORIENTED_EDGE('',*,*,#993,.F.);
#1414=ORIENTED_EDGE('',*,*,#989,.F.);
#1415=ORIENTED_EDGE('',*,*,#988,.F.);
#1416=ORIENTED_EDGE('',*,*,#985,.F.);
#1417=ORIENTED_EDGE('',*,*,#981,.F.);
#1418=ORIENTED_EDGE('',*,*,#980,.F.);
#1419=ORIENTED_EDGE('',*,*,#977,.F.);
#1420=ORIENTED_EDGE('',*,*,#976,.F.);
#1421=ORIENTED_EDGE('',*,*,#972,.F.);
#1422=ORIENTED_EDGE('',*,*,#1050,.F.);
#1423=ORIENTED_EDGE('',*,*,#1014,.F.);
#1424=ORIENTED_EDGE('',*,*,#1041,.F.);
#1425=ORIENTED_EDGE('',*,*,#1040,.F.);
#1426=ORIENTED_EDGE('',*,*,#1039,.F.);
#1427=ORIENTED_EDGE('',*,*,#1038,.F.);
#1428=ORIENTED_EDGE('',*,*,#1037,.F.);
#1429=ORIENTED_EDGE('',*,*,#1036,.F.);
#1430=ORIENTED_EDGE('',*,*,#1035,.F.);
#1431=ORIENTED_EDGE('',*,*,#1034,.F.);
#1432=ORIENTED_EDGE('',*,*,#1033,.F.);
#1433=ORIENTED_EDGE('',*,*,#1032,.F.);
#1434=ORIENTED_EDGE('',*,*,#1031,.F.);
#1435=ORIENTED_EDGE('',*,*,#1030,.F.);
#1436=ORIENTED_EDGE('',*,*,#1051,.T.);
#1437=ORIENTED_EDGE('',*,*,#1047,.T.);
#1438=ORIENTED_EDGE('',*,*,#1015,.F.);
#1439=ORIENTED_EDGE('',*,*,#1050,.T.);
#1440=ORIENTED_EDGE('',*,*,#971,.T.);
#1441=ORIENTED_EDGE('',*,*,#1052,.F.);
#1442=ORIENTED_EDGE('',*,*,#1029,.T.);
#1443=ORIENTED_EDGE('',*,*,#1046,.T.);
#1444=ORIENTED_EDGE('',*,*,#1043,.T.);
#1445=ORIENTED_EDGE('',*,*,#1049,.T.);
#1446=ORIENTED_EDGE('',*,*,#1048,.T.);
#1447=ORIENTED_EDGE('',*,*,#1053,.F.);
#1448=ORIENTED_EDGE('',*,*,#1054,.T.);
#1449=ORIENTED_EDGE('',*,*,#1052,.T.);
#1450=ORIENTED_EDGE('',*,*,#1054,.F.);
#1451=ORIENTED_EDGE('',*,*,#1053,.T.);
#1452=ORIENTED_EDGE('',*,*,#1055,.T.);
#1453=ORIENTED_EDGE('',*,*,#1056,.F.);
#1454=ORIENTED_EDGE('',*,*,#1055,.F.);
#1455=ORIENTED_EDGE('',*,*,#1057,.F.);
#1456=ORIENTED_EDGE('',*,*,#1058,.T.);
#1457=ORIENTED_EDGE('',*,*,#1056,.T.);
#1458=ORIENTED_EDGE('',*,*,#1058,.F.);
#1459=ORIENTED_EDGE('',*,*,#1059,.F.);
#1460=ORIENTED_EDGE('',*,*,#1057,.T.);
#1461=ORIENTED_EDGE('',*,*,#1060,.F.);
#1462=ORIENTED_EDGE('',*,*,#1061,.T.);
#1463=ORIENTED_EDGE('',*,*,#1059,.T.);
#1464=ORIENTED_EDGE('',*,*,#1061,.F.);
#1465=ORIENTED_EDGE('',*,*,#1062,.F.);
#1466=ORIENTED_EDGE('',*,*,#1063,.T.);
#1467=ORIENTED_EDGE('',*,*,#1060,.T.);
#1468=ORIENTED_EDGE('',*,*,#1063,.F.);
#1469=ORIENTED_EDGE('',*,*,#1062,.T.);
#1470=ORIENTED_EDGE('',*,*,#1064,.F.);
#1471=ORIENTED_EDGE('',*,*,#1065,.F.);
#1472=ORIENTED_EDGE('',*,*,#1066,.T.);
#1473=ORIENTED_EDGE('',*,*,#1064,.T.);
#1474=ORIENTED_EDGE('',*,*,#1066,.F.);
#1475=ORIENTED_EDGE('',*,*,#1067,.F.);
#1476=ORIENTED_EDGE('',*,*,#1065,.T.);
#1477=ORIENTED_EDGE('',*,*,#1051,.F.);
#1478=ORIENTED_EDGE('',*,*,#1068,.T.);
#1479=ORIENTED_EDGE('',*,*,#1067,.T.);
#1480=ORIENTED_EDGE('',*,*,#1068,.F.);
#1702=PLANE('',#2022);
#1703=PLANE('',#2024);
#1704=PLANE('',#2025);
#1705=PLANE('',#2033);
#1706=PLANE('',#2040);
#1707=PLANE('',#2044);
#1758=ADVANCED_FACE('',(#436),#335,.T.);
#1759=ADVANCED_FACE('',(#437),#336,.T.);
#1760=ADVANCED_FACE('',(#438),#337,.T.);
#1761=ADVANCED_FACE('',(#439),#338,.T.);
#1762=ADVANCED_FACE('',(#440),#339,.T.);
#1763=ADVANCED_FACE('',(#441),#340,.T.);
#1764=ADVANCED_FACE('',(#442),#341,.T.);
#1765=ADVANCED_FACE('',(#443),#342,.T.);
#1766=ADVANCED_FACE('',(#444),#343,.T.);
#1767=ADVANCED_FACE('',(#445),#344,.T.);
#1768=ADVANCED_FACE('',(#446),#345,.T.);
#1769=ADVANCED_FACE('',(#447),#346,.T.);
#1770=ADVANCED_FACE('',(#448),#347,.T.);
#1771=ADVANCED_FACE('',(#449),#51,.F.);
#1772=ADVANCED_FACE('',(#450),#52,.F.);
#1773=ADVANCED_FACE('',(#451),#1702,.T.);
#1774=ADVANCED_FACE('',(#452),#1703,.T.);
#1775=ADVANCED_FACE('',(#453,#385),#1704,.T.);
#1776=ADVANCED_FACE('',(#454),#348,.T.);
#1777=ADVANCED_FACE('',(#455),#43,.T.);
#1778=ADVANCED_FACE('',(#456),#349,.T.);
#1779=ADVANCED_FACE('',(#457,#386),#1705,.T.);
#1780=ADVANCED_FACE('',(#458),#350,.T.);
#1781=ADVANCED_FACE('',(#459),#172,.T.);
#1782=ADVANCED_FACE('',(#460,#387),#1706,.T.);
#1783=ADVANCED_FACE('',(#461),#351,.F.);
#1784=ADVANCED_FACE('',(#462,#388),#1707,.T.);
#1785=ADVANCED_FACE('',(#463),#352,.F.);
#1831=CLOSED_SHELL('',(#1758,#1759,#1760,#1761,#1762,#1763,#1764,#1765,
#1766,#1767,#1768,#1769,#1770,#1771,#1772,#1773,#1774,#1775,#1776,#1777,
#1778,#1779,#1780,#1781,#1782,#1783,#1784,#1785));
#2004=AXIS2_PLACEMENT_3D('',#2729,#2307,#2308);
#2005=AXIS2_PLACEMENT_3D('',#2730,#2309,#2310);
#2006=AXIS2_PLACEMENT_3D('',#2866,#2312,#2313);
#2007=AXIS2_PLACEMENT_3D('',#2964,#2314,#2315);
#2008=AXIS2_PLACEMENT_3D('',#3173,#2317,#2318);
#2009=AXIS2_PLACEMENT_3D('',#3541,#2320,#2321);
#2010=AXIS2_PLACEMENT_3D('',#3926,#2323,#2324);
#2011=AXIS2_PLACEMENT_3D('',#4291,#2326,#2327);
#2012=AXIS2_PLACEMENT_3D('',#4658,#2329,#2330);
#2013=AXIS2_PLACEMENT_3D('',#5033,#2332,#2333);
#2014=AXIS2_PLACEMENT_3D('',#5400,#2335,#2336);
#2015=AXIS2_PLACEMENT_3D('',#5769,#2338,#2339);
#2016=AXIS2_PLACEMENT_3D('',#6146,#2341,#2342);
#2017=AXIS2_PLACEMENT_3D('',#6511,#2344,#2345);
#2018=AXIS2_PLACEMENT_3D('',#6521,#2346,#2347);
#2019=AXIS2_PLACEMENT_3D('',#6991,#2348,#2349);
#2020=AXIS2_PLACEMENT_3D('',#7310,#2350,#2351);
#2021=AXIS2_PLACEMENT_3D('',#7467,#2352,#2353);
#2022=AXIS2_PLACEMENT_3D('',#8559,#2354,#2355);
#2023=AXIS2_PLACEMENT_3D('',#8561,#2356,#2357);
#2024=AXIS2_PLACEMENT_3D('',#8562,#2358,#2359);
#2025=AXIS2_PLACEMENT_3D('',#8563,#2360,#2361);
#2026=AXIS2_PLACEMENT_3D('',#8565,#2362,#2363);
#2027=AXIS2_PLACEMENT_3D('',#8566,#2364,#2365);
#2028=AXIS2_PLACEMENT_3D('',#8568,#2366,#2367);
#2029=AXIS2_PLACEMENT_3D('',#8570,#2369,#2370);
#2030=AXIS2_PLACEMENT_3D('',#8573,#2372,#2373);
#2031=AXIS2_PLACEMENT_3D('',#8574,#2374,#2375);
#2032=AXIS2_PLACEMENT_3D('',#8576,#2376,#2377);
#2033=AXIS2_PLACEMENT_3D('',#8578,#2379,#2380);
#2034=AXIS2_PLACEMENT_3D('',#8580,#2381,#2382);
#2035=AXIS2_PLACEMENT_3D('',#8581,#2383,#2384);
#2036=AXIS2_PLACEMENT_3D('',#8583,#2385,#2386);
#2037=AXIS2_PLACEMENT_3D('',#8585,#2388,#2389);
#2038=AXIS2_PLACEMENT_3D('',#8587,#2390,#2391);
#2039=AXIS2_PLACEMENT_3D('',#8588,#2392,#2393);
#2040=AXIS2_PLACEMENT_3D('',#8589,#2394,#2395);
#2041=AXIS2_PLACEMENT_3D('',#8591,#2396,#2397);
#2042=AXIS2_PLACEMENT_3D('',#8592,#2398,#2399);
#2043=AXIS2_PLACEMENT_3D('',#8594,#2400,#2401);
#2044=AXIS2_PLACEMENT_3D('',#8596,#2403,#2404);
#2045=AXIS2_PLACEMENT_3D('',#8598,#2405,#2406);
#2046=AXIS2_PLACEMENT_3D('',#8599,#2407,#2408);
#2307=DIRECTION('axis',(0.,0.,1.));
#2308=DIRECTION('refdir',(1.,0.,0.));
#2309=DIRECTION('center_axis',(0.,0.,1.));
#2310=DIRECTION('ref_axis',(0.839955785831598,-0.542654842278241,0.));
#2311=DIRECTION('',(0.,0.,-1.));
#2312=DIRECTION('center_axis',(0.,0.,-1.));
#2313=DIRECTION('ref_axis',(1.,5.80632514073727E-14,0.));
#2314=DIRECTION('center_axis',(0.,0.,1.));
#2315=DIRECTION('ref_axis',(0.839955785831598,-0.542654842278241,0.));
#2316=DIRECTION('',(0.,0.,-1.));
#2317=DIRECTION('center_axis',(0.,0.,1.));
#2318=DIRECTION('ref_axis',(0.839955785831598,-0.542654842278241,0.));
#2319=DIRECTION('',(0.,0.,-1.));
#2320=DIRECTION('center_axis',(0.,0.,1.));
#2321=DIRECTION('ref_axis',(0.839955785831598,-0.542654842278241,0.));
#2322=DIRECTION('',(0.,0.,-1.));
#2323=DIRECTION('center_axis',(0.,0.,1.));
#2324=DIRECTION('ref_axis',(0.839955785831598,-0.542654842278241,0.));
#2325=DIRECTION('',(0.,0.,-1.));
#2326=DIRECTION('center_axis',(0.,0.,1.));
#2327=DIRECTION('ref_axis',(0.839955785831598,-0.542654842278241,0.));
#2328=DIRECTION('',(0.,0.,-1.));
#2329=DIRECTION('center_axis',(0.,0.,1.));
#2330=DIRECTION('ref_axis',(0.839955785831598,-0.542654842278241,0.));
#2331=DIRECTION('',(0.,0.,-1.));
#2332=DIRECTION('center_axis',(0.,0.,1.));
#2333=DIRECTION('ref_axis',(0.839955785831598,-0.542654842278241,0.));
#2334=DIRECTION('',(0.,0.,-1.));
#2335=DIRECTION('center_axis',(0.,0.,1.));
#2336=DIRECTION('ref_axis',(0.839955785831598,-0.542654842278241,0.));
#2337=DIRECTION('',(0.,0.,-1.));
#2338=DIRECTION('center_axis',(0.,0.,1.));
#2339=DIRECTION('ref_axis',(0.839955785831598,-0.542654842278241,0.));
#2340=DIRECTION('',(0.,0.,-1.));
#2341=DIRECTION('center_axis',(0.,0.,1.));
#2342=DIRECTION('ref_axis',(0.839955785831598,-0.542654842278241,0.));
#2343=DIRECTION('',(0.,0.,-1.));
#2344=DIRECTION('center_axis',(0.,0.,1.));
#2345=DIRECTION('ref_axis',(1.,0.,0.));
#2346=DIRECTION('center_axis',(0.,0.,1.));
#2347=DIRECTION('ref_axis',(1.,0.,0.));
#2348=DIRECTION('center_axis',(0.,0.,1.));
#2349=DIRECTION('ref_axis',(1.,0.,0.));
#2350=DIRECTION('center_axis',(0.,0.,1.));
#2351=DIRECTION('ref_axis',(0.839955785831598,-0.542654842278241,0.));
#2352=DIRECTION('center_axis',(0.,0.,1.));
#2353=DIRECTION('ref_axis',(1.,5.80632514073727E-14,0.));
#2354=DIRECTION('center_axis',(0.,0.,1.));
#2355=DIRECTION('ref_axis',(1.,0.,0.));
#2356=DIRECTION('center_axis',(0.,0.,1.));
#2357=DIRECTION('ref_axis',(1.,0.,0.));
#2358=DIRECTION('center_axis',(0.,0.,-1.));
#2359=DIRECTION('ref_axis',(-1.,0.,0.));
#2360=DIRECTION('center_axis',(0.,0.,-1.));
#2361=DIRECTION('ref_axis',(-1.,0.,0.));
#2362=DIRECTION('center_axis',(0.,0.,1.));
#2363=DIRECTION('ref_axis',(1.,0.,0.));
#2364=DIRECTION('center_axis',(0.,0.,1.));
#2365=DIRECTION('ref_axis',(1.,0.,0.));
#2366=DIRECTION('center_axis',(0.,0.,1.));
#2367=DIRECTION('ref_axis',(1.,0.,0.));
#2368=DIRECTION('',(0.,0.,-1.));
#2369=DIRECTION('center_axis',(0.,0.,-1.));
#2370=DIRECTION('ref_axis',(1.,0.,0.));
#2371=DIRECTION('',(0.890347471651363,-1.09036118128678E-16,0.455281648788994));
#2372=DIRECTION('center_axis',(0.,0.,1.));
#2373=DIRECTION('ref_axis',(1.,0.,0.));
#2374=DIRECTION('center_axis',(0.,0.,1.));
#2375=DIRECTION('ref_axis',(1.,0.,0.));
#2376=DIRECTION('center_axis',(0.,0.,1.));
#2377=DIRECTION('ref_axis',(1.,0.,0.));
#2378=DIRECTION('',(0.,0.,-1.));
#2379=DIRECTION('center_axis',(0.,0.,-1.));
#2380=DIRECTION('ref_axis',(-1.,0.,0.));
#2381=DIRECTION('center_axis',(0.,0.,1.));
#2382=DIRECTION('ref_axis',(1.,0.,0.));
#2383=DIRECTION('center_axis',(0.,0.,1.));
#2384=DIRECTION('ref_axis',(1.,0.,0.));
#2385=DIRECTION('center_axis',(0.,0.,1.));
#2386=DIRECTION('ref_axis',(1.,0.,0.));
#2387=DIRECTION('',(0.,0.,-1.));
#2388=DIRECTION('center_axis',(0.,0.,1.));
#2389=DIRECTION('ref_axis',(1.,0.,0.));
#2390=DIRECTION('center_axis',(0.,0.,1.));
#2391=DIRECTION('ref_axis',(1.,0.,0.));
#2392=DIRECTION('center_axis',(1.22464679914735E-16,-1.,0.));
#2393=DIRECTION('ref_axis',(-1.,-1.22464679914735E-16,0.));
#2394=DIRECTION('center_axis',(0.,0.,1.));
#2395=DIRECTION('ref_axis',(1.,0.,0.));
#2396=DIRECTION('center_axis',(0.,0.,1.));
#2397=DIRECTION('ref_axis',(1.,0.,0.));
#2398=DIRECTION('center_axis',(0.,0.,1.));
#2399=DIRECTION('ref_axis',(1.,0.,0.));
#2400=DIRECTION('center_axis',(0.,0.,1.));
#2401=DIRECTION('ref_axis',(1.,0.,0.));
#2402=DIRECTION('',(0.,0.,1.));
#2403=DIRECTION('center_axis',(0.,0.,-1.));
#2404=DIRECTION('ref_axis',(-1.,0.,0.));
#2405=DIRECTION('center_axis',(0.,0.,1.));
#2406=DIRECTION('ref_axis',(1.,0.,0.));
#2407=DIRECTION('center_axis',(0.,0.,1.));
#2408=DIRECTION('ref_axis',(1.,0.,0.));
#2409=DIRECTION('',(0.,0.,1.));
#2729=CARTESIAN_POINT('',(0.,0.,0.));
#2730=CARTESIAN_POINT('Origin',(0.,0.,-1.10921167016993));
#2731=CARTESIAN_POINT('',(-1.14737960344596,0.741266514552076,0.454399650883576));
#2732=CARTESIAN_POINT('',(-1.14737960344596,0.741266514552078,0.335993717254283));
#2733=CARTESIAN_POINT('',(-1.14737960344596,0.741266514552077,-1.10921167016993));
#2734=CARTESIAN_POINT('',(-0.793737169645199,-1.11172717225209,4.50645841770791E-5));
#2735=CARTESIAN_POINT('Ctrl Pts',(-0.793737169645199,-1.11172717225209,
4.50645841774122E-5));
#2736=CARTESIAN_POINT('Ctrl Pts',(-0.751639642335613,-1.14178344236023,
0.0036785650865398));
#2737=CARTESIAN_POINT('Ctrl Pts',(-0.70774020306432,-1.16951088815659,0.00731206558890195));
#2738=CARTESIAN_POINT('Ctrl Pts',(-0.662329724218108,-1.19468629205209,
0.0109455660912643));
#2739=CARTESIAN_POINT('Ctrl Pts',(-0.616977478597539,-1.21982941165962,
0.0145744070863938));
#2740=CARTESIAN_POINT('Ctrl Pts',(-0.570118503567981,-1.24242669896913,
0.0182032480815238));
#2741=CARTESIAN_POINT('Ctrl Pts',(-0.52207319003199,-1.26229773993691,0.0218320890766532));
#2742=CARTESIAN_POINT('Ctrl Pts',(-0.474068808551045,-1.2821518518333,0.0254578384920127));
#2743=CARTESIAN_POINT('Ctrl Pts',(-0.424880595233744,-1.29928410516619,
0.0290835879073719));
#2744=CARTESIAN_POINT('Ctrl Pts',(-0.374851798930883,-1.31356085844482,
0.0327093373227314));
#2745=CARTESIAN_POINT('Ctrl Pts',(-0.324844095785002,-1.32783159235419,
0.0363335580484712));
#2746=CARTESIAN_POINT('Ctrl Pts',(-0.273997040078241,-1.33924906128545,
0.039957778774211));
#2747=CARTESIAN_POINT('Ctrl Pts',(-0.222669546158888,-1.34772930264701,
0.0435819994999509));
#2748=CARTESIAN_POINT('Ctrl Pts',(-0.171305410096995,-1.35621559796112,
0.0472088075176525));
#2749=CARTESIAN_POINT('Ctrl Pts',(-0.119460693090967,-1.36176037993733,
0.050835615535354));
#2750=CARTESIAN_POINT('Ctrl Pts',(-0.0675032006527575,-1.36433108808003,
0.0544624235530555));
#2751=CARTESIAN_POINT('Ctrl Pts',(-0.0155290642017095,-1.36690261972089,
0.0580903933789271));
#2752=CARTESIAN_POINT('Ctrl Pts',(0.0365573687379424,-1.36649817889123,
0.0617183632047989));
#2753=CARTESIAN_POINT('Ctrl Pts',(0.088388047322021,-1.36313739332857,0.0653463330306705));
#2754=CARTESIAN_POINT('Ctrl Pts',(0.140314932876691,-1.35977036954934,0.068981037014687));
#2755=CARTESIAN_POINT('Ctrl Pts',(0.191984568102908,-1.35343610419073,0.0726157409987032));
#2756=CARTESIAN_POINT('Ctrl Pts',(0.243035214301144,-1.34420604246879,0.0762504449827197));
#2757=CARTESIAN_POINT('Ctrl Pts',(0.286596093508279,-1.3363301460074,0.0793518925253544));
#2758=CARTESIAN_POINT('Ctrl Pts',(0.329706251292679,-1.32634675090387,0.0824533400679891));
#2759=CARTESIAN_POINT('Ctrl Pts',(0.372150158132393,-1.31432882483876,0.0855547876106237));
#2760=CARTESIAN_POINT('Ctrl Pts',(0.422553436740067,-1.30005721506368,0.0892378398133543));
#2761=CARTESIAN_POINT('Ctrl Pts',(0.472236728814164,-1.28285315030033,0.0929208920160846));
#2762=CARTESIAN_POINT('Ctrl Pts',(0.520836570594336,-1.26280848378982,0.0966039442188151));
#2763=CARTESIAN_POINT('Ctrl Pts',(0.569352750610994,-1.24279832299142,0.10028065626423));
#2764=CARTESIAN_POINT('Ctrl Pts',(0.61678869076564,-1.21995746573567,0.103957368309646));
#2765=CARTESIAN_POINT('Ctrl Pts',(0.662796534801183,-1.19442737470955,0.107634080355061));
#2766=CARTESIAN_POINT('Ctrl Pts',(0.708760648998604,-1.16892154969221,0.111307297735035));
#2767=CARTESIAN_POINT('Ctrl Pts',(0.753298890590591,-1.14073181236285,0.114980515115009));
#2768=CARTESIAN_POINT('Ctrl Pts',(0.796085668064992,-1.11004666978534,0.118653732494983));
#2769=CARTESIAN_POINT('Ctrl Pts',(0.838849036797168,-1.07937831511837,0.122324940249464));
#2770=CARTESIAN_POINT('Ctrl Pts',(0.879862407211625,-1.04621757228296,0.125996148003945));
#2771=CARTESIAN_POINT('Ctrl Pts',(0.918829042873192,-1.01079631477995,0.129667355758426));
#2772=CARTESIAN_POINT('Ctrl Pts',(0.957790077042176,-0.975380149117903,
0.133338035773145));
#2773=CARTESIAN_POINT('Ctrl Pts',(0.994704566209091,-0.937704474229589,
0.137008715787865));
#2774=CARTESIAN_POINT('Ctrl Pts',(1.02931060115345,-0.898039913563496,0.140679395802584));
#2775=CARTESIAN_POINT('Ctrl Pts',(1.06394993909219,-0.858337181848816,0.144353608283133));
#2776=CARTESIAN_POINT('Ctrl Pts',(1.09627603522514,-0.816642146342524,0.148027820763682));
#2777=CARTESIAN_POINT('Ctrl Pts',(1.12606657452244,-0.773259380637117,0.15170203324423));
#2778=CARTESIAN_POINT('Ctrl Pts',(1.15587257497474,-0.729854099472749,0.15537815262442));
#2779=CARTESIAN_POINT('Ctrl Pts',(1.18314012000445,-0.684759800914628,0.159054272004609));
#2780=CARTESIAN_POINT('Ctrl Pts',(1.20769149326283,-0.63830812081673,0.162730391384798));
#2781=CARTESIAN_POINT('Ctrl Pts',(1.23228776877378,-0.591771484775637,0.166413234056558));
#2782=CARTESIAN_POINT('Ctrl Pts',(1.254157732108,-0.543872997364555,0.170096076728318));
#2783=CARTESIAN_POINT('Ctrl Pts',(1.27317128162862,-0.494965541867454,0.173778919400078));
#2784=CARTESIAN_POINT('Ctrl Pts',(1.28377240174473,-0.467696892753009,0.175832310719237));
#2785=CARTESIAN_POINT('Ctrl Pts',(1.29348643851001,-0.440114891305328,0.177885702038397));
#2786=CARTESIAN_POINT('Ctrl Pts',(1.30229766419691,-0.412282419983284,0.179939093357556));
#2787=CARTESIAN_POINT('Ctrl Pts',(1.3180543625256,-0.362510927350304,0.183611075975687));
#2788=CARTESIAN_POINT('Ctrl Pts',(1.33098780187201,-0.311727064905966,0.187283058593818));
#2789=CARTESIAN_POINT('Ctrl Pts',(1.34097323626866,-0.260282115426988,0.190955041211949));
#2790=CARTESIAN_POINT('Ctrl Pts',(1.35094057822144,-0.208930378203374,0.194620370625344));
#2791=CARTESIAN_POINT('Ctrl Pts',(1.3579704104302,-0.156920454413018,0.198285700038739));
#2792=CARTESIAN_POINT('Ctrl Pts',(1.36198789621833,-0.104618213303267,0.201951029452135));
#2793=CARTESIAN_POINT('Ctrl Pts',(1.36600135074658,-0.0523684537546225,
0.205612680969411));
#2794=CARTESIAN_POINT('Ctrl Pts',(1.36700840358335,0.000172508177129028,
0.209274332486688));
#2795=CARTESIAN_POINT('Ctrl Pts',(1.36498569854959,0.0526311956457186,0.212935984003965));
#2796=CARTESIAN_POINT('Ctrl Pts',(1.36296419249614,0.105058787658907,0.216595465037629));
#2797=CARTESIAN_POINT('Ctrl Pts',(1.35791650798661,0.157403665011107,0.220254946071294));
#2798=CARTESIAN_POINT('Ctrl Pts',(1.34987137383988,0.209292317316323,0.223914427104958));
#2799=CARTESIAN_POINT('Ctrl Pts',(1.34182770485348,0.261171519785902,0.227573241682804));
#2800=CARTESIAN_POINT('Ctrl Pts',(1.33078775312727,0.312594130645045,0.231232056260649));
#2801=CARTESIAN_POINT('Ctrl Pts',(1.31683179740051,0.363194186840785,0.234890870838494));
#2802=CARTESIAN_POINT('Ctrl Pts',(1.30286281544566,0.413841472182751,0.238553100485446));
#2803=CARTESIAN_POINT('Ctrl Pts',(1.2859725378804,0.463664149814199,0.242215330132398));
#2804=CARTESIAN_POINT('Ctrl Pts',(1.26629142338985,0.512310483056241,0.24587755977935));
#2805=CARTESIAN_POINT('Ctrl Pts',(1.24660050841667,0.560981040411392,0.249541613084105));
#2806=CARTESIAN_POINT('Ctrl Pts',(1.22411621856117,0.608473599297943,0.25320566638886));
#2807=CARTESIAN_POINT('Ctrl Pts',(1.19901620077949,0.654458669641039,0.256869719693615));
#2808=CARTESIAN_POINT('Ctrl Pts',(1.17387005003326,0.700528258952944,0.260540507401615));
#2809=CARTESIAN_POINT('Ctrl Pts',(1.1460988579627,0.74508437064621,0.264211295109616));
#2810=CARTESIAN_POINT('Ctrl Pts',(1.11592426213602,0.787825514423194,0.267882082817616));
#2811=CARTESIAN_POINT('Ctrl Pts',(1.09827463386285,0.812825527810852,0.270029188246571));
#2812=CARTESIAN_POINT('Ctrl Pts',(1.0798035203546,0.837205186230783,0.272176293675525));
#2813=CARTESIAN_POINT('Ctrl Pts',(1.06056136792303,0.860909742580046,0.274323399104479));
#2814=CARTESIAN_POINT('Ctrl Pts',(1.02759784932718,0.901517755992458,0.278001581677153));
#2815=CARTESIAN_POINT('Ctrl Pts',(0.992229539636963,0.940315040623115,0.281679764249827));
#2816=CARTESIAN_POINT('Ctrl Pts',(0.954682800137662,0.977003966788935,0.285357946822501));
#2817=CARTESIAN_POINT('Ctrl Pts',(0.917202768032331,1.01362770959437,0.289029594554142));
#2818=CARTESIAN_POINT('Ctrl Pts',(0.877552365838462,1.04815015433973,0.292701242285782));
#2819=CARTESIAN_POINT('Ctrl Pts',(0.835997481287777,1.08030746145738,0.296372890017422));
#2820=CARTESIAN_POINT('Ctrl Pts',(0.794483456349179,1.11243314930551,0.300040927533232));
#2821=CARTESIAN_POINT('Ctrl Pts',(0.751069080026469,1.1421979789467,0.303708965049042));
#2822=CARTESIAN_POINT('Ctrl Pts',(0.706054797570703,1.16937702338784,0.307377002564852));
#2823=CARTESIAN_POINT('Ctrl Pts',(0.661066469187005,1.19654039709426,0.311042925185015));
#2824=CARTESIAN_POINT('Ctrl Pts',(0.614480521023724,1.22112066376083,0.314708847805177));
#2825=CARTESIAN_POINT('Ctrl Pts',(0.566625972166103,1.24293644554612,0.31837477042534));
#2826=CARTESIAN_POINT('Ctrl Pts',(0.51877955420565,1.26474852064349,0.322040070173893));
#2827=CARTESIAN_POINT('Ctrl Pts',(0.469665451480756,1.2837968219978,0.325705369922446));
#2828=CARTESIAN_POINT('Ctrl Pts',(0.419634648089527,1.29994721512944,0.329370669670999));
#2829=CARTESIAN_POINT('Ctrl Pts',(0.369557020317372,1.31611272359221,0.33303939981403));
#2830=CARTESIAN_POINT('Ctrl Pts',(0.318561489935458,1.32937474308056,0.336708129957061));
#2831=CARTESIAN_POINT('Ctrl Pts',(0.267014692991089,1.33964889195896,0.340376860100091));
#2832=CARTESIAN_POINT('Ctrl Pts',(0.215442020405072,1.3499281982906,0.344047431885127));
#2833=CARTESIAN_POINT('Ctrl Pts',(0.163318061560322,1.35721657132989,0.347718003670162));
#2834=CARTESIAN_POINT('Ctrl Pts',(0.111016790111677,1.36148127872303,0.351388575455198));
#2835=CARTESIAN_POINT('Ctrl Pts',(0.0586202528237817,1.36575375420512,0.355065833121703));
#2836=CARTESIAN_POINT('Ctrl Pts',(0.00604629471542903,1.36699155515212,
0.358743090788209));
#2837=CARTESIAN_POINT('Ctrl Pts',(-0.046330323551458,1.36521408618561,0.362420348454715));
#2838=CARTESIAN_POINT('Ctrl Pts',(-0.0761814151132315,1.36420105039554,
0.364516133920278));
#2839=CARTESIAN_POINT('Ctrl Pts',(-0.10596847410221,1.36220954607447,0.366611919385841));
#2840=CARTESIAN_POINT('Ctrl Pts',(-0.135623318953185,1.35925064478783,0.368707704851404));
#2841=CARTESIAN_POINT('Ctrl Pts',(-0.187642818708641,1.35406024283056,0.372384058987169));
#2842=CARTESIAN_POINT('Ctrl Pts',(-0.23947307154391,1.34586842646892,0.376060413122934));
#2843=CARTESIAN_POINT('Ctrl Pts',(-0.290741487431388,1.33470048605902,0.379736767258699));
#2844=CARTESIAN_POINT('Ctrl Pts',(-0.341937330532648,1.32354835437926,0.383407917347135));
#2845=CARTESIAN_POINT('Ctrl Pts',(-0.392572392128989,1.30942855401121,0.387079067435571));
#2846=CARTESIAN_POINT('Ctrl Pts',(-0.442280156726634,1.29241799080865,0.390750217524007));
#2847=CARTESIAN_POINT('Ctrl Pts',(-0.491937793461506,1.27542458193167,0.394417665436146));
#2848=CARTESIAN_POINT('Ctrl Pts',(-0.540669480756072,1.25554635847026,0.398085113348285));
#2849=CARTESIAN_POINT('Ctrl Pts',(-0.588122222418167,1.23291047992055,0.401752561260424));
#2850=CARTESIAN_POINT('Ctrl Pts',(-0.63554642529022,1.21028821492746,0.405417803514423));
#2851=CARTESIAN_POINT('Ctrl Pts',(-0.681692724534928,1.18491181371754,0.409083045768422));
#2852=CARTESIAN_POINT('Ctrl Pts',(-0.72622880467367,1.15695623221549,0.41274828802242));
#2853=CARTESIAN_POINT('Ctrl Pts',(-0.770780158134974,1.12899106355146,0.41641478724441));
#2854=CARTESIAN_POINT('Ctrl Pts',(-0.813719727493361,1.09844522153416,0.4200812864664));
#2855=CARTESIAN_POINT('Ctrl Pts',(-0.854742110151995,1.06553832644955,0.42374778568839));
#2856=CARTESIAN_POINT('Ctrl Pts',(-0.895769796412266,1.03262717697865,0.427414758935778));
#2857=CARTESIAN_POINT('Ctrl Pts',(-0.934879393335804,0.997354714589682,
0.431081732183166));
#2858=CARTESIAN_POINT('Ctrl Pts',(-0.971799154517271,0.959980418175037,
0.434748705430555));
#2859=CARTESIAN_POINT('Ctrl Pts',(-1.00877133198009,0.922553060159411,0.438420884808625));
#2860=CARTESIAN_POINT('Ctrl Pts',(-1.04354709922193,0.88301830310746,0.442093064186694));
#2861=CARTESIAN_POINT('Ctrl Pts',(-1.07589314086733,0.841670927046092,0.445765243564764));
#2862=CARTESIAN_POINT('Ctrl Pts',(-1.10124492518607,0.809264187094878,0.448643379337701));
#2863=CARTESIAN_POINT('Ctrl Pts',(-1.12510489750646,0.775744725514016,0.451521515110639));
#2864=CARTESIAN_POINT('Ctrl Pts',(-1.14737960344596,0.741266514552077,0.454399650883576));
#2865=CARTESIAN_POINT('',(0.79376424639115,-1.11170783983522,0.));
#2866=CARTESIAN_POINT('Origin',(0.,0.,0.));
#2867=CARTESIAN_POINT('Ctrl Pts',(0.793764246391152,-1.11170783983522,-4.44089209850063E-16));
#2868=CARTESIAN_POINT('Ctrl Pts',(0.839547624132048,-1.07901830844257,0.00393267940612148));
#2869=CARTESIAN_POINT('Ctrl Pts',(0.88334665467536,-1.04346915171738,0.00786535881224336));
#2870=CARTESIAN_POINT('Ctrl Pts',(0.924804470391501,-1.00533212996696,0.0117980382183653));
#2871=CARTESIAN_POINT('Ctrl Pts',(0.964439482492348,-0.968871904254196,
0.0155578068689291));
#2872=CARTESIAN_POINT('Ctrl Pts',(1.00193447662138,-0.930047025035295,0.0193175755194929));
#2873=CARTESIAN_POINT('Ctrl Pts',(1.03701191980893,-0.889135691654659,0.0230773441700567));
#2874=CARTESIAN_POINT('Ctrl Pts',(1.07208184091284,-0.848233131389829,0.0268363065676081));
#2875=CARTESIAN_POINT('Ctrl Pts',(1.10473491471357,-0.805245385353481,0.0305952689651596));
#2876=CARTESIAN_POINT('Ctrl Pts',(1.13473279690904,-0.76048502918794,0.034354231362711));
#2877=CARTESIAN_POINT('Ctrl Pts',(1.16473383991346,-0.715719956724978,0.0381135898336224));
#2878=CARTESIAN_POINT('Ctrl Pts',(1.19207885790094,-0.669182319737291,0.0418729483045338));
#2879=CARTESIAN_POINT('Ctrl Pts',(1.21657301646592,-0.621213405849402,0.0456323067754452));
#2880=CARTESIAN_POINT('Ctrl Pts',(1.24107759069276,-0.573224094119078,0.0493932638400193));
#2881=CARTESIAN_POINT('Ctrl Pts',(1.26272867202181,-0.52380274333007,0.0531542209045935));
#2882=CARTESIAN_POINT('Ctrl Pts',(1.28137842533247,-0.473313142742192,0.0569151779691677));
#2883=CARTESIAN_POINT('Ctrl Pts',(1.30005661343255,-0.422746561985347,0.0606818692662755));
#2884=CARTESIAN_POINT('Ctrl Pts',(1.31572416930455,-0.371108952170183,0.0644485605633832));
#2885=CARTESIAN_POINT('Ctrl Pts',(1.32828263625582,-0.318780862382442,0.068215251860491));
#2886=CARTESIAN_POINT('Ctrl Pts',(1.34085194875564,-0.266407581820977,0.0719851960891464));
#2887=CARTESIAN_POINT('Ctrl Pts',(1.35030673650858,-0.213343126544116,0.0757551403178016));
#2888=CARTESIAN_POINT('Ctrl Pts',(1.35659995290541,-0.159976772617293,0.079525084546457));
#2889=CARTESIAN_POINT('Ctrl Pts',(1.36290556532907,-0.106505300621519,0.0833024546010909));
#2890=CARTESIAN_POINT('Ctrl Pts',(1.3660371439318,-0.0527312425025266,0.087079824655725));
#2891=CARTESIAN_POINT('Ctrl Pts',(1.36599966715517,0.000953588993072139,
0.0908571947103589));
#2892=CARTESIAN_POINT('Ctrl Pts',(1.36598800253573,0.0176629537032467,0.0920328983892155));
#2893=CARTESIAN_POINT('Ctrl Pts',(1.36566971183152,0.0343637026982444,0.0932086020680719));
#2894=CARTESIAN_POINT('Ctrl Pts',(1.36504596856042,0.0510441349907324,0.0943843057469285));
#2895=CARTESIAN_POINT('Ctrl Pts',(1.36311507457556,0.102680998858287,0.0980238787357558));
#2896=CARTESIAN_POINT('Ctrl Pts',(1.35824494995059,0.154340769049966,0.101663451724583));
#2897=CARTESIAN_POINT('Ctrl Pts',(1.35043002218929,0.205656886998317,0.10530302471341));
#2898=CARTESIAN_POINT('Ctrl Pts',(1.34263095596918,0.256868851364768,0.108935210655466));
#2899=CARTESIAN_POINT('Ctrl Pts',(1.33189901875094,0.307738009171175,0.112567396597523));
#2900=CARTESIAN_POINT('Ctrl Pts',(1.31828056759875,0.357899909320372,0.116199582539579));
#2901=CARTESIAN_POINT('Ctrl Pts',(1.3046775273593,0.408005045256218,0.119827658227097));
#2902=CARTESIAN_POINT('Ctrl Pts',(1.28819457884667,0.457403980420958,0.123455733914616));
#2903=CARTESIAN_POINT('Ctrl Pts',(1.2689292619985,0.505741562503954,0.127083809602134));
#2904=CARTESIAN_POINT('Ctrl Pts',(1.24967747407379,0.554045199884493,0.130709337500863));
#2905=CARTESIAN_POINT('Ctrl Pts',(1.22764738884494,0.601288450906808,0.134334865399592));
#2906=CARTESIAN_POINT('Ctrl Pts',(1.20298583332618,0.647132973056167,0.137960393298322));
#2907=CARTESIAN_POINT('Ctrl Pts',(1.17833100864943,0.692964982927643,0.141584931687064));
#2908=CARTESIAN_POINT('Ctrl Pts',(1.15104639821546,0.737398537781149,0.145209470075805));
#2909=CARTESIAN_POINT('Ctrl Pts',(1.12132509524405,0.780119241382957,0.148834008464547));
#2910=CARTESIAN_POINT('Ctrl Pts',(1.09157774953995,0.822877378197753,0.152461722786877));
#2911=CARTESIAN_POINT('Ctrl Pts',(1.05938976027312,0.863919213687103,0.156089437109208));
#2912=CARTESIAN_POINT('Ctrl Pts',(1.02499693519614,0.902960288627645,0.159717151431538));
#2913=CARTESIAN_POINT('Ctrl Pts',(0.990588653942779,0.942018908673566,0.163346496052987));
#2914=CARTESIAN_POINT('Ctrl Pts',(0.953973950157304,0.979074586295714,0.166975840674436));
#2915=CARTESIAN_POINT('Ctrl Pts',(0.915425782563449,1.01387949807563,0.170605185295885));
#2916=CARTESIAN_POINT('Ctrl Pts',(0.876805015732143,1.04874995927625,0.174241365200783));
#2917=CARTESIAN_POINT('Ctrl Pts',(0.836243944415294,1.08136084783297,0.177877545105682));
#2918=CARTESIAN_POINT('Ctrl Pts',(0.794047693405854,1.11150540286444,0.18151372501058));
#2919=CARTESIAN_POINT('Ctrl Pts',(0.765984449461231,1.13155348726087,0.183932020505004));
#2920=CARTESIAN_POINT('Ctrl Pts',(0.737198571536647,1.15051157425271,0.186350315999428));
#2921=CARTESIAN_POINT('Ctrl Pts',(0.707785740498224,1.16833015263126,0.188768611493852));
#2922=CARTESIAN_POINT('Ctrl Pts',(0.662990831832107,1.19546734285903,0.192451607042933));
#2923=CARTESIAN_POINT('Ctrl Pts',(0.616540497489185,1.22008065146032,0.196134602592014));
#2924=CARTESIAN_POINT('Ctrl Pts',(0.568749283224068,1.24196628490153,0.199817598141095));
#2925=CARTESIAN_POINT('Ctrl Pts',(0.521042871503823,1.26381308364392,0.203494058443058));
#2926=CARTESIAN_POINT('Ctrl Pts',(0.472000783491401,1.28294159078561,0.20717051874502));
#2927=CARTESIAN_POINT('Ctrl Pts',(0.421963296418883,1.29919320213558,0.210846979046983));
#2928=CARTESIAN_POINT('Ctrl Pts',(0.371975013053495,1.31542883267653,0.214519824149891));
#2929=CARTESIAN_POINT('Ctrl Pts',(0.320993775526985,1.32879300680675,0.218192669252799));
#2930=CARTESIAN_POINT('Ctrl Pts',(0.269379203383589,1.33917543465538,0.221865514355707));
#2931=CARTESIAN_POINT('Ctrl Pts',(0.217794559408266,1.34955184236217,0.22553622979792));
#2932=CARTESIAN_POINT('Ctrl Pts',(0.165577831743621,1.35694982551169,0.229206945240134));
#2933=CARTESIAN_POINT('Ctrl Pts',(0.113100803751644,1.36130973998967,0.232877660682347));
#2934=CARTESIAN_POINT('Ctrl Pts',(0.0606330314821481,1.36566888548053,0.236547728696062));
#2935=CARTESIAN_POINT('Ctrl Pts',(0.00790558248072019,1.36699098290877,
0.240217796709777));
#2936=CARTESIAN_POINT('Ctrl Pts',(-0.0447050425036199,1.36526827370109,
0.243887864723492));
#2937=CARTESIAN_POINT('Ctrl Pts',(-0.0973637415889933,1.36354399033045,
0.247561286341551));
#2938=CARTESIAN_POINT('Ctrl Pts',(-0.149904868266707,1.35876936192454,0.251234707959611));
#2939=CARTESIAN_POINT('Ctrl Pts',(-0.201953983831821,1.35098874474011,0.25490812957767));
#2940=CARTESIAN_POINT('Ctrl Pts',(-0.254028665796359,1.34320430573537,0.258583355571525));
#2941=CARTESIAN_POINT('Ctrl Pts',(-0.305610331150917,1.33241104487945,0.26225858156538));
#2942=CARTESIAN_POINT('Ctrl Pts',(-0.356335033438439,1.31870441871726,0.265933807559235));
#2943=CARTESIAN_POINT('Ctrl Pts',(-0.407150432714315,1.30497328477765,0.26961560494561));
#2944=CARTESIAN_POINT('Ctrl Pts',(-0.457105301754811,1.28831855360352,0.273297402331984));
#2945=CARTESIAN_POINT('Ctrl Pts',(-0.505852515199843,1.26888503532274,0.276979199718359));
#2946=CARTESIAN_POINT('Ctrl Pts',(-0.533099309290899,1.25802285400733,0.279037105559165));
#2947=CARTESIAN_POINT('Ctrl Pts',(-0.559969194260518,1.24629339880498,0.281095011399971));
#2948=CARTESIAN_POINT('Ctrl Pts',(-0.586404959992857,1.23372818031193,0.283152917240777));
#2949=CARTESIAN_POINT('Ctrl Pts',(-0.633713951483963,1.21124168149852,0.2868357101244));
#2950=CARTESIAN_POINT('Ctrl Pts',(-0.67982354190126,1.18598452557416,0.290518503008023));
#2951=CARTESIAN_POINT('Ctrl Pts',(-0.724390781783443,1.15810793765831,0.294201295891646));
#2952=CARTESIAN_POINT('Ctrl Pts',(-0.768884467149523,1.13027735772814,0.297878010632463));
#2953=CARTESIAN_POINT('Ctrl Pts',(-0.811840401668115,1.09983620262544,0.30155472537328));
#2954=CARTESIAN_POINT('Ctrl Pts',(-0.852939234293832,1.06698203480764,0.305231440114097));
#2955=CARTESIAN_POINT('Ctrl Pts',(-0.89399780078697,1.03416005550208,0.308904552633786));
#2956=CARTESIAN_POINT('Ctrl Pts',(-0.933202455006571,0.998930080160931,
0.312577665153476));
#2957=CARTESIAN_POINT('Ctrl Pts',(-0.970263678560064,0.961532315664478,
0.316250777673165));
#2958=CARTESIAN_POINT('Ctrl Pts',(-1.0073116793192,0.924147894034291,0.319922579690749));
#2959=CARTESIAN_POINT('Ctrl Pts',(-1.04221738145856,0.88459758727491,0.323594381708332));
#2960=CARTESIAN_POINT('Ctrl Pts',(-1.07472681225964,0.843159699588541,0.327266183725916));
#2961=CARTESIAN_POINT('Ctrl Pts',(-1.10048411489069,0.810328358429109,0.330175361568705));
#2962=CARTESIAN_POINT('Ctrl Pts',(-1.12473780846742,0.776312929348634,0.333084539411494));
#2963=CARTESIAN_POINT('Ctrl Pts',(-1.14737960344596,0.741266514552078,0.335993717254284));
#2964=CARTESIAN_POINT('Origin',(0.,0.,-1.10921167016993));
#2965=CARTESIAN_POINT('',(-1.14737959575237,0.741266526460718,1.05477007217181));
#2966=CARTESIAN_POINT('',(-1.14885860607148,0.742234466194312,0.935969339060826));
#2967=CARTESIAN_POINT('',(-1.14737960344596,0.741266514552077,-1.10921167016993));
#2968=CARTESIAN_POINT('',(-1.36599999643447,9.5954861566352E-5,0.509307464475418));
#2969=CARTESIAN_POINT('Ctrl Pts',(-1.14737959575237,0.741266526460718,1.05477007217181));
#2970=CARTESIAN_POINT('Ctrl Pts',(-1.12470332541913,0.776366303611523,1.05162393080854));
#2971=CARTESIAN_POINT('Ctrl Pts',(-1.10042580611056,0.810411025106853,1.04845578440971));
#2972=CARTESIAN_POINT('Ctrl Pts',(-1.03892990164795,0.888776365247056,1.04093215917889));
#2973=CARTESIAN_POINT('Ctrl Pts',(-1.00038150994656,0.931953319766969,1.036593838144));
#2974=CARTESIAN_POINT('Ctrl Pts',(-0.95058246780969,0.9810686879414,1.03152583234021));
#2975=CARTESIAN_POINT('Ctrl Pts',(-0.941842921853207,0.989461841099333,
1.03065475304995));
#2976=CARTESIAN_POINT('Ctrl Pts',(-0.927677032072904,1.00270847417346,1.02927342027029));
#2977=CARTESIAN_POINT('Ctrl Pts',(-0.922321788946925,1.00763658328123,1.02875803347421));
#2978=CARTESIAN_POINT('Ctrl Pts',(-0.91170432487129,1.01725162781242,1.02774996021258));
#2979=CARTESIAN_POINT('Ctrl Pts',(-0.906444773601099,1.02194105831177,1.02725711876946));
#2980=CARTESIAN_POINT('Ctrl Pts',(-0.892866218962798,1.03386042785621,1.02600065843099));
#2981=CARTESIAN_POINT('Ctrl Pts',(-0.884495350603236,1.04103096191356,1.02524114680688));
#2982=CARTESIAN_POINT('Ctrl Pts',(-0.846162385274117,1.07307099156654,1.02182578918361));
#2983=CARTESIAN_POINT('Ctrl Pts',(-0.815229419698272,1.09675600028045,1.01924041416139));
#2984=CARTESIAN_POINT('Ctrl Pts',(-0.700672728752013,1.17694174373649,1.01009118010413));
#2985=CARTESIAN_POINT('Ctrl Pts',(-0.611866859053799,1.22546088975011,1.00374688719229));
#2986=CARTESIAN_POINT('Ctrl Pts',(-0.480888515164538,1.27920179085412,0.994464353421084));
#2987=CARTESIAN_POINT('Ctrl Pts',(-0.442583914750704,1.29295397847068,0.991761330429912));
#2988=CARTESIAN_POINT('Ctrl Pts',(-0.387767925705394,1.30991261058457,0.987872438347571));
#2989=CARTESIAN_POINT('Ctrl Pts',(-0.371721903840006,1.31455612165221,0.986731743680233));
#2990=CARTESIAN_POINT('Ctrl Pts',(-0.343899394152305,1.32205746687706,0.984747683184836));
#2991=CARTESIAN_POINT('Ctrl Pts',(-0.332162359061671,1.32505505163825,0.983908828809258));
#2992=CARTESIAN_POINT('Ctrl Pts',(-0.307928085993631,1.33090216141196,0.982172160868193));
#2993=CARTESIAN_POINT('Ctrl Pts',(-0.295427540803823,1.33373266351745,0.98127384124049));
#2994=CARTESIAN_POINT('Ctrl Pts',(-0.262901436295729,1.3406178631847,0.9789290485056));
#2995=CARTESIAN_POINT('Ctrl Pts',(-0.242822091407495,1.34439978147679,0.977474284569879));
#2996=CARTESIAN_POINT('Ctrl Pts',(-0.139554868590767,1.36146117003613,0.969951361165812));
#2997=CARTESIAN_POINT('Ctrl Pts',(-0.0553648351471,1.36747302604255,0.963665894653975));
#2998=CARTESIAN_POINT('Ctrl Pts',(0.111119535220584,1.36395865656298,0.951084274612596));
#2999=CARTESIAN_POINT('Ctrl Pts',(0.19309051307315,1.3547873754692,0.944819709072733));
#3000=CARTESIAN_POINT('Ctrl Pts',(0.28748088634379,1.335480213202,0.93780658799867));
#3001=CARTESIAN_POINT('Ctrl Pts',(0.301176559409139,1.33245839655782,0.936794395007166));
#3002=CARTESIAN_POINT('Ctrl Pts',(0.322375046547035,1.32743758704017,0.935238503318165));
#3003=CARTESIAN_POINT('Ctrl Pts',(0.329911033883498,1.325584752239,0.934687527724469));
#3004=CARTESIAN_POINT('Ctrl Pts',(0.344027808549043,1.32198608618546,0.933659947133613));
#3005=CARTESIAN_POINT('Ctrl Pts',(0.350611650371849,1.32025520939486,0.933182624483118));
#3006=CARTESIAN_POINT('Ctrl Pts',(0.366536391978728,1.31594110289744,0.932032323226874));
#3007=CARTESIAN_POINT('Ctrl Pts',(0.375863215836806,1.31330756857618,0.931362112621733));
#3008=CARTESIAN_POINT('Ctrl Pts',(0.4101698316904,1.30322528353338,0.928907133783455));
#3009=CARTESIAN_POINT('Ctrl Pts',(0.434964551314517,1.2951607918785,0.92715293432231));
#3010=CARTESIAN_POINT('Ctrl Pts',(0.501703594658899,1.27132076434657,0.922447988664138));
#3011=CARTESIAN_POINT('Ctrl Pts',(0.543128078391972,1.25418316138734,0.919545531620396));
#3012=CARTESIAN_POINT('Ctrl Pts',(0.67692349798588,1.19095598905223,0.910010148093891));
#3013=CARTESIAN_POINT('Ctrl Pts',(0.76490498143937,1.13645048756277,0.903448197219732));
#3014=CARTESIAN_POINT('Ctrl Pts',(0.862453880801481,1.0595155759424,0.895098778056297));
#3015=CARTESIAN_POINT('Ctrl Pts',(0.878692987030042,1.04608723720592,0.893669750023547));
#3016=CARTESIAN_POINT('Ctrl Pts',(0.904398027030114,1.02381044135106,0.891338862302064));
#3017=CARTESIAN_POINT('Ctrl Pts',(0.914060371333503,1.01519319783945,0.890446285170131));
#3018=CARTESIAN_POINT('Ctrl Pts',(0.932482945346784,0.998287014819886,0.888711387356815));
#3019=CARTESIAN_POINT('Ctrl Pts',(0.941258783908613,0.99001681431853,0.887869894260922));
#3020=CARTESIAN_POINT('Ctrl Pts',(0.961670079256935,0.970264830753224,0.88587606079604));
#3021=CARTESIAN_POINT('Ctrl Pts',(0.973210967858884,0.958688455154802,0.884719748248485));
#3022=CARTESIAN_POINT('Ctrl Pts',(1.01298478530772,0.917333917895172,0.880629327979428));
#3023=CARTESIAN_POINT('Ctrl Pts',(1.0400788234312,0.886495982379196,0.877649380150823));
#3024=CARTESIAN_POINT('Ctrl Pts',(1.10901688399886,0.800514488758387,0.869520985454619));
#3025=CARTESIAN_POINT('Ctrl Pts',(1.14812564786238,0.743335590055816,0.864294449373019));
#3026=CARTESIAN_POINT('Ctrl Pts',(1.21703628858013,0.624082920059139,0.853876519721248));
#3027=CARTESIAN_POINT('Ctrl Pts',(1.24682541577135,0.562214445751434,0.848700692153322));
#3028=CARTESIAN_POINT('Ctrl Pts',(1.27634768520716,0.48687261286958,0.842834304629746));
#3029=CARTESIAN_POINT('Ctrl Pts',(1.28069515075193,0.475319169373216,0.841946491388744));
#3030=CARTESIAN_POINT('Ctrl Pts',(1.28737252223326,0.456816877620064,0.840545078818139));
#3031=CARTESIAN_POINT('Ctrl Pts',(1.28980404402359,0.44990577361557,0.840026096186995));
#3032=CARTESIAN_POINT('Ctrl Pts',(1.29445323251035,0.436343868811065,0.839016875223297));
#3033=CARTESIAN_POINT('Ctrl Pts',(1.29667550116893,0.42969499775443,0.838526417961329));
#3034=CARTESIAN_POINT('Ctrl Pts',(1.30220466697686,0.412718538258572,0.837284440516891));
#3035=CARTESIAN_POINT('Ctrl Pts',(1.30544004559378,0.402367857395817,0.836536841081613));
#3036=CARTESIAN_POINT('Ctrl Pts',(1.31911346517483,0.356721625139771,0.833277645772659));
#3037=CARTESIAN_POINT('Ctrl Pts',(1.32824671708704,0.321048011076773,0.830828823665884));
#3038=CARTESIAN_POINT('Ctrl Pts',(1.35407831099748,0.199982698284748,0.822712975968081));
#3039=CARTESIAN_POINT('Ctrl Pts',(1.36406300638835,0.11337803042746,0.817216025408476));
#3040=CARTESIAN_POINT('Ctrl Pts',(1.36678616203293,-0.0274510004467692,
0.808069656315618));
#3041=CARTESIAN_POINT('Ctrl Pts',(1.36464064212542,-0.0813199155979687,
0.804524732361915));
#3042=CARTESIAN_POINT('Ctrl Pts',(1.35753562277348,-0.152904362041534,0.799663494086752));
#3043=CARTESIAN_POINT('Ctrl Pts',(1.35539361442374,-0.170853182351565,0.798432114295665));
#3044=CARTESIAN_POINT('Ctrl Pts',(1.35135963039426,-0.19976687381323,0.796425554654793));
#3045=CARTESIAN_POINT('Ctrl Pts',(1.34968868660415,-0.210760743950194,0.795657218396887));
#3046=CARTESIAN_POINT('Ctrl Pts',(1.34589805872927,-0.233803467809813,0.794034844583878));
#3047=CARTESIAN_POINT('Ctrl Pts',(1.343750369976,-0.245846643418606,0.7931800041941));
#3048=CARTESIAN_POINT('Ctrl Pts',(1.33815415633044,-0.274959420758521,0.791095961382389));
#3049=CARTESIAN_POINT('Ctrl Pts',(1.33454047932909,-0.291994672089594,0.789861736309058));
#3050=CARTESIAN_POINT('Ctrl Pts',(1.31923218988621,-0.357924050461646,0.785025141429504));
#3051=CARTESIAN_POINT('Ctrl Pts',(1.30516895363054,-0.406221764754839,0.781350968541966));
#3052=CARTESIAN_POINT('Ctrl Pts',(1.25157826387111,-0.558439297196694,0.769355688179964));
#3053=CARTESIAN_POINT('Ctrl Pts',(1.20203196062032,-0.658346151971301,0.760802120996546));
#3054=CARTESIAN_POINT('Ctrl Pts',(1.12923931012127,-0.768912910158518,0.751044261213925));
#3055=CARTESIAN_POINT('Ctrl Pts',(1.1171280984892,-0.786405375095243,0.749492398271245));
#3056=CARTESIAN_POINT('Ctrl Pts',(1.09967367435903,-0.810397611144833,0.747359770340762));
#3057=CARTESIAN_POINT('Ctrl Pts',(1.09467223495471,-0.817140860146732,0.746759910639003));
#3058=CARTESIAN_POINT('Ctrl Pts',(1.08551612640903,-0.82925073967982,0.74568242203702));
#3059=CARTESIAN_POINT('Ctrl Pts',(1.08138304307442,-0.83463331619384,0.745203432084687));
#3060=CARTESIAN_POINT('Ctrl Pts',(1.07254061708044,-0.845972978155569,0.744194475430444));
#3061=CARTESIAN_POINT('Ctrl Pts',(1.06782146025793,-0.851921939566133,0.743665180564802));
#3062=CARTESIAN_POINT('Ctrl Pts',(1.05450343250258,-0.868426075851183,0.742195830475928));
#3063=CARTESIAN_POINT('Ctrl Pts',(1.04579575170206,-0.878892837248058,0.74126290075392));
#3064=CARTESIAN_POINT('Ctrl Pts',(1.02548302493403,-0.90257959205657,0.739144467780926));
#3065=CARTESIAN_POINT('Ctrl Pts',(1.01377605236927,-0.915709304396001,0.737964914314965));
#3066=CARTESIAN_POINT('Ctrl Pts',(0.972390391295399,-0.960357665738139,
0.733920175961271));
#3067=CARTESIAN_POINT('Ctrl Pts',(0.941468045953489,-0.990690835827146,
0.73111194018989));
#3068=CARTESIAN_POINT('Ctrl Pts',(0.829839899372953,-1.09023644360328,0.72146843002732));
#3069=CARTESIAN_POINT('Ctrl Pts',(0.742550098032493,-1.15146292774452,0.714720626862009));
#3070=CARTESIAN_POINT('Ctrl Pts',(0.630873626567376,-1.21176778993492,0.70618497768149));
#3071=CARTESIAN_POINT('Ctrl Pts',(0.612477987412635,-1.22116884572154,0.704783182704664));
#3072=CARTESIAN_POINT('Ctrl Pts',(0.582293821502172,-1.23574080897006,0.702485523879612));
#3073=CARTESIAN_POINT('Ctrl Pts',(0.570632552690334,-1.24116876851978,0.701598446494986));
#3074=CARTESIAN_POINT('Ctrl Pts',(0.547862747484823,-1.25137869445491,0.699866518767907));
#3075=CARTESIAN_POINT('Ctrl Pts',(0.536763900918507,-1.2561794159826,0.699022395625653));
#3076=CARTESIAN_POINT('Ctrl Pts',(0.510308137269681,-1.26720803109582,0.697009733439444));
#3077=CARTESIAN_POINT('Ctrl Pts',(0.494899058674679,-1.27330493909369,0.695837004425059));
#3078=CARTESIAN_POINT('Ctrl Pts',(0.439314291503018,-1.29413677860556,0.691603021444579));
#3079=CARTESIAN_POINT('Ctrl Pts',(0.398565778452222,-1.30726113894922,0.688491433962572));
#3080=CARTESIAN_POINT('Ctrl Pts',(0.289746939849012,-1.33674873893412,0.68016247323671));
#3081=CARTESIAN_POINT('Ctrl Pts',(0.220920758644372,-1.34983071270429,0.67487020869525));
#3082=CARTESIAN_POINT('Ctrl Pts',(0.0911551707190771,-1.36430260085462,
0.664996340255401));
#3083=CARTESIAN_POINT('Ctrl Pts',(0.0305221387698023,-1.36700422630184,
0.660426642802755));
#3084=CARTESIAN_POINT('Ctrl Pts',(-0.0450138014688476,-1.36533968399014,
0.654916976798727));
#3085=CARTESIAN_POINT('Ctrl Pts',(-0.0599275413553788,-1.36476643812124,
0.653838249591838));
#3086=CARTESIAN_POINT('Ctrl Pts',(-0.0827695306686175,-1.36351326963545,
0.652202873967985));
#3087=CARTESIAN_POINT('Ctrl Pts',(-0.0907057251456946,-1.36300833128363,
0.651637798445057));
#3088=CARTESIAN_POINT('Ctrl Pts',(-0.104705713736729,-1.36199476213979,
0.650646988521089));
#3089=CARTESIAN_POINT('Ctrl Pts',(-0.110770928450203,-1.36151489973399,
0.650219784784554));
#3090=CARTESIAN_POINT('Ctrl Pts',(-0.125698029025745,-1.36023349889597,
0.649173204512182));
#3091=CARTESIAN_POINT('Ctrl Pts',(-0.134555611766342,-1.35938587760195,
0.648556301204183));
#3092=CARTESIAN_POINT('Ctrl Pts',(-0.163913406787781,-1.35628673010197,
0.646523437734934));
#3093=CARTESIAN_POINT('Ctrl Pts',(-0.184371915954379,-1.35365741820773,
0.645125941602153));
#3094=CARTESIAN_POINT('Ctrl Pts',(-0.334996255337121,-1.33082069734599,
0.634926851666106));
#3095=CARTESIAN_POINT('Ctrl Pts',(-0.461697235191861,-1.29234264611732,
0.626782148790904));
#3096=CARTESIAN_POINT('Ctrl Pts',(-0.612739443756689,-1.2213684941944,0.61578020457222));
#3097=CARTESIAN_POINT('Ctrl Pts',(-0.643950003674871,-1.20520483561193,
0.613434460149172));
#3098=CARTESIAN_POINT('Ctrl Pts',(-0.688145489969292,-1.18010931141388,
0.609982982474489));
#3099=CARTESIAN_POINT('Ctrl Pts',(-0.701655046375404,-1.17212728152373,
0.608909738571869));
#3100=CARTESIAN_POINT('Ctrl Pts',(-0.725255196663827,-1.1576290820534,0.607000578995664));
#3101=CARTESIAN_POINT('Ctrl Pts',(-0.735403113850195,-1.15120911917018,
0.606168161232628));
#3102=CARTESIAN_POINT('Ctrl Pts',(-0.756451654380441,-1.13750112231342,
0.604416581750326));
#3103=CARTESIAN_POINT('Ctrl Pts',(-0.767334567805011,-1.13018828012402,
0.603496573564412));
#3104=CARTESIAN_POINT('Ctrl Pts',(-0.796084768345773,-1.11026272285886,
0.601026449071966));
#3105=CARTESIAN_POINT('Ctrl Pts',(-0.81375660398966,-1.09737612700514,0.599466307248487));
#3106=CARTESIAN_POINT('Ctrl Pts',(-0.884762041809014,-1.04293933680528,
0.593019895953218));
#3107=CARTESIAN_POINT('Ctrl Pts',(-0.935278502704825,-0.997886834144783,
0.5880043158672));
#3108=CARTESIAN_POINT('Ctrl Pts',(-1.03526868624114,-0.894424880740563,
0.577172516095617));
#3109=CARTESIAN_POINT('Ctrl Pts',(-1.08360069506678,-0.83521675611104,0.571353707097514));
#3110=CARTESIAN_POINT('Ctrl Pts',(-1.14233896367567,-0.749519353743777,
0.563639454464373));
#3111=CARTESIAN_POINT('Ctrl Pts',(-1.1572488417153,-0.726287082800166,0.561613254277114));
#3112=CARTESIAN_POINT('Ctrl Pts',(-1.17666668426288,-0.693912492256261,
0.558892387332601));
#3113=CARTESIAN_POINT('Ctrl Pts',(-1.18179072441828,-0.685149423308594,
0.558165888912684));
#3114=CARTESIAN_POINT('Ctrl Pts',(-1.19018966968345,-0.670411036053599,
0.556961579801388));
#3115=CARTESIAN_POINT('Ctrl Pts',(-1.19351834800689,-0.664466980674374,
0.556480591483509));
#3116=CARTESIAN_POINT('Ctrl Pts',(-1.2004296492375,-0.651905873887536,0.555474363452153));
#3117=CARTESIAN_POINT('Ctrl Pts',(-1.20400229361304,-0.64528373219101,0.554949716038826));
#3118=CARTESIAN_POINT('Ctrl Pts',(-1.21373972330462,-0.626872286024494,
0.553506160624112));
#3119=CARTESIAN_POINT('Ctrl Pts',(-1.21978746794125,-0.615021580990691,
0.552593994222108));
#3120=CARTESIAN_POINT('Ctrl Pts',(-1.25669945158538,-0.540004496585257,
0.546913876345834));
#3121=CARTESIAN_POINT('Ctrl Pts',(-1.28282565801612,-0.47461478826364,0.54237433823007));
#3122=CARTESIAN_POINT('Ctrl Pts',(-1.33189446435503,-0.317617117155719,
0.531792766946884));
#3123=CARTESIAN_POINT('Ctrl Pts',(-1.35061430885415,-0.225082976948201,
0.525778325928075));
#3124=CARTESIAN_POINT('Ctrl Pts',(-1.36177845043777,-0.109529145641503,
0.517993482619221));
#3125=CARTESIAN_POINT('Ctrl Pts',(-1.3633616009835,-0.0876483812206271,
0.516508640083566));
#3126=CARTESIAN_POINT('Ctrl Pts',(-1.36502239500673,-0.0531789904680141,
0.514147489695694));
#3127=CARTESIAN_POINT('Ctrl Pts',(-1.36545410072905,-0.0406106475250119,
0.513281978098375));
#3128=CARTESIAN_POINT('Ctrl Pts',(-1.36590527229224,-0.0186347628800302,
0.511759778070425));
#3129=CARTESIAN_POINT('Ctrl Pts',(-1.36600119826705,-0.00922954513205333,
0.51110548077593));
#3130=CARTESIAN_POINT('Ctrl Pts',(-1.3659999887036,0.000175675168235992,
0.510448192708096));
#3131=CARTESIAN_POINT('Ctrl Pts',(-1.14737960344596,0.741266514552077,0.454399650883576));
#3132=CARTESIAN_POINT('Ctrl Pts',(-1.16980381270752,0.706556892810074,0.457297104121828));
#3133=CARTESIAN_POINT('Ctrl Pts',(-1.19062132235074,0.67087574888106,0.460194557360079));
#3134=CARTESIAN_POINT('Ctrl Pts',(-1.209754948191,0.634388654790895,0.46309201059833));
#3135=CARTESIAN_POINT('Ctrl Pts',(-1.23535670833523,0.585567075490906,0.466968949734391));
#3136=CARTESIAN_POINT('Ctrl Pts',(-1.25804035543911,0.535115314397402,0.470845888870453));
#3137=CARTESIAN_POINT('Ctrl Pts',(-1.27760921812476,0.4833949583546,0.474722828006513));
#3138=CARTESIAN_POINT('Ctrl Pts',(-1.2971361549215,0.431785412118988,0.478591460879605));
#3139=CARTESIAN_POINT('Ctrl Pts',(-1.31356140704316,0.378913085531293,0.482460093752696));
#3140=CARTESIAN_POINT('Ctrl Pts',(-1.32673491272539,0.325162223137256,0.486328726625788));
#3141=CARTESIAN_POINT('Ctrl Pts',(-1.33987073668409,0.271565110639755,0.490186293594493));
#3142=CARTESIAN_POINT('Ctrl Pts',(-1.34977321737813,0.217094895152634,0.494043860563197));
#3143=CARTESIAN_POINT('Ctrl Pts',(-1.35634174144863,0.162151411970686,0.497901427531902));
#3144=CARTESIAN_POINT('Ctrl Pts',(-1.36276129738084,0.108453996902938,0.501671508398166));
#3145=CARTESIAN_POINT('Ctrl Pts',(-1.36599645439874,0.0543049796234106,
0.505441589264431));
#3146=CARTESIAN_POINT('Ctrl Pts',(-1.36599999708368,8.92602306106192E-5,
0.509211670130695));
#3147=CARTESIAN_POINT('',(-1.36714090672731,0.00103847535578433,0.390789005901724));
#3148=CARTESIAN_POINT('Ctrl Pts',(-1.14737960344596,0.741266514552078,0.335993717254284));
#3149=CARTESIAN_POINT('Ctrl Pts',(-1.17597380908877,0.697006578770251,0.339667702888683));
#3150=CARTESIAN_POINT('Ctrl Pts',(-1.20199560468014,0.65110181371439,0.343341688523083));
#3151=CARTESIAN_POINT('Ctrl Pts',(-1.22526698137143,0.603884777387997,0.347015674157483));
#3152=CARTESIAN_POINT('Ctrl Pts',(-1.24854868955544,0.556646778723448,0.350691290883863));
#3153=CARTESIAN_POINT('Ctrl Pts',(-1.2690773348328,0.508095840000956,0.354366907610241));
#3154=CARTESIAN_POINT('Ctrl Pts',(-1.28672281254762,0.458585219637033,0.358042524336621));
#3155=CARTESIAN_POINT('Ctrl Pts',(-1.30440173491501,0.408980758487189,0.361725107704901));
#3156=CARTESIAN_POINT('Ctrl Pts',(-1.31918642143983,0.358413495999061,0.365407691073181));
#3157=CARTESIAN_POINT('Ctrl Pts',(-1.33099684162401,0.307251375240078,0.36909027444146));
#3158=CARTESIAN_POINT('Ctrl Pts',(-1.34002691658575,0.268133564150332,0.371905923956875));
#3159=CARTESIAN_POINT('Ctrl Pts',(-1.34731930023076,0.228668325964515,0.374721573472289));
#3160=CARTESIAN_POINT('Ctrl Pts',(-1.35285868001946,0.189022199479346,0.377537222987704));
#3161=CARTESIAN_POINT('Ctrl Pts',(-1.36154855341204,0.126827543614587,0.381954258601826));
#3162=CARTESIAN_POINT('Ctrl Pts',(-1.36595132362477,0.0640157464585561,
0.386371294215948));
#3163=CARTESIAN_POINT('Ctrl Pts',(-1.36599959856312,0.00104724658421214,
0.390788329830071));
#3164=CARTESIAN_POINT('Ctrl Pts',(-1.36716844264157,0.00103826373564391,
0.390789022213051));
#3165=CARTESIAN_POINT('Ctrl Pts',(-1.36407996739449,-0.384831305017282,
0.417833191053577));
#3166=CARTESIAN_POINT('Ctrl Pts',(-0.993135927374991,-1.22506008325323,
0.476338795143076));
#3167=CARTESIAN_POINT('Ctrl Pts',(0.425019159697173,-1.55235943515438,0.566305834481554));
#3168=CARTESIAN_POINT('Ctrl Pts',(1.53026813668533,-0.498999262857103,0.660690140228478));
#3169=CARTESIAN_POINT('Ctrl Pts',(1.25840837427535,1.00357516935923,0.755074445975404));
#3170=CARTESIAN_POINT('Ctrl Pts',(-0.10689282456352,1.58625723301147,0.84683417891952));
#3171=CARTESIAN_POINT('Ctrl Pts',(-0.923664677800894,1.08605463080936,0.90713247661466));
#3172=CARTESIAN_POINT('Ctrl Pts',(-1.14885860607148,0.742234466194312,0.935969339060826));
#3173=CARTESIAN_POINT('Origin',(0.,0.,-1.10921167016993));
#3174=CARTESIAN_POINT('',(-1.14737959979828,0.741266520198191,1.65532966579394));
#3175=CARTESIAN_POINT('',(-1.14737969890459,0.741266366795107,1.5357812853031));
#3176=CARTESIAN_POINT('',(-1.14737960344596,0.741266514552077,-1.10921167016993));
#3177=CARTESIAN_POINT('Ctrl Pts',(-1.14737959979828,0.741266520198191,1.65532966579394));
#3178=CARTESIAN_POINT('Ctrl Pts',(-1.13157732704963,0.765726285867094,1.65340285213149));
#3179=CARTESIAN_POINT('Ctrl Pts',(-1.11499628676279,0.789675525276667,1.65145455257775));
#3180=CARTESIAN_POINT('Ctrl Pts',(-1.09618984841233,0.815064371089371,1.64931104945167));
#3181=CARTESIAN_POINT('Ctrl Pts',(-1.09471282790514,0.817047083754974,1.64914312583003));
#3182=CARTESIAN_POINT('Ctrl Pts',(-1.09203671576753,0.820619141406182,1.64883962896734));
#3183=CARTESIAN_POINT('Ctrl Pts',(-1.09083951413336,0.822209899091305,1.64870412408433));
#3184=CARTESIAN_POINT('Ctrl Pts',(-1.08863657816546,0.825123725688757,1.64845527392725));
#3185=CARTESIAN_POINT('Ctrl Pts',(-1.08763189726973,0.826447589394383,1.64834196717432));
#3186=CARTESIAN_POINT('Ctrl Pts',(-1.08575151311276,0.82891599611319,1.64813024171768));
#3187=CARTESIAN_POINT('Ctrl Pts',(-1.08487640885809,0.830060994334693,1.64803184511967));
#3188=CARTESIAN_POINT('Ctrl Pts',(-1.08320819288929,0.832236566109536,1.64784453049659));
#3189=CARTESIAN_POINT('Ctrl Pts',(-1.0824154177483,0.833267396766278,1.64775562499771));
#3190=CARTESIAN_POINT('Ctrl Pts',(-1.08087361045307,0.835266266755387,1.64758293302855));
#3191=CARTESIAN_POINT('Ctrl Pts',(-1.08012474656809,0.836234434825733,1.64749915288156));
#3192=CARTESIAN_POINT('Ctrl Pts',(-1.07136207112076,0.847531844260759,1.64651994512447));
#3193=CARTESIAN_POINT('Ctrl Pts',(-1.06320191857769,0.857746218013062,1.64561905816151));
#3194=CARTESIAN_POINT('Ctrl Pts',(-1.04726522499238,0.877117915237756,1.6438793225995));
#3195=CARTESIAN_POINT('Ctrl Pts',(-1.03951199119753,0.886292893270802,1.64304145020067));
#3196=CARTESIAN_POINT('Ctrl Pts',(-1.02131423617514,0.907260354219105,1.64109348573989));
#3197=CARTESIAN_POINT('Ctrl Pts',(-1.01078489732438,0.918976590491354,1.63998001589182));
#3198=CARTESIAN_POINT('Ctrl Pts',(-0.975800267832639,0.956576040269497,
1.6363223781997));
#3199=CARTESIAN_POINT('Ctrl Pts',(-0.950536957374356,0.981683744160941,
1.63374519266463));
#3200=CARTESIAN_POINT('Ctrl Pts',(-0.827648614567908,1.09462024340742,1.62149315287158));
#3201=CARTESIAN_POINT('Ctrl Pts',(-0.718687769668506,1.16904921015942,1.61133802036522));
#3202=CARTESIAN_POINT('Ctrl Pts',(-0.582325191167811,1.23583021295908,1.60016533406788));
#3203=CARTESIAN_POINT('Ctrl Pts',(-0.563652377964652,1.24445773362186,1.59866763668675));
#3204=CARTESIAN_POINT('Ctrl Pts',(-0.536643199072388,1.25620420874822,1.59655382827057));
#3205=CARTESIAN_POINT('Ctrl Pts',(-0.528461052119848,1.25966815650352,1.59592025298032));
#3206=CARTESIAN_POINT('Ctrl Pts',(-0.514623531442021,1.2653677680976,1.59486081727722));
#3207=CARTESIAN_POINT('Ctrl Pts',(-0.508986191775682,1.26764586126778,1.59443257253152));
#3208=CARTESIAN_POINT('Ctrl Pts',(-0.495939338273296,1.27281712568727,1.59344929703094));
#3209=CARTESIAN_POINT('Ctrl Pts',(-0.488519503045984,1.27568333289407,1.592895817731));
#3210=CARTESIAN_POINT('Ctrl Pts',(-0.467095814635799,1.28374474923591,1.59131295322562));
#3211=CARTESIAN_POINT('Ctrl Pts',(-0.453030761263395,1.28877548701948,1.59029236419117));
#3212=CARTESIAN_POINT('Ctrl Pts',(-0.381314162641116,1.31310756518761,1.58516857237657));
#3213=CARTESIAN_POINT('Ctrl Pts',(-0.322496554436863,1.32877747540901,1.58122482071883));
#3214=CARTESIAN_POINT('Ctrl Pts',(-0.209358126060383,1.35096030710697,1.5737964073502));
#3215=CARTESIAN_POINT('Ctrl Pts',(-0.155313087492419,1.35823499743524,1.57031321191162));
#3216=CARTESIAN_POINT('Ctrl Pts',(-0.0640505476519799,1.3649998892132,1.5643728572327));
#3217=CARTESIAN_POINT('Ctrl Pts',(-0.0270287085696955,1.36623436238396,
1.5619475656185));
#3218=CARTESIAN_POINT('Ctrl Pts',(0.0375925412209382,1.36576148153045,1.55764651497081));
#3219=CARTESIAN_POINT('Ctrl Pts',(0.0651752125591951,1.36472328603271,1.55578924772369));
#3220=CARTESIAN_POINT('Ctrl Pts',(0.106897417192534,1.36188518906193,1.55293672271717));
#3221=CARTESIAN_POINT('Ctrl Pts',(0.121072339273535,1.36069827252482,1.55196004321749));
#3222=CARTESIAN_POINT('Ctrl Pts',(0.147030469113191,1.35811589078796,1.55015629090638));
#3223=CARTESIAN_POINT('Ctrl Pts',(0.158819099150086,1.3567878278786,1.54933136815925));
#3224=CARTESIAN_POINT('Ctrl Pts',(0.184753951117711,1.35352348080542,1.54750309522908));
#3225=CARTESIAN_POINT('Ctrl Pts',(0.198889962799352,1.3515186239245,1.5464977174662));
#3226=CARTESIAN_POINT('Ctrl Pts',(0.239671234317948,1.34508112949963,1.54357039161257));
#3227=CARTESIAN_POINT('Ctrl Pts',(0.266218411995413,1.34007952061447,1.54163130482753));
#3228=CARTESIAN_POINT('Ctrl Pts',(0.391271416578256,1.31265656760955,1.53233212369918));
#3229=CARTESIAN_POINT('Ctrl Pts',(0.487227415380485,1.28014221812151,1.52467441351063));
#3230=CARTESIAN_POINT('Ctrl Pts',(0.613975549195938,1.2208628589983,1.51410791260819));
#3231=CARTESIAN_POINT('Ctrl Pts',(0.648526424390272,1.20286571048635,1.51118118289506));
#3232=CARTESIAN_POINT('Ctrl Pts',(0.70293794930403,1.17149638267966,1.50653954856131));
#3233=CARTESIAN_POINT('Ctrl Pts',(0.72329864407153,1.1590361388582,1.50479504611658));
#3234=CARTESIAN_POINT('Ctrl Pts',(0.751200485149323,1.14093907548456,1.50240394369346));
#3235=CARTESIAN_POINT('Ctrl Pts',(0.759024618434151,1.13574899700753,1.50173339362481));
#3236=CARTESIAN_POINT('Ctrl Pts',(0.772394788113732,1.12668011327739,1.50058827360131));
#3237=CARTESIAN_POINT('Ctrl Pts',(0.777966496633989,1.12284011522064,1.50011132569043));
#3238=CARTESIAN_POINT('Ctrl Pts',(0.789998762271181,1.11441496178589,1.49908207692748));
#3239=CARTESIAN_POINT('Ctrl Pts',(0.796448281383773,1.10981480185904,1.49853075880253));
#3240=CARTESIAN_POINT('Ctrl Pts',(0.814817394342888,1.09647030849328,1.49696046975757));
#3241=CARTESIAN_POINT('Ctrl Pts',(0.826635953658063,1.08758795861832,1.49595008233042));
#3242=CARTESIAN_POINT('Ctrl Pts',(0.883949331738296,1.04303939534848,1.49103713249067));
#3243=CARTESIAN_POINT('Ctrl Pts',(0.927297354056396,1.00469829895977,1.48727847335196));
#3244=CARTESIAN_POINT('Ctrl Pts',(1.01998784567374,0.911587744246213,1.47880513393602));
#3245=CARTESIAN_POINT('Ctrl Pts',(1.06758868727028,0.855348711828194,1.47411867390129));
#3246=CARTESIAN_POINT('Ctrl Pts',(1.13511255015301,0.761099030570097,1.46652308406284));
#3247=CARTESIAN_POINT('Ctrl Pts',(1.15817676408061,0.725519322274498,1.4637084902383));
#3248=CARTESIAN_POINT('Ctrl Pts',(1.18787990540595,0.674663042408695,1.45971519310126));
#3249=CARTESIAN_POINT('Ctrl Pts',(1.19595152740628,0.660249040149263,1.45858668759304));
#3250=CARTESIAN_POINT('Ctrl Pts',(1.20947166205826,0.635043566939719,1.45661680995541));
#3251=CARTESIAN_POINT('Ctrl Pts',(1.21504210182008,0.624319395639666,1.45577976885854));
#3252=CARTESIAN_POINT('Ctrl Pts',(1.22625459015882,0.602014611412802,1.45404027590548));
#3253=CARTESIAN_POINT('Ctrl Pts',(1.23187655440053,0.590425310145571,1.45313723932975));
#3254=CARTESIAN_POINT('Ctrl Pts',(1.24612414164939,0.559965254266523,1.45076491473821));
#3255=CARTESIAN_POINT('Ctrl Pts',(1.25448489957484,0.540975060079367,1.44928696295526));
#3256=CARTESIAN_POINT('Ctrl Pts',(1.30274543076363,0.42421722483658,1.4402013830026));
#3257=CARTESIAN_POINT('Ctrl Pts',(1.33162344036849,0.322299666113666,1.43223568499318));
#3258=CARTESIAN_POINT('Ctrl Pts',(1.35543875472185,0.175051978015087,1.42095794797091));
#3259=CARTESIAN_POINT('Ctrl Pts',(1.36033606789949,0.1316951096914,1.41767056900508));
#3260=CARTESIAN_POINT('Ctrl Pts',(1.36480587007387,0.0625946555582757,1.41254245531937));
#3261=CARTESIAN_POINT('Ctrl Pts',(1.3657403127223,0.0369695940772661,1.41066509672106));
#3262=CARTESIAN_POINT('Ctrl Pts',(1.36603291079038,0.00169869731663778,
1.40812702760474));
#3263=CARTESIAN_POINT('Ctrl Pts',(1.36601092469451,-0.00793512638533304,
1.40743850892886));
#3264=CARTESIAN_POINT('Ctrl Pts',(1.3657995827943,-0.0243664154470303,1.40627311981112));
#3265=CARTESIAN_POINT('Ctrl Pts',(1.36566139112101,-0.0311640127470081,
1.40579363266095));
#3266=CARTESIAN_POINT('Ctrl Pts',(1.36525601021453,-0.0457458357883727,
1.4047709463584));
#3267=CARTESIAN_POINT('Ctrl Pts',(1.36497299857079,-0.0535292035892514,
1.40422858085078));
#3268=CARTESIAN_POINT('Ctrl Pts',(1.36398811968669,-0.0754504161648913,
1.40270988709086));
#3269=CARTESIAN_POINT('Ctrl Pts',(1.36313303449358,-0.089580831262057,1.40174129523892));
#3270=CARTESIAN_POINT('Ctrl Pts',(1.35599886749487,-0.183288830481665,1.39537160295281));
#3271=CARTESIAN_POINT('Ctrl Pts',(1.34297358179724,-0.262207804118862,1.39025853295132));
#3272=CARTESIAN_POINT('Ctrl Pts',(1.30124664725503,-0.42480771320341,1.37946772875809));
#3273=CARTESIAN_POINT('Ctrl Pts',(1.27117918385615,-0.507745485106411,1.37380390350069));
#3274=CARTESIAN_POINT('Ctrl Pts',(1.2248906524783,-0.6049675230205,1.36654940931271));
#3275=CARTESIAN_POINT('Ctrl Pts',(1.21605388867345,-0.622539709065144,1.36521285771542));
#3276=CARTESIAN_POINT('Ctrl Pts',(1.2009086985965,-0.651102658503491,1.3629945352084));
#3277=CARTESIAN_POINT('Ctrl Pts',(1.19482106669932,-0.662207651953928,1.36212039962681));
#3278=CARTESIAN_POINT('Ctrl Pts',(1.18263673340026,-0.68371908208986,1.3604032463307));
#3279=CARTESIAN_POINT('Ctrl Pts',(1.17655485970583,-0.694132604098824,1.35956081092558));
#3280=CARTESIAN_POINT('Ctrl Pts',(1.16289587070979,-0.716824478669667,1.35769966294096));
#3281=CARTESIAN_POINT('Ctrl Pts',(1.15526057367156,-0.729065921551139,1.35667894141426));
#3282=CARTESIAN_POINT('Ctrl Pts',(1.12812899701686,-0.771068554796105,1.35311693600891));
#3283=CARTESIAN_POINT('Ctrl Pts',(1.10766645147329,-0.800185216770624,1.35054138397971));
#3284=CARTESIAN_POINT('Ctrl Pts',(1.00656548959112,-0.932725039616337,1.33830225576582));
#3285=CARTESIAN_POINT('Ctrl Pts',(0.912457086631124,-1.02497058099155,1.32816074412412));
#3286=CARTESIAN_POINT('Ctrl Pts',(0.790090475053509,-1.11451089361474,1.31700399001067));
#3287=CARTESIAN_POINT('Ctrl Pts',(0.773249869817719,-1.12626028940802,1.31550893075498));
#3288=CARTESIAN_POINT('Ctrl Pts',(0.748755252895523,-1.14254120537556,1.3133981193078));
#3289=CARTESIAN_POINT('Ctrl Pts',(0.741312769643017,-1.14738407832488,1.3127649672859));
#3290=CARTESIAN_POINT('Ctrl Pts',(0.728695630625511,-1.15542011298492,1.31170600298635));
#3291=CARTESIAN_POINT('Ctrl Pts',(0.723546119789299,-1.15865179301619,1.31127781176725));
#3292=CARTESIAN_POINT('Ctrl Pts',(0.71160650986227,-1.1660340902125,1.31029432538927));
#3293=CARTESIAN_POINT('Ctrl Pts',(0.70480147755425,-1.17015990772813,1.30974058578339));
#3294=CARTESIAN_POINT('Ctrl Pts',(0.685105528684215,-1.18186718881086,1.30815619751506));
#3295=CARTESIAN_POINT('Ctrl Pts',(0.672125224610417,-1.18929700469306,1.3071343710307));
#3296=CARTESIAN_POINT('Ctrl Pts',(0.605547051049838,-1.22596747115425,1.3019920417282));
#3297=CARTESIAN_POINT('Ctrl Pts',(0.550148437685273,-1.25180742227082,1.29803234143895));
#3298=CARTESIAN_POINT('Ctrl Pts',(0.441199273615448,-1.29398947432656,1.29050547070303));
#3299=CARTESIAN_POINT('Ctrl Pts',(0.388014332740054,-1.31091963926611,1.28694094239898));
#3300=CARTESIAN_POINT('Ctrl Pts',(0.281838612941561,-1.33768851156519,1.27982747121024));
#3301=CARTESIAN_POINT('Ctrl Pts',(0.229008622398246,-1.34773797395584,1.27628896444022));
#3302=CARTESIAN_POINT('Ctrl Pts',(0.158129251480435,-1.35693259513905,1.27145572110254));
#3303=CARTESIAN_POINT('Ctrl Pts',(0.140488398532634,-1.35887228587463,1.27024607528252));
#3304=CARTESIAN_POINT('Ctrl Pts',(0.11057118219621,-1.36157304499883,1.26818060616542));
#3305=CARTESIAN_POINT('Ctrl Pts',(0.0983129365656097,-1.362513006413,1.26733034208558));
#3306=CARTESIAN_POINT('Ctrl Pts',(0.0735425453086204,-1.36407639201882,
1.26560338430746));
#3307=CARTESIAN_POINT('Ctrl Pts',(0.0610311989708883,-1.36469340275687,
1.26472657895214));
#3308=CARTESIAN_POINT('Ctrl Pts',(0.0295547822926375,-1.36581199350444,
1.26250846074222));
#3309=CARTESIAN_POINT('Ctrl Pts',(0.0105849825755796,-1.36609069275984,
1.26116050162535));
#3310=CARTESIAN_POINT('Ctrl Pts',(-0.0760357699270293,-1.3655590587654,
1.25495115622482));
#3311=CARTESIAN_POINT('Ctrl Pts',(-0.143553530846213,-1.36011871736758,
1.24995341463193));
#3312=CARTESIAN_POINT('Ctrl Pts',(-0.3048634630354,-1.33497487584253,1.23768901239036));
#3313=CARTESIAN_POINT('Ctrl Pts',(-0.397537925459773,-1.31036792905016,
1.23036176982192));
#3314=CARTESIAN_POINT('Ctrl Pts',(-0.503806367226208,-1.26982801047383,
1.22202347632841));
#3315=CARTESIAN_POINT('Ctrl Pts',(-0.520599444622563,-1.26303615480609,
1.22070860304169));
#3316=CARTESIAN_POINT('Ctrl Pts',(-0.545037031249402,-1.25258225503137,
1.21880413648154));
#3317=CARTESIAN_POINT('Ctrl Pts',(-0.552789768928874,-1.24918019195862,
1.2182012994533));
#3318=CARTESIAN_POINT('Ctrl Pts',(-0.566023340487419,-1.2432256917826,1.21717520673911));
#3319=CARTESIAN_POINT('Ctrl Pts',(-0.571519480170527,-1.24070868077049,
1.216749961424));
#3320=CARTESIAN_POINT('Ctrl Pts',(-0.58450832064387,-1.23465568388712,1.21574712916741));
#3321=CARTESIAN_POINT('Ctrl Pts',(-0.591985816169586,-1.23108790792638,
1.21517143350831));
#3322=CARTESIAN_POINT('Ctrl Pts',(-0.614810946185485,-1.21994117487299,
1.21341770018541));
#3323=CARTESIAN_POINT('Ctrl Pts',(-0.630049606176986,-1.21214129939181,
1.21225186849617));
#3324=CARTESIAN_POINT('Ctrl Pts',(-0.720803745453559,-1.16351485954236,
1.20531489930424));
#3325=CARTESIAN_POINT('Ctrl Pts',(-0.792487961997044,-1.11592613945786,
1.19985275676933));
#3326=CARTESIAN_POINT('Ctrl Pts',(-0.899960954706448,-1.02896577508745,
1.19095788458645));
#3327=CARTESIAN_POINT('Ctrl Pts',(-0.938754056362153,-0.993700446105792,
1.18757376884359));
#3328=CARTESIAN_POINT('Ctrl Pts',(-0.99981992989095,-0.931413141811491,
1.18181774950615));
#3329=CARTESIAN_POINT('Ctrl Pts',(-1.02325259697926,-0.90560705522448,1.17948890840282));
#3330=CARTESIAN_POINT('Ctrl Pts',(-1.05561843802805,-0.867101312770434,
1.17606954363348));
#3331=CARTESIAN_POINT('Ctrl Pts',(-1.06536322526795,-0.855100075337538,
1.17501121988319));
#3332=CARTESIAN_POINT('Ctrl Pts',(-1.08227001783854,-0.83354074675601,1.1731212235882));
#3333=CARTESIAN_POINT('Ctrl Pts',(-1.08951439314667,-0.824049112244289,
1.17229286615374));
#3334=CARTESIAN_POINT('Ctrl Pts',(-1.10459476690387,-0.803744176684975,
1.17052786589274));
#3335=CARTESIAN_POINT('Ctrl Pts',(-1.11239844606318,-0.792908554252095,
1.16959010806056));
#3336=CARTESIAN_POINT('Ctrl Pts',(-1.13325946616582,-0.763028258460327,
1.16701427138683));
#3337=CARTESIAN_POINT('Ctrl Pts',(-1.14599423610522,-0.743764907222998,
1.16536458182868));
#3338=CARTESIAN_POINT('Ctrl Pts',(-1.22478611878269,-0.617748863874061,
1.15463541675137));
#3339=CARTESIAN_POINT('Ctrl Pts',(-1.27633928039711,-0.50265420886069,1.14503984477189));
#3340=CARTESIAN_POINT('Ctrl Pts',(-1.32308195813287,-0.342256069747352,
1.13250260758063));
#3341=CARTESIAN_POINT('Ctrl Pts',(-1.33288802714624,-0.301819924240409,
1.12941581173562));
#3342=CARTESIAN_POINT('Ctrl Pts',(-1.3429784543516,-0.249981559509147,1.12559793785485));
#3343=CARTESIAN_POINT('Ctrl Pts',(-1.34498668216468,-0.238940902006796,
1.12479275219632));
#3344=CARTESIAN_POINT('Ctrl Pts',(-1.34804102960402,-0.220888237432621,
1.12349045250493));
#3345=CARTESIAN_POINT('Ctrl Pts',(-1.34916898496192,-0.213890832000283,
1.12298914849105));
#3346=CARTESIAN_POINT('Ctrl Pts',(-1.35133703327292,-0.19974096666365,1.12198287222489));
#3347=CARTESIAN_POINT('Ctrl Pts',(-1.35237492353611,-0.192588430649364,
1.12147802405521));
#3348=CARTESIAN_POINT('Ctrl Pts',(-1.35496873258695,-0.173657356554059,
1.12015106283942));
#3349=CARTESIAN_POINT('Ctrl Pts',(-1.35642788350477,-0.16186588527212,1.11933399261896));
#3350=CARTESIAN_POINT('Ctrl Pts',(-1.36320088912587,-0.100582694163536,
1.11512939661801));
#3351=CARTESIAN_POINT('Ctrl Pts',(-1.3659611275071,-0.0508413741491877,
1.11185760075806));
#3352=CARTESIAN_POINT('Ctrl Pts',(-1.36608560145227,0.110268494496373,1.10140450719495));
#3353=CARTESIAN_POINT('Ctrl Pts',(-1.35256365678427,0.221178661717358,1.0943951332629));
#3354=CARTESIAN_POINT('Ctrl Pts',(-1.32013206461214,0.351777820116467,1.08541682949322));
#3355=CARTESIAN_POINT('Ctrl Pts',(-1.31395532898235,0.374189250266236,1.08385104960099));
#3356=CARTESIAN_POINT('Ctrl Pts',(-1.30295487259447,0.410462652564167,1.08126885063572));
#3357=CARTESIAN_POINT('Ctrl Pts',(-1.29847412286516,0.424424213827309,1.08026319994651));
#3358=CARTESIAN_POINT('Ctrl Pts',(-1.28995975318309,0.449556244798788,1.07843007567478));
#3359=CARTESIAN_POINT('Ctrl Pts',(-1.286003502312,0.460751514999018,1.07760516809675));
#3360=CARTESIAN_POINT('Ctrl Pts',(-1.27710652106028,0.484920226046374,1.07580545425383));
#3361=CARTESIAN_POINT('Ctrl Pts',(-1.27211299595738,0.497872666528782,1.07482899979953));
#3362=CARTESIAN_POINT('Ctrl Pts',(-1.25728339813184,0.53465797163118,1.07202035033582));
#3363=CARTESIAN_POINT('Ctrl Pts',(-1.24696928439987,0.558290368356846,1.07017273559371));
#3364=CARTESIAN_POINT('Ctrl Pts',(-1.2145883724344,0.627103172903603,1.0646605492661));
#3365=CARTESIAN_POINT('Ctrl Pts',(-1.19069091880293,0.671369855409078,1.06094017952552));
#3366=CARTESIAN_POINT('Ctrl Pts',(-1.15883876703743,0.723299585331697,1.05637300530005));
#3367=CARTESIAN_POINT('Ctrl Pts',(-1.15316122838722,0.732317346808646,1.05557222496468));
#3368=CARTESIAN_POINT('Ctrl Pts',(-1.14737959575237,0.741266526460718,1.05477007217181));
#3369=CARTESIAN_POINT('',(-1.36400241667853,1.39474960495158E-5,0.990700274402563));
#3370=CARTESIAN_POINT('Ctrl Pts',(-1.14885860607148,0.742234466194312,0.935969339060826));
#3371=CARTESIAN_POINT('Ctrl Pts',(-1.16935452030627,0.710941843607821,0.938593911863636));
#3372=CARTESIAN_POINT('Ctrl Pts',(-1.30251261166389,0.487041195934633,0.9568669035642));
#3373=CARTESIAN_POINT('Ctrl Pts',(-1.36387713097247,0.224696456629905,0.975139895264764));
#3374=CARTESIAN_POINT('Ctrl Pts',(-1.36384943109475,2.00760032713424E-5,
0.990788314162518));
#3375=CARTESIAN_POINT('Ctrl Pts',(-1.36599999840197,-6.6074383892362E-5,
0.989550711083759));
#3376=CARTESIAN_POINT('Ctrl Pts',(-1.36599971820694,-0.00585873393595662,
0.989953076044015));
#3377=CARTESIAN_POINT('Ctrl Pts',(-1.36596259150209,-0.011651267602572,
0.990356560016656));
#3378=CARTESIAN_POINT('Ctrl Pts',(-1.36578899683438,-0.0252444878524435,
0.991306141617785));
#3379=CARTESIAN_POINT('Ctrl Pts',(-1.36562254090052,-0.0330445056752,0.991853141539721));
#3380=CARTESIAN_POINT('Ctrl Pts',(-1.36490816371014,-0.0569265470916234,
0.993534654597446));
#3381=CARTESIAN_POINT('Ctrl Pts',(-1.3641429041869,-0.0730001705183924,
0.994675728498607));
#3382=CARTESIAN_POINT('Ctrl Pts',(-1.36007357431624,-0.135285506229272,
0.999135492985641));
#3383=CARTESIAN_POINT('Ctrl Pts',(-1.35470372623049,-0.181326384655276,
1.00251504937969));
#3384=CARTESIAN_POINT('Ctrl Pts',(-1.32760515654106,-0.342127015480296,
1.01460520713435));
#3385=CARTESIAN_POINT('Ctrl Pts',(-1.29352781976786,-0.454278660724451,
1.02360662992386));
#3386=CARTESIAN_POINT('Ctrl Pts',(-1.23709430889794,-0.579641219598352,
1.03372539977164));
#3387=CARTESIAN_POINT('Ctrl Pts',(-1.22814924475359,-0.598360943080897,
1.03523634447006));
#3388=CARTESIAN_POINT('Ctrl Pts',(-1.21475642286182,-0.624821770877291,
1.03736503505638));
#3389=CARTESIAN_POINT('Ctrl Pts',(-1.2106543024637,-0.632733421903402,1.03800057467419));
#3390=CARTESIAN_POINT('Ctrl Pts',(-1.20362293793128,-0.645975856424783,
1.03906207707982));
#3391=CARTESIAN_POINT('Ctrl Pts',(-1.20073509571223,-0.651328042645779,
1.03949045058018));
#3392=CARTESIAN_POINT('Ctrl Pts',(-1.1939988674979,-0.663615554845057,1.04047229726013));
#3393=CARTESIAN_POINT('Ctrl Pts',(-1.19012569366639,-0.670536905338416,
1.04102424118296));
#3394=CARTESIAN_POINT('Ctrl Pts',(-1.17883665185755,-0.690304389260967,
1.04259854532155));
#3395=CARTESIAN_POINT('Ctrl Pts',(-1.1712712992169,-0.703064427855035,1.04361225254016));
#3396=CARTESIAN_POINT('Ctrl Pts',(-1.12687739197088,-0.775234784811891,
1.04934623798698));
#3397=CARTESIAN_POINT('Ctrl Pts',(-1.08573544125307,-0.83187889150494,1.05385191525824));
#3398=CARTESIAN_POINT('Ctrl Pts',(-0.998299780142475,-0.934655883076809,
1.06253045750487));
#3399=CARTESIAN_POINT('Ctrl Pts',(-0.952685966083009,-0.981108020341267,
1.06669416484621));
#3400=CARTESIAN_POINT('Ctrl Pts',(-0.874208534799108,-1.05037514167524,
1.07356843496014));
#3401=CARTESIAN_POINT('Ctrl Pts',(-0.843351948914514,-1.07530718565557,
1.07620771903259));
#3402=CARTESIAN_POINT('Ctrl Pts',(-0.79845842317706,-1.10845894684282,1.07999483548594));
#3403=CARTESIAN_POINT('Ctrl Pts',(-0.785291300497509,-1.11782584807407,
1.08109944607787));
#3404=CARTESIAN_POINT('Ctrl Pts',(-0.762038259500069,-1.1337541040856,1.08304160395797));
#3405=CARTESIAN_POINT('Ctrl Pts',(-0.752025877316006,-1.14041998459369,
1.08387516859844));
#3406=CARTESIAN_POINT('Ctrl Pts',(-0.730998849231473,-1.1540216982819,1.08562094697105));
#3407=CARTESIAN_POINT('Ctrl Pts',(-0.719970526919759,-1.16093402797429,
1.08653390748459));
#3408=CARTESIAN_POINT('Ctrl Pts',(-0.690533193135543,-1.17880398018401,
1.08896476446125));
#3409=CARTESIAN_POINT('Ctrl Pts',(-0.671962945912466,-1.18948754599371,
1.09049214010104));
#3410=CARTESIAN_POINT('Ctrl Pts',(-0.56500683908583,-1.24771599357046,1.09925988093357));
#3411=CARTESIAN_POINT('Ctrl Pts',(-0.47185790456303,-1.28583485888557,1.10681726125845));
#3412=CARTESIAN_POINT('Ctrl Pts',(-0.330903572902713,-1.32612218781549,
1.11790517178678));
#3413=CARTESIAN_POINT('Ctrl Pts',(-0.285792030538076,-1.33657045526746,
1.12139892576925));
#3414=CARTESIAN_POINT('Ctrl Pts',(-0.214065676243491,-1.34938452167839,
1.12680055089519));
#3415=CARTESIAN_POINT('Ctrl Pts',(-0.187763169472017,-1.35329520503533,
1.1287492374207));
#3416=CARTESIAN_POINT('Ctrl Pts',(-0.151673010699197,-1.35758848340937,
1.13136552408717));
#3417=CARTESIAN_POINT('Ctrl Pts',(-0.141972225098897,-1.35863721939741,
1.13206310568842));
#3418=CARTESIAN_POINT('Ctrl Pts',(-0.125477028225057,-1.36024187879218,
1.13323876489778));
#3419=CARTESIAN_POINT('Ctrl Pts',(-0.118688322072044,-1.36085103671198,
1.13371958023493));
#3420=CARTESIAN_POINT('Ctrl Pts',(-0.104196571770856,-1.36204212105187,
1.134739240854));
#3421=CARTESIAN_POINT('Ctrl Pts',(-0.0964927459160662,-1.36260956346707,
1.13527732401677));
#3422=CARTESIAN_POINT('Ctrl Pts',(-0.0749497824999238,-1.36401273289613,
1.13677197227432));
#3423=CARTESIAN_POINT('Ctrl Pts',(-0.061101696657003,-1.36470320033262,
1.13772118002585));
#3424=CARTESIAN_POINT('Ctrl Pts',(0.0372034780668299,-1.36810524496565,
1.14439263975978));
#3425=CARTESIAN_POINT('Ctrl Pts',(0.121752283431182,-1.36318604633399,1.14978869893391));
#3426=CARTESIAN_POINT('Ctrl Pts',(0.261098416573521,-1.34200131594934,1.15885047828505));
#3427=CARTESIAN_POINT('Ctrl Pts',(0.31630198531597,-1.33007232795107,1.16248466690074));
#3428=CARTESIAN_POINT('Ctrl Pts',(0.405727375668058,-1.30486503144901,1.16860518912165));
#3429=CARTESIAN_POINT('Ctrl Pts',(0.440434414905356,-1.29356276266282,1.17104024991354));
#3430=CARTESIAN_POINT('Ctrl Pts',(0.489372418490752,-1.27542828355224,1.17458575774299));
#3431=CARTESIAN_POINT('Ctrl Pts',(0.504003801265473,-1.26971760818832,1.17566041880422));
#3432=CARTESIAN_POINT('Ctrl Pts',(0.529603649078354,-1.25921371029358,1.17756846976397));
#3433=CARTESIAN_POINT('Ctrl Pts',(0.540613836152455,-1.25452614864311,1.17839830839343));
#3434=CARTESIAN_POINT('Ctrl Pts',(0.563652892255889,-1.24435771414835,1.18015500620983));
#3435=CARTESIAN_POINT('Ctrl Pts',(0.575666573623299,-1.23884570386525,1.18108283938831));
#3436=CARTESIAN_POINT('Ctrl Pts',(0.607844845302013,-1.22351283349132,1.18360103690442));
#3437=CARTESIAN_POINT('Ctrl Pts',(0.627849877946327,-1.21336863127762,1.18520214746491));
#3438=CARTESIAN_POINT('Ctrl Pts',(0.722260749054286,-1.16253456225445,1.19293489870159));
#3439=CARTESIAN_POINT('Ctrl Pts',(0.793009068206225,-1.11547280294266,1.19928094237725));
#3440=CARTESIAN_POINT('Ctrl Pts',(0.902456238054577,-1.02696755214495,1.20992271836466));
#3441=CARTESIAN_POINT('Ctrl Pts',(0.943780540101118,-0.989125053524125,
1.21416834627533));
#3442=CARTESIAN_POINT('Ctrl Pts',(1.00329583183991,-0.927488764535791,1.22054050063554));
#3443=CARTESIAN_POINT('Ctrl Pts',(1.02322386288932,-0.905456322927489,1.22272388323281));
#3444=CARTESIAN_POINT('Ctrl Pts',(1.04896815072218,-0.875056859813829,1.22559487893615));
#3445=CARTESIAN_POINT('Ctrl Pts',(1.05543105956159,-0.86725081919667,1.22632014292951));
#3446=CARTESIAN_POINT('Ctrl Pts',(1.06613268586864,-0.854028324184944,1.22752776457364));
#3447=CARTESIAN_POINT('Ctrl Pts',(1.07041837039391,-0.848650577914439,1.22801322911521));
#3448=CARTESIAN_POINT('Ctrl Pts',(1.07933043287372,-0.837292644668275,1.22902634846271));
#3449=CARTESIAN_POINT('Ctrl Pts',(1.08394805692281,-0.831306064574237,1.22955343522473));
#3450=CARTESIAN_POINT('Ctrl Pts',(1.09664771947624,-0.814555673175179,1.23101009396719));
#3451=CARTESIAN_POINT('Ctrl Pts',(1.10462097499715,-0.803709960806694,1.23193273713203));
#3452=CARTESIAN_POINT('Ctrl Pts',(1.16443993179773,-0.719768268015663,1.23893319260093));
#3453=CARTESIAN_POINT('Ctrl Pts',(1.2091464515665,-0.641837967024095,1.24463793109827));
#3454=CARTESIAN_POINT('Ctrl Pts',(1.26795620987057,-0.511015547243028,1.25386333794568));
#3455=CARTESIAN_POINT('Ctrl Pts',(1.28709406617809,-0.460693126610454,1.25733471660028));
#3456=CARTESIAN_POINT('Ctrl Pts',(1.31055276517993,-0.386014348683778,1.26249686011757));
#3457=CARTESIAN_POINT('Ctrl Pts',(1.31726149745273,-0.362460576343731,1.26412609371639));
#3458=CARTESIAN_POINT('Ctrl Pts',(1.32838342292677,-0.319011309159441,1.26714393205334));
#3459=CARTESIAN_POINT('Ctrl Pts',(1.33299147646412,-0.299172835840265,1.26852647854059));
#3460=CARTESIAN_POINT('Ctrl Pts',(1.33977097379199,-0.266708839967383,1.2708005266587));
#3461=CARTESIAN_POINT('Ctrl Pts',(1.34221143627971,-0.254142300176839,1.2716835857127));
#3462=CARTESIAN_POINT('Ctrl Pts',(1.34661726390728,-0.229618683653578,1.27341324842383));
#3463=CARTESIAN_POINT('Ctrl Pts',(1.34860085356431,-0.217666066371998,1.2742591969321));
#3464=CARTESIAN_POINT('Ctrl Pts',(1.35294499213508,-0.189145170331141,1.27628548220772));
#3465=CARTESIAN_POINT('Ctrl Pts',(1.35516052050762,-0.172557140514531,1.27747017057894));
#3466=CARTESIAN_POINT('Ctrl Pts',(1.36174076419938,-0.115289964440575,1.28158327774038));
#3467=CARTESIAN_POINT('Ctrl Pts',(1.36458219978601,-0.0744614408658086,
1.28455666860532));
#3468=CARTESIAN_POINT('Ctrl Pts',(1.36806039770056,0.0670257218852508,1.29500164968891));
#3469=CARTESIAN_POINT('Ctrl Pts',(1.35940948633371,0.167582899848372,1.30269848514071));
#3470=CARTESIAN_POINT('Ctrl Pts',(1.33221638261792,0.304415278280409,1.31315012516));
#3471=CARTESIAN_POINT('Ctrl Pts',(1.32300708088774,0.342230901882291,1.31603197950062));
#3472=CARTESIAN_POINT('Ctrl Pts',(1.30913367781016,0.390187617103829,1.31963908805924));
#3473=CARTESIAN_POINT('Ctrl Pts',(1.30594421413549,0.400733193468631,1.32042924026901));
#3474=CARTESIAN_POINT('Ctrl Pts',(1.30050678211481,0.41795660881569,1.32171348571905));
#3475=CARTESIAN_POINT('Ctrl Pts',(1.2983341713222,0.424657514180147,1.32221156272101));
#3476=CARTESIAN_POINT('Ctrl Pts',(1.29381224996417,0.438245136255998,1.32321792442939));
#3477=CARTESIAN_POINT('Ctrl Pts',(1.2914595765778,0.445130437013794,1.32372601241792));
#3478=CARTESIAN_POINT('Ctrl Pts',(1.28504346124139,0.46342858781296,1.3250721248761));
#3479=CARTESIAN_POINT('Ctrl Pts',(1.28088292254041,0.47480703191576,1.32590484144544));
#3480=CARTESIAN_POINT('Ctrl Pts',(1.25599704284703,0.540157164712757,1.33067048288301));
#3481=CARTESIAN_POINT('Ctrl Pts',(1.23201091411976,0.5928313831814,1.33444591814982));
#3482=CARTESIAN_POINT('Ctrl Pts',(1.18003156111349,0.690096495058467,1.3415717651673));
#3483=CARTESIAN_POINT('Ctrl Pts',(1.15266315102943,0.734898206343554,1.34492331878128));
#3484=CARTESIAN_POINT('Ctrl Pts',(1.09842580315503,0.813170379170403,1.35107699943143));
#3485=CARTESIAN_POINT('Ctrl Pts',(1.07242945004472,0.847159961708913,1.35386246169437));
#3486=CARTESIAN_POINT('Ctrl Pts',(1.02523650298917,0.903203423018099,1.35872103338478));
#3487=CARTESIAN_POINT('Ctrl Pts',(1.00481548580632,0.925868202763723,1.3607676692199));
#3488=CARTESIAN_POINT('Ctrl Pts',(0.973424929579,0.958445221402814,1.3638488384095));
#3489=CARTESIAN_POINT('Ctrl Pts',(0.963024812776036,0.968894482057306,1.36485976165408));
#3490=CARTESIAN_POINT('Ctrl Pts',(0.943945671069267,0.987453081424666,1.36669820810733));
#3491=CARTESIAN_POINT('Ctrl Pts',(0.935326023762489,0.995621530342088,1.36752308807179));
#3492=CARTESIAN_POINT('Ctrl Pts',(0.916452581968859,1.01304562735979,1.369317792464));
#3493=CARTESIAN_POINT('Ctrl Pts',(0.906162778296736,1.02226012957224,1.37028920010721));
#3494=CARTESIAN_POINT('Ctrl Pts',(0.877078910421223,1.04752050574687,1.37301652726726));
#3495=CARTESIAN_POINT('Ctrl Pts',(0.85798736800867,1.06321407150413,1.37478615687274));
#3496=CARTESIAN_POINT('Ctrl Pts',(0.741794189063529,1.15355868777923,1.38544222987471));
#3497=CARTESIAN_POINT('Ctrl Pts',(0.635444600106159,1.21538316082066,1.39480632342373));
#3498=CARTESIAN_POINT('Ctrl Pts',(0.484137394908458,1.27799610643505,1.40709252244094));
#3499=CARTESIAN_POINT('Ctrl Pts',(0.445259392287595,1.29205565010245,1.41015899748468));
#3500=CARTESIAN_POINT('Ctrl Pts',(0.395105893142297,1.30765927294194,1.41395595125018));
#3501=CARTESIAN_POINT('Ctrl Pts',(0.384370512151149,1.31085497713966,1.41475960322069));
#3502=CARTESIAN_POINT('Ctrl Pts',(0.366784818952044,1.31585525358002,1.41605998066588));
#3503=CARTESIAN_POINT('Ctrl Pts',(0.359957835692098,1.3177391682049,1.41656087570821));
#3504=CARTESIAN_POINT('Ctrl Pts',(0.34613265694,1.32143877915577,1.41756689103193));
#3505=CARTESIAN_POINT('Ctrl Pts',(0.339134115492188,1.32325217594435,1.4180718811622));
#3506=CARTESIAN_POINT('Ctrl Pts',(0.320581903322071,1.32790239363983,1.41940007166375));
#3507=CARTESIAN_POINT('Ctrl Pts',(0.309004716639921,1.33064406703903,1.42021821049536));
#3508=CARTESIAN_POINT('Ctrl Pts',(0.248426050811365,1.34415681080554,1.42445065102255));
#3509=CARTESIAN_POINT('Ctrl Pts',(0.198889122788832,1.3523746814428,1.42774733026674));
#3510=CARTESIAN_POINT('Ctrl Pts',(0.0662809023176067,1.3669268119549,1.4364007878843));
#3511=CARTESIAN_POINT('Ctrl Pts',(-0.0171007684340999,1.368426015679,1.44167504131703));
#3512=CARTESIAN_POINT('Ctrl Pts',(-0.144987923195956,1.35902915175095,1.45005740647554));
#3513=CARTESIAN_POINT('Ctrl Pts',(-0.189680614389856,1.35351482330885,1.45304029687786));
#3514=CARTESIAN_POINT('Ctrl Pts',(-0.250605291534695,1.34292088147446,1.45723016631043));
#3515=CARTESIAN_POINT('Ctrl Pts',(-0.267138611501065,1.33972998270011,1.45837972152194));
#3516=CARTESIAN_POINT('Ctrl Pts',(-0.295476671902101,1.33371539090555,1.46037396341401));
#3517=CARTESIAN_POINT('Ctrl Pts',(-0.307310772708272,1.33103842172536,1.46121400475911));
#3518=CARTESIAN_POINT('Ctrl Pts',(-0.331522048115637,1.32522154884207,1.46294832692322));
#3519=CARTESIAN_POINT('Ctrl Pts',(-0.343893957955208,1.32206503168961,1.46384305637293));
#3520=CARTESIAN_POINT('Ctrl Pts',(-0.375720445324805,1.31346799894435,1.46616762533902));
#3521=CARTESIAN_POINT('Ctrl Pts',(-0.39510122864154,1.30776870250963,1.46760548940642));
#3522=CARTESIAN_POINT('Ctrl Pts',(-0.518592069877246,1.26845824971648,1.476916428314));
#3523=CARTESIAN_POINT('Ctrl Pts',(-0.618455546352899,1.22287696765016,1.48517945344773));
#3524=CARTESIAN_POINT('Ctrl Pts',(-0.74745539599868,1.14412069327667,1.4966024619638));
#3525=CARTESIAN_POINT('Ctrl Pts',(-0.782100977569658,1.12072305894729,1.49974889806064));
#3526=CARTESIAN_POINT('Ctrl Pts',(-0.829437186269884,1.08548910299477,1.50411563306687));
#3527=CARTESIAN_POINT('Ctrl Pts',(-0.843058184683076,1.07494446051572,1.50538047425985));
#3528=CARTESIAN_POINT('Ctrl Pts',(-0.866915684933313,1.0557427512455,1.50760602581046));
#3529=CARTESIAN_POINT('Ctrl Pts',(-0.877230942197576,1.04718740912945,1.50857178937316));
#3530=CARTESIAN_POINT('Ctrl Pts',(-0.893157186541404,1.03357786785068,1.51006629646821));
#3531=CARTESIAN_POINT('Ctrl Pts',(-0.89885470255575,1.02862685141355,1.51060164790513));
#3532=CARTESIAN_POINT('Ctrl Pts',(-0.90960919327487,1.0191238395641,1.51161302967644));
#3533=CARTESIAN_POINT('Ctrl Pts',(-0.914673615887704,1.01458092993267,1.51208962135287));
#3534=CARTESIAN_POINT('Ctrl Pts',(-0.925969279302745,1.00429512419505,1.51315382058671));
#3535=CARTESIAN_POINT('Ctrl Pts',(-0.932181548827975,0.998531607876709,
1.51373995789283));
#3536=CARTESIAN_POINT('Ctrl Pts',(-0.954200705440345,0.977718434680552,
1.51582235912017));
#3537=CARTESIAN_POINT('Ctrl Pts',(-0.969700927019773,0.962347423181087,
1.51729735589802));
#3538=CARTESIAN_POINT('Ctrl Pts',(-1.04549531662969,0.883493062094843,1.52459831004909));
#3539=CARTESIAN_POINT('Ctrl Pts',(-1.09992250297435,0.814723663141511,1.53014261435709));
#3540=CARTESIAN_POINT('Ctrl Pts',(-1.14737969890454,0.741266366795177,1.5357812853031));
#3541=CARTESIAN_POINT('Origin',(0.,0.,-1.10921167016993));
#3542=CARTESIAN_POINT('',(-1.14737960344529,0.741266514553124,2.25320219258599));
#3543=CARTESIAN_POINT('',(-1.14737960371854,0.741266514130168,2.135049540568));
#3544=CARTESIAN_POINT('',(-1.14737960344596,0.741266514552077,-1.10921167016993));
#3545=CARTESIAN_POINT('',(-1.36599959227551,0.0011382718177414,1.70898245993473));
#3546=CARTESIAN_POINT('Ctrl Pts',(-1.14737960344529,0.741266514553124,2.25320219258599));
#3547=CARTESIAN_POINT('Ctrl Pts',(-1.14445511162778,0.745793229568547,2.25282905037715));
#3548=CARTESIAN_POINT('Ctrl Pts',(-1.14150377684851,0.750302721850362,2.25245750693874));
#3549=CARTESIAN_POINT('Ctrl Pts',(-1.12420874842134,0.77639039027772,2.25030841753053));
#3550=CARTESIAN_POINT('Ctrl Pts',(-1.1092790965877,0.797575976318259,2.24856437172645));
#3551=CARTESIAN_POINT('Ctrl Pts',(-1.06717671624587,0.853849027793015,2.24389757279359));
#3552=CARTESIAN_POINT('Ctrl Pts',(-1.0388820822608,0.888059031968562,2.24102217132267));
#3553=CARTESIAN_POINT('Ctrl Pts',(-0.938828385019889,0.997689384824558,
2.23145678395337));
#3554=CARTESIAN_POINT('Ctrl Pts',(-0.860141974766843,1.06627218862519,2.2248422786487));
#3555=CARTESIAN_POINT('Ctrl Pts',(-0.757174265703757,1.13713775611744,2.21644016614157));
#3556=CARTESIAN_POINT('Ctrl Pts',(-0.739641422695242,1.1486190113294,2.21501867968504));
#3557=CARTESIAN_POINT('Ctrl Pts',(-0.710881183244377,1.16652086997473,2.21269702938018));
#3558=CARTESIAN_POINT('Ctrl Pts',(-0.699814171982334,1.17319354832763,2.21180601059069));
#3559=CARTESIAN_POINT('Ctrl Pts',(-0.67823343471858,1.1857913022383,2.21007205922352));
#3560=CARTESIAN_POINT('Ctrl Pts',(-0.667732550068085,1.19173605700885,2.20922992700998));
#3561=CARTESIAN_POINT('Ctrl Pts',(-0.642773149910792,1.20543261307876,2.20723122537711));
#3562=CARTESIAN_POINT('Ctrl Pts',(-0.628251309955228,1.21306444877735,2.20607062640862));
#3563=CARTESIAN_POINT('Ctrl Pts',(-0.576529716964119,1.23906847950664,2.20194303707089));
#3564=CARTESIAN_POINT('Ctrl Pts',(-0.538637322008174,1.25600414846177,2.1989290605175));
#3565=CARTESIAN_POINT('Ctrl Pts',(-0.434315959238254,1.29704014928147,2.19065726485226));
#3566=CARTESIAN_POINT('Ctrl Pts',(-0.366694825105042,1.31775443718619,2.18531753674902));
#3567=CARTESIAN_POINT('Ctrl Pts',(-0.237683512724645,1.34657143932558,2.17532002118052));
#3568=CARTESIAN_POINT('Ctrl Pts',(-0.176740113790914,1.3559175349425,2.17067545622709));
#3569=CARTESIAN_POINT('Ctrl Pts',(-0.100429649689385,1.3623856589389,2.16508987497068));
#3570=CARTESIAN_POINT('Ctrl Pts',(-0.0854693252049242,1.36340597002702,
2.16400593341543));
#3571=CARTESIAN_POINT('Ctrl Pts',(-0.062539297974867,1.36459088748245,2.16236440620136));
#3572=CARTESIAN_POINT('Ctrl Pts',(-0.0545804118632267,1.36493239419239,
2.16179829858248));
#3573=CARTESIAN_POINT('Ctrl Pts',(-0.0405439649607817,1.36541170819417,
2.16080686413368));
#3574=CARTESIAN_POINT('Ctrl Pts',(-0.03446805439255,1.36557859586381,2.16038005029851));
#3575=CARTESIAN_POINT('Ctrl Pts',(-0.0195256361898784,1.36588922526132,
2.15933594172263));
#3576=CARTESIAN_POINT('Ctrl Pts',(-0.0106585245172626,1.36598720080949,
2.15872109477129));
#3577=CARTESIAN_POINT('Ctrl Pts',(0.0186673079805364,1.36602564615178,2.15670147168563));
#3578=CARTESIAN_POINT('Ctrl Pts',(0.0391247549541757,1.3655928733285,2.15531485619726));
#3579=CARTESIAN_POINT('Ctrl Pts',(0.190191064322846,1.35899917704707,2.14518933649449));
#3580=CARTESIAN_POINT('Ctrl Pts',(0.319330730285382,1.33457366653338,2.13710173139782));
#3581=CARTESIAN_POINT('Ctrl Pts',(0.476989377424977,1.28051755840669,2.12612521357094));
#3582=CARTESIAN_POINT('Ctrl Pts',(0.510464697207438,1.26754468822479,2.12373139493531));
#3583=CARTESIAN_POINT('Ctrl Pts',(0.556668002682986,1.24751201767715,2.12031329508312));
#3584=CARTESIAN_POINT('Ctrl Pts',(0.569854819316886,1.24154378003136,2.11932436406474));
#3585=CARTESIAN_POINT('Ctrl Pts',(0.593859806606356,1.23021633044349,2.11749791709684));
#3586=CARTESIAN_POINT('Ctrl Pts',(0.604706643555955,1.22492103772442,2.11666260873504));
#3587=CARTESIAN_POINT('Ctrl Pts',(0.62677103981207,1.2137849813579,2.11494202027823));
#3588=CARTESIAN_POINT('Ctrl Pts',(0.637980473502349,1.20793079840907,2.11405634321333));
#3589=CARTESIAN_POINT('Ctrl Pts',(0.666331983982746,1.1926193596651,2.11178570868848));
#3590=CARTESIAN_POINT('Ctrl Pts',(0.683354470256632,1.18294794796436,2.1103934371967));
#3591=CARTESIAN_POINT('Ctrl Pts',(0.720117365180872,1.16100261430409,2.10732085922092));
#3592=CARTESIAN_POINT('Ctrl Pts',(0.739763900960852,1.14858406307028,2.10563590447739));
#3593=CARTESIAN_POINT('Ctrl Pts',(0.799941240925523,1.10836149643084,2.1003386900016));
#3594=CARTESIAN_POINT('Ctrl Pts',(0.839292191643858,1.07886932698377,2.09667432428138));
#3595=CARTESIAN_POINT('Ctrl Pts',(0.93590657008881,0.997970288377145,2.08718673582138));
#3596=CARTESIAN_POINT('Ctrl Pts',(0.990576504683026,0.943728996559882,2.08132325813323));
#3597=CARTESIAN_POINT('Ctrl Pts',(1.05780724003935,0.864709174676084,2.07362556634221));
#3598=CARTESIAN_POINT('Ctrl Pts',(1.07461422450469,0.843731358375023,2.07165392307157));
#3599=CARTESIAN_POINT('Ctrl Pts',(1.09684394004442,0.814242244173363,2.06899307832166));
#3600=CARTESIAN_POINT('Ctrl Pts',(1.10280676645812,0.80614782283621,2.06827374192052));
#3601=CARTESIAN_POINT('Ctrl Pts',(1.11265026385836,0.792471818039264,2.06707770370535));
#3602=CARTESIAN_POINT('Ctrl Pts',(1.11657953952223,0.786925874766503,2.06659792118672));
#3603=CARTESIAN_POINT('Ctrl Pts',(1.12479782640733,0.775140737694921,2.06558970669665));
#3604=CARTESIAN_POINT('Ctrl Pts',(1.12907661791458,0.768894863678611,2.06506191852614));
#3605=CARTESIAN_POINT('Ctrl Pts',(1.1408419043936,0.751410727626345,2.0636016142575));
#3606=CARTESIAN_POINT('Ctrl Pts',(1.14821425047003,0.740096211247739,2.06267608071435));
#3607=CARTESIAN_POINT('Ctrl Pts',(1.16469870091291,0.713957721894388,2.06057753315102));
#3608=CARTESIAN_POINT('Ctrl Pts',(1.17369791628639,0.699065055835065,2.05941030763603));
#3609=CARTESIAN_POINT('Ctrl Pts',(1.20368982138575,0.647219226519583,2.05542921262411));
#3610=CARTESIAN_POINT('Ctrl Pts',(1.22324238701773,0.609459147245914,2.05267040547807));
#3611=CARTESIAN_POINT('Ctrl Pts',(1.28608220616754,0.472847241513493,2.04297108349625));
#3612=CARTESIAN_POINT('Ctrl Pts',(1.31939023804453,0.369863666238663,2.03612735561043));
#3613=CARTESIAN_POINT('Ctrl Pts',(1.34418640305466,0.244000036540371,2.02749642267661));
#3614=CARTESIAN_POINT('Ctrl Pts',(1.34768398674082,0.223876983283783,2.02611004107536));
#3615=CARTESIAN_POINT('Ctrl Pts',(1.35263989307281,0.19101191331196,2.02383115205553));
#3616=CARTESIAN_POINT('Ctrl Pts',(1.35437229793197,0.178314022947975,2.02294715344436));
#3617=CARTESIAN_POINT('Ctrl Pts',(1.35739432598119,0.15356888944215,2.02121667279309));
#3618=CARTESIAN_POINT('Ctrl Pts',(1.35870283040466,0.141525128568418,2.02037085937764));
#3619=CARTESIAN_POINT('Ctrl Pts',(1.3614345349831,0.112832543907044,2.01834658679157));
#3620=CARTESIAN_POINT('Ctrl Pts',(1.36271274832917,0.0961722290341604,2.01716380373507));
#3621=CARTESIAN_POINT('Ctrl Pts',(1.36624012099508,0.0356611486721819,2.01283905959066));
#3622=CARTESIAN_POINT('Ctrl Pts',(1.36668019520095,-0.00826405532143513,
2.0096438025234));
#3623=CARTESIAN_POINT('Ctrl Pts',(1.36253159718782,-0.116893027612649,2.00160497196603));
#3624=CARTESIAN_POINT('Ctrl Pts',(1.35545257246667,-0.18139297887735,1.99670816699871));
#3625=CARTESIAN_POINT('Ctrl Pts',(1.33226378488829,-0.308510002733987,1.98693412446569));
#3626=CARTESIAN_POINT('Ctrl Pts',(1.31623518861522,-0.370987323090179,1.98206955718731));
#3627=CARTESIAN_POINT('Ctrl Pts',(1.29114996346084,-0.446216374935332,1.97628713545863));
#3628=CARTESIAN_POINT('Ctrl Pts',(1.28621396616711,-0.460250975101351,1.97521191144228));
#3629=CARTESIAN_POINT('Ctrl Pts',(1.27829270220742,-0.481650110489766,1.97358076019292));
#3630=CARTESIAN_POINT('Ctrl Pts',(1.27547098753056,-0.489073439714652,1.97301646647839));
#3631=CARTESIAN_POINT('Ctrl Pts',(1.27037395959123,-0.502138425591383,1.97202657597735));
#3632=CARTESIAN_POINT('Ctrl Pts',(1.26812556170161,-0.50778987546991,1.97159951783793));
#3633=CARTESIAN_POINT('Ctrl Pts',(1.26249291896948,-0.5216770070138,1.97055269496694));
#3634=CARTESIAN_POINT('Ctrl Pts',(1.25906578646912,-0.529894920079635,1.96993541218426));
#3635=CARTESIAN_POINT('Ctrl Pts',(1.24741206366561,-0.557087821974397,1.9678982489885));
#3636=CARTESIAN_POINT('Ctrl Pts',(1.23883453041687,-0.575910422932184,1.96649696448957));
#3637=CARTESIAN_POINT('Ctrl Pts',(1.1791187654265,-0.699436755686919,1.95731286834299));
#3638=CARTESIAN_POINT('Ctrl Pts',(1.11518736998412,-0.797430738654654,1.95004864461582));
#3639=CARTESIAN_POINT('Ctrl Pts',(1.00940672473423,-0.92153037274044,1.93940772411775));
#3640=CARTESIAN_POINT('Ctrl Pts',(0.977442641931367,-0.955366619199421,
1.93633043647606));
#3641=CARTESIAN_POINT('Ctrl Pts',(0.931242315930409,-0.999523050843923,
1.93200558113118));
#3642=CARTESIAN_POINT('Ctrl Pts',(0.918439378901246,-1.01129997608506,1.93081916804241));
#3643=CARTESIAN_POINT('Ctrl Pts',(0.896348343538204,-1.03085512212222,1.92878967321063));
#3644=CARTESIAN_POINT('Ctrl Pts',(0.887175099203037,-1.0387603009385,1.92795188824321));
#3645=CARTESIAN_POINT('Ctrl Pts',(0.868256268483771,-1.05463047490952,1.92623324085248));
#3646=CARTESIAN_POINT('Ctrl Pts',(0.85850329609829,-1.06258480049047,1.92535206451859));
#3647=CARTESIAN_POINT('Ctrl Pts',(0.833541829727616,-1.08237487111844,1.92310800227951));
#3648=CARTESIAN_POINT('Ctrl Pts',(0.818190646494332,-1.09402529331905,1.9217381426185));
#3649=CARTESIAN_POINT('Ctrl Pts',(0.737215259425626,-1.15282201073183,1.91456074679416));
#3650=CARTESIAN_POINT('Ctrl Pts',(0.667759053286836,-1.19439474762756,1.90855192537885));
#3651=CARTESIAN_POINT('Ctrl Pts',(0.514672635122422,-1.26847996067337,1.89571792024527));
#3652=CARTESIAN_POINT('Ctrl Pts',(0.430671548381346,-1.2994050498778,1.88890298774178));
#3653=CARTESIAN_POINT('Ctrl Pts',(0.33118371819476,-1.32531340024732,1.88143033263445));
#3654=CARTESIAN_POINT('Ctrl Pts',(0.318068581770678,-1.32852198938294,1.8804571541798));
#3655=CARTESIAN_POINT('Ctrl Pts',(0.297528369967677,-1.33322547777744,1.87895371608838));
#3656=CARTESIAN_POINT('Ctrl Pts',(0.29013517412984,-1.33485388462334,1.87841672826287));
#3657=CARTESIAN_POINT('Ctrl Pts',(0.276002095612671,-1.3378438302344,1.87739860379967));
#3658=CARTESIAN_POINT('Ctrl Pts',(0.269264930201854,-1.33921606561981,1.87691694877503));
#3659=CARTESIAN_POINT('Ctrl Pts',(0.252587846850224,-1.34248194024522,1.87573319782721));
#3660=CARTESIAN_POINT('Ctrl Pts',(0.242636466012541,-1.34431616114968,1.87503427881584));
#3661=CARTESIAN_POINT('Ctrl Pts',(0.203548499834071,-1.35107258249412,1.87231481683694));
#3662=CARTESIAN_POINT('Ctrl Pts',(0.174273649232726,-1.3551598059289,1.87033407557648));
#3663=CARTESIAN_POINT('Ctrl Pts',(0.0897290340902734,-1.36417803532848,
1.86471508731536));
#3664=CARTESIAN_POINT('Ctrl Pts',(0.0342603580363892,-1.3666967555137,1.86115068860117));
#3665=CARTESIAN_POINT('Ctrl Pts',(-0.10669439680372,-1.36450779035077,1.8520885067005));
#3666=CARTESIAN_POINT('Ctrl Pts',(-0.191855490701469,-1.35515853224204,
1.84659830138456));
#3667=CARTESIAN_POINT('Ctrl Pts',(-0.297540023977596,-1.33338990611254,
1.83936273782924));
#3668=CARTESIAN_POINT('Ctrl Pts',(-0.319384360919034,-1.3283268587274,1.83784479470394));
#3669=CARTESIAN_POINT('Ctrl Pts',(-0.353893108402389,-1.31942805768302,
1.83540545402121));
#3670=CARTESIAN_POINT('Ctrl Pts',(-0.366644000952135,-1.31594182516014,
1.83449504132481));
#3671=CARTESIAN_POINT('Ctrl Pts',(-0.390841585417997,-1.30894696148159,
1.83274891106145));
#3672=CARTESIAN_POINT('Ctrl Pts',(-0.402296723615491,-1.30547180092407,
1.83191433139074));
#3673=CARTESIAN_POINT('Ctrl Pts',(-0.428682435290027,-1.2970868770445,1.82997273787605));
#3674=CARTESIAN_POINT('Ctrl Pts',(-0.443576632824335,-1.29206916655532,
1.82886234918674));
#3675=CARTESIAN_POINT('Ctrl Pts',(-0.492803179493639,-1.27453376204648,
1.82514261085172));
#3676=CARTESIAN_POINT('Ctrl Pts',(-0.526716979709552,-1.26089653513326,
1.82249796109589));
#3677=CARTESIAN_POINT('Ctrl Pts',(-0.611624981139666,-1.22273032771862,
1.81566225591028));
#3678=CARTESIAN_POINT('Ctrl Pts',(-0.661714782062654,-1.19636409239602,
1.8114224311337));
#3679=CARTESIAN_POINT('Ctrl Pts',(-0.782157752281162,-1.12308283669411,
1.8007736761182));
#3680=CARTESIAN_POINT('Ctrl Pts',(-0.850073213613315,-1.07259657094254,
1.79434174313261));
#3681=CARTESIAN_POINT('Ctrl Pts',(-0.923271613869274,-1.00683667542334,
1.78718261223841));
#3682=CARTESIAN_POINT('Ctrl Pts',(-0.933505027874658,-0.997355987145639,
1.7861763389394));
#3683=CARTESIAN_POINT('Ctrl Pts',(-0.949132816127487,-0.982426393510283,
1.78463351231115));
#3684=CARTESIAN_POINT('Ctrl Pts',(-0.954629256730586,-0.97708633742299,
1.78408967904563));
#3685=CARTESIAN_POINT('Ctrl Pts',(-0.964945353656844,-0.966893599539856,
1.78306716901225));
#3686=CARTESIAN_POINT('Ctrl Pts',(-0.969773735305371,-0.962050764145826,
1.78258788341687));
#3687=CARTESIAN_POINT('Ctrl Pts',(-0.98150052794822,-0.950110865921041,
1.7814215923595));
#3688=CARTESIAN_POINT('Ctrl Pts',(-0.988358551429485,-0.942974725167201,
1.78073755931147));
#3689=CARTESIAN_POINT('Ctrl Pts',(-1.01410505193649,-0.915594609311967,
1.77815902620023));
#3690=CARTESIAN_POINT('Ctrl Pts',(-1.03245537780718,-0.894851206236809,
1.77629924919481));
#3691=CARTESIAN_POINT('Ctrl Pts',(-1.08183620700637,-0.835487454907541,
1.77118408703859));
#3692=CARTESIAN_POINT('Ctrl Pts',(-1.11141654365469,-0.79571525891398,1.76798778719929));
#3693=CARTESIAN_POINT('Ctrl Pts',(-1.19099869846004,-0.675588849510802,
1.75871704552248));
#3694=CARTESIAN_POINT('Ctrl Pts',(-1.23489246943862,-0.591554385658636,
1.75267571229501));
#3695=CARTESIAN_POINT('Ctrl Pts',(-1.27787244972568,-0.483200453657775,
1.74485407883813));
#3696=CARTESIAN_POINT('Ctrl Pts',(-1.28549353671963,-0.462544002193186,
1.74336282867914));
#3697=CARTESIAN_POINT('Ctrl Pts',(-1.29685978183979,-0.42928228733208,1.7409560722325));
#3698=CARTESIAN_POINT('Ctrl Pts',(-1.30092806094247,-0.416790997567367,
1.74005102802091));
#3699=CARTESIAN_POINT('Ctrl Pts',(-1.30836446014995,-0.392787810577541,
1.73830858894257));
#3700=CARTESIAN_POINT('Ctrl Pts',(-1.31176236794827,-0.381286373525596,
1.73747224168596));
#3701=CARTESIAN_POINT('Ctrl Pts',(-1.31930882341895,-0.354446978648465,
1.73551649844034));
#3702=CARTESIAN_POINT('Ctrl Pts',(-1.32334199571494,-0.339078688235434,
1.73439356533218));
#3703=CARTESIAN_POINT('Ctrl Pts',(-1.33128787542859,-0.306496525143005,
1.73200531088562));
#3704=CARTESIAN_POINT('Ctrl Pts',(-1.33513677488205,-0.289270235209399,
1.73073824013441));
#3705=CARTESIAN_POINT('Ctrl Pts',(-1.35691669726328,-0.182070234890282,
1.72282413030013));
#3706=CARTESIAN_POINT('Ctrl Pts',(-1.36607590322703,-0.0905701796946844,
1.71591966835577));
#3707=CARTESIAN_POINT('Ctrl Pts',(-1.36599952626833,0.00113764436645534,
1.70898239201339));
#3708=CARTESIAN_POINT('Ctrl Pts',(-1.3659995257529,0.0011382630833804,1.70898234521029));
#3709=CARTESIAN_POINT('Ctrl Pts',(-1.36595693287914,0.0522528482884494,
1.70511576125377));
#3710=CARTESIAN_POINT('Ctrl Pts',(-1.3630453716916,0.103328490601572,1.7012522683266));
#3711=CARTESIAN_POINT('Ctrl Pts',(-1.35497227647164,0.174423345397627,1.69595591105718));
#3712=CARTESIAN_POINT('Ctrl Pts',(-1.35221197745924,0.194669563579413,1.69445721974636));
#3713=CARTESIAN_POINT('Ctrl Pts',(-1.34761071158863,0.22356030720678,1.69233895204357));
#3714=CARTESIAN_POINT('Ctrl Pts',(-1.34613862569921,0.23225987857602,1.69170376025564));
#3715=CARTESIAN_POINT('Ctrl Pts',(-1.34341679380799,0.247448943861795,1.69060008469709));
#3716=CARTESIAN_POINT('Ctrl Pts',(-1.34220407200252,0.253944669891001,1.69012980489682));
#3717=CARTESIAN_POINT('Ctrl Pts',(-1.33978587019547,0.266395827545442,1.68923198103947));
#3718=CARTESIAN_POINT('Ctrl Pts',(-1.33858772032088,0.272352409878506,1.68880408888295));
#3719=CARTESIAN_POINT('Ctrl Pts',(-1.33572378177384,0.286114794282151,1.68781930928704));
#3720=CARTESIAN_POINT('Ctrl Pts',(-1.3340292749263,0.293914270507637,1.68726400184207));
#3721=CARTESIAN_POINT('Ctrl Pts',(-1.32893890762142,0.316392742440755,1.68567046807468));
#3722=CARTESIAN_POINT('Ctrl Pts',(-1.3253683206518,0.331031492042125,1.68464122020308));
#3723=CARTESIAN_POINT('Ctrl Pts',(-1.30471599541868,0.410002854434877,1.67912016892745));
#3724=CARTESIAN_POINT('Ctrl Pts',(-1.28318990128706,0.473087605192201,1.67482071080976));
#3725=CARTESIAN_POINT('Ctrl Pts',(-1.23091908741703,0.596061690347427,1.66622291499242));
#3726=CARTESIAN_POINT('Ctrl Pts',(-1.20018524352135,0.655748556398573,1.66193505481183));
#3727=CARTESIAN_POINT('Ctrl Pts',(-1.15937133142569,0.722453179462495,1.65680265936874));
#3728=CARTESIAN_POINT('Ctrl Pts',(-1.15343259859728,0.731897302581674,1.65606772423466));
#3729=CARTESIAN_POINT('Ctrl Pts',(-1.14737959979828,0.741266520198191,1.65532966579394));
#3730=CARTESIAN_POINT('Ctrl Pts',(-1.14737969890454,0.741266366795177,1.5357812853031));
#3731=CARTESIAN_POINT('Ctrl Pts',(-1.15979031477089,0.722056418342358,1.5372558641891));
#3732=CARTESIAN_POINT('Ctrl Pts',(-1.1717242941471,0.702525830968656,1.53873610928852));
#3733=CARTESIAN_POINT('Ctrl Pts',(-1.20824692153093,0.639228700555636,1.54349469650132));
#3734=CARTESIAN_POINT('Ctrl Pts',(-1.23090890831737,0.594421062350722,1.54680746498365));
#3735=CARTESIAN_POINT('Ctrl Pts',(-1.25804092835754,0.532533451947612,1.55138029053075));
#3736=CARTESIAN_POINT('Ctrl Pts',(-1.26472291715757,0.516463698455412,1.55256722146124));
#3737=CARTESIAN_POINT('Ctrl Pts',(-1.27557475575496,0.488891203635803,1.55460551483191));
#3738=CARTESIAN_POINT('Ctrl Pts',(-1.2799005024791,0.477451833649006,1.55545166685833));
#3739=CARTESIAN_POINT('Ctrl Pts',(-1.28786502986081,0.455503364289027,1.55707687422918));
#3740=CARTESIAN_POINT('Ctrl Pts',(-1.29153022593086,0.445004845606531,1.55785499034693));
#3741=CARTESIAN_POINT('Ctrl Pts',(-1.30081750221069,0.417320918145946,1.55990938125595));
#3742=CARTESIAN_POINT('Ctrl Pts',(-1.30622708055654,0.400067095944435,1.56119234504403));
#3743=CARTESIAN_POINT('Ctrl Pts',(-1.32640781953353,0.330921444893526,1.56634670456232));
#3744=CARTESIAN_POINT('Ctrl Pts',(-1.33843989490008,0.278287707039891,1.57030129942558));
#3745=CARTESIAN_POINT('Ctrl Pts',(-1.35980639277899,0.150391449871338,1.57996896313017));
#3746=CARTESIAN_POINT('Ctrl Pts',(-1.3660513788397,0.0747903911061498,1.58573562827326));
#3747=CARTESIAN_POINT('Ctrl Pts',(-1.36596814699086,-0.0471228114460157,
1.5949077998794));
#3748=CARTESIAN_POINT('Ctrl Pts',(-1.36359378446912,-0.093286560033794,
1.59834890468488));
#3749=CARTESIAN_POINT('Ctrl Pts',(-1.35768994075569,-0.150901693767822,
1.60254126649432));
#3750=CARTESIAN_POINT('Ctrl Pts',(-1.35634553152681,-0.162542668533079,
1.60338298691338));
#3751=CARTESIAN_POINT('Ctrl Pts',(-1.35393456769329,-0.181297817321447,
1.60472900977372));
#3752=CARTESIAN_POINT('Ctrl Pts',(-1.35296136370907,-0.188423105242078,
1.60523801726153));
#3753=CARTESIAN_POINT('Ctrl Pts',(-1.35091333127309,-0.202582827722728,
1.60624440608073));
#3754=CARTESIAN_POINT('Ctrl Pts',(-1.349839720395,-0.209617187246116,1.6067418269699));
#3755=CARTESIAN_POINT('Ctrl Pts',(-1.34690926396758,-0.22786074443878,1.60802603585138));
#3756=CARTESIAN_POINT('Ctrl Pts',(-1.34496740682321,-0.239056018908052,
1.60880835094565));
#3757=CARTESIAN_POINT('Ctrl Pts',(-1.33488735099321,-0.293152531990371,
1.61256639565084));
#3758=CARTESIAN_POINT('Ctrl Pts',(-1.32483415674441,-0.335675293826939,
1.61545300977587));
#3759=CARTESIAN_POINT('Ctrl Pts',(-1.29720218521854,-0.431728235621065,
1.62196671830796));
#3760=CARTESIAN_POINT('Ctrl Pts',(-1.278317043785,-0.484797597008448,1.62556201686632));
#3761=CARTESIAN_POINT('Ctrl Pts',(-1.22705392118097,-0.604818252505102,
1.63396583960278));
#3762=CARTESIAN_POINT('Ctrl Pts',(-1.19238366608627,-0.670586107108913,
1.63878585909729));
#3763=CARTESIAN_POINT('Ctrl Pts',(-1.14224300219914,-0.749403340349715,
1.64508482906809));
#3764=CARTESIAN_POINT('Ctrl Pts',(-1.13160028901366,-0.765379100782187,
1.64639017719041));
#3765=CARTESIAN_POINT('Ctrl Pts',(-1.11343816456112,-0.791435029837025,
1.64857052428237));
#3766=CARTESIAN_POINT('Ctrl Pts',(-1.10610966856757,-0.801645392745407,
1.64943841575736));
#3767=CARTESIAN_POINT('Ctrl Pts',(-1.09135809452728,-0.821610448686908,
1.6511632701297));
#3768=CARTESIAN_POINT('Ctrl Pts',(-1.08394252640595,-0.831369233295349,
1.65201989161256));
#3769=CARTESIAN_POINT('Ctrl Pts',(-1.06559023157837,-0.85485761231133,1.65411570260013));
#3770=CARTESIAN_POINT('Ctrl Pts',(-1.05451850304957,-0.868478413569991,
1.65536005491605));
#3771=CARTESIAN_POINT('Ctrl Pts',(-1.00981571073322,-0.921357861067739,
1.66030955055087));
#3772=CARTESIAN_POINT('Ctrl Pts',(-0.974233787236853,-0.958903249182929,
1.66409099710995));
#3773=CARTESIAN_POINT('Ctrl Pts',(-0.86947134803995,-1.05758388555974,1.6747998885656));
#3774=CARTESIAN_POINT('Ctrl Pts',(-0.796100854592957,-1.11386079793027,
1.68185536036118));
#3775=CARTESIAN_POINT('Ctrl Pts',(-0.688055432984376,-1.18056902493645,
1.69134361628397));
#3776=CARTESIAN_POINT('Ctrl Pts',(-0.657799232249098,-1.19769115466372,
1.69391094670888));
#3777=CARTESIAN_POINT('Ctrl Pts',(-0.617215340032979,-1.21865521971508,
1.6972105420373));
#3778=CARTESIAN_POINT('Ctrl Pts',(-0.607450113423378,-1.22355208291806,
1.69799384868198));
#3779=CARTESIAN_POINT('Ctrl Pts',(-0.591933664871887,-1.23110138521432,
1.69922060515191));
#3780=CARTESIAN_POINT('Ctrl Pts',(-0.5862211854455,-1.23383175928202,1.69966846371098));
#3781=CARTESIAN_POINT('Ctrl Pts',(-0.574064970579749,-1.23953853707716,
1.70061320573431));
#3782=CARTESIAN_POINT('Ctrl Pts',(-0.56761659623023,-1.24250463980213,1.70110943454097));
#3783=CARTESIAN_POINT('Ctrl Pts',(-0.550864806079229,-1.25005244223705,
1.70238661142853));
#3784=CARTESIAN_POINT('Ctrl Pts',(-0.540526990564212,-1.25455718734628,
1.70316317937415));
#3785=CARTESIAN_POINT('Ctrl Pts',(-0.491066587832421,-1.27538485387955,
1.70682919735454));
#3786=CARTESIAN_POINT('Ctrl Pts',(-0.451250238748048,-1.29001041934034,
1.70963477203816));
#3787=CARTESIAN_POINT('Ctrl Pts',(-0.309549525402229,-1.33469447777594,
1.71932757039139));
#3788=CARTESIAN_POINT('Ctrl Pts',(-0.204908935915653,-1.35471155272163,
1.72599961104273));
#3789=CARTESIAN_POINT('Ctrl Pts',(-0.0643910851198161,-1.36492277259684,
1.73529798285556));
#3790=CARTESIAN_POINT('Ctrl Pts',(-0.0296973215127461,-1.3661179093773,
1.73761756356733));
#3791=CARTESIAN_POINT('Ctrl Pts',(0.0202710338553627,-1.36593492724722,
1.74101450183231));
#3792=CARTESIAN_POINT('Ctrl Pts',(0.0355373115934018,-1.36562301102716,
1.74205980144477));
#3793=CARTESIAN_POINT('Ctrl Pts',(0.0627315591294048,-1.36461109424488,
1.74393681762103));
#3794=CARTESIAN_POINT('Ctrl Pts',(0.0746617843607647,-1.36401036991554,
1.74476542036769));
#3795=CARTESIAN_POINT('Ctrl Pts',(0.0998639783399317,-1.36240974050904,
1.74652745720307));
#3796=CARTESIAN_POINT('Ctrl Pts',(0.113132211796685,-1.36137217382533,1.74746196279611));
#3797=CARTESIAN_POINT('Ctrl Pts',(0.14916468594926,-1.35802407697473,1.75001942433337));
#3798=CARTESIAN_POINT('Ctrl Pts',(0.171888533606348,-1.35533527872778,1.75165371562096));
#3799=CARTESIAN_POINT('Ctrl Pts',(0.222848432821054,-1.34800331518345,1.75536924942726));
#3800=CARTESIAN_POINT('Ctrl Pts',(0.251027081363046,-1.34304116417229,1.75745908610927));
#3801=CARTESIAN_POINT('Ctrl Pts',(0.349556602605851,-1.32248142442519,1.76488895904059));
#3802=CARTESIAN_POINT('Ctrl Pts',(0.418805312692536,-1.30220863972253,1.77034067748926));
#3803=CARTESIAN_POINT('Ctrl Pts',(0.541995075039818,-1.25529732381879,1.78030824375599));
#3804=CARTESIAN_POINT('Ctrl Pts',(0.596412708914412,-1.23037522250698,1.78481280426713));
#3805=CARTESIAN_POINT('Ctrl Pts',(0.662110654960098,-1.19490024581714,1.79025703076469));
#3806=CARTESIAN_POINT('Ctrl Pts',(0.675079453394635,-1.18762152804031,1.79133184612928));
#3807=CARTESIAN_POINT('Ctrl Pts',(0.69478593584553,-1.17613414455211,1.79296241947197));
#3808=CARTESIAN_POINT('Ctrl Pts',(0.701609658132619,-1.17207632782718,1.79352653769146));
#3809=CARTESIAN_POINT('Ctrl Pts',(0.713596933441673,-1.16480573107767,1.7945161320364));
#3810=CARTESIAN_POINT('Ctrl Pts',(0.718774762820622,-1.1616177586051,1.79494306854411));
#3811=CARTESIAN_POINT('Ctrl Pts',(0.731479386535359,-1.1536780872011,1.79598958265653));
#3812=CARTESIAN_POINT('Ctrl Pts',(0.738981301846574,-1.14888723041647,1.79660667987652));
#3813=CARTESIAN_POINT('Ctrl Pts',(0.763749689625065,-1.13272670273973,1.7986431244583));
#3814=CARTESIAN_POINT('Ctrl Pts',(0.780805734832701,-1.12103786147678,1.80004388997056));
#3815=CARTESIAN_POINT('Ctrl Pts',(0.892143391326122,-1.04096152236886,1.80922410355532));
#3816=CARTESIAN_POINT('Ctrl Pts',(0.977618909325426,-0.961138804459532,
1.81648530253784));
#3817=CARTESIAN_POINT('Ctrl Pts',(1.08164744551156,-0.83556217078932,1.82712605079926));
#3818=CARTESIAN_POINT('Ctrl Pts',(1.10950380236102,-0.798201716139281,1.83020690364902));
#3819=CARTESIAN_POINT('Ctrl Pts',(1.1450686222001,-0.745034559755364,1.83453561316257));
#3820=CARTESIAN_POINT('Ctrl Pts',(1.15446366260434,-0.730391847358991,1.83572214500001));
#3821=CARTESIAN_POINT('Ctrl Pts',(1.16991844935883,-0.705261231545455,1.8377516054818));
#3822=CARTESIAN_POINT('Ctrl Pts',(1.17612315953832,-0.694864648806059,1.83858923352938));
#3823=CARTESIAN_POINT('Ctrl Pts',(1.18849137527153,-0.673500187716444,1.84030734340655));
#3824=CARTESIAN_POINT('Ctrl Pts',(1.19464317604421,-0.662526916569924,1.84118813647998));
#3825=CARTESIAN_POINT('Ctrl Pts',(1.20982561328582,-0.634546101434539,1.84343074348033));
#3826=CARTESIAN_POINT('Ctrl Pts',(1.21864953639005,-0.617430166024213,1.84479951679691));
#3827=CARTESIAN_POINT('Ctrl Pts',(1.26240783761792,-0.52795654813841,1.85194305323672));
#3828=CARTESIAN_POINT('Ctrl Pts',(1.29126466282779,-0.452817109349181,1.85791664565611));
#3829=CARTESIAN_POINT('Ctrl Pts',(1.33807042273222,-0.289148431385013,1.8707611013959));
#3830=CARTESIAN_POINT('Ctrl Pts',(1.35419800661244,-0.20047237521511,1.87762446816413));
#3831=CARTESIAN_POINT('Ctrl Pts',(1.36258439726296,-0.0974680645364525,
1.88513511386748));
#3832=CARTESIAN_POINT('Ctrl Pts',(1.36347662556989,-0.0840701443760326,
1.88610280800168));
#3833=CARTESIAN_POINT('Ctrl Pts',(1.36456192063752,-0.0631174811284687,
1.88759961860249));
#3834=CARTESIAN_POINT('Ctrl Pts',(1.36489007738468,-0.0555709935379551,
1.88813537441347));
#3835=CARTESIAN_POINT('Ctrl Pts',(1.36539748947144,-0.0411464116040726,
1.88915255846849));
#3836=CARTESIAN_POINT('Ctrl Pts',(1.36558740485288,-0.0342691310991905,
1.88963448772472));
#3837=CARTESIAN_POINT('Ctrl Pts',(1.36592892455662,-0.0172405652041577,
1.89082081033994));
#3838=CARTESIAN_POINT('Ctrl Pts',(1.36601933983523,-0.00708822082055721,
1.89152199185013));
#3839=CARTESIAN_POINT('Ctrl Pts',(1.36592957592852,0.0329230015985243,1.89426470334038));
#3840=CARTESIAN_POINT('Ctrl Pts',(1.36488361542284,0.0627737554192573,1.89626555151596));
#3841=CARTESIAN_POINT('Ctrl Pts',(1.35902933441631,0.148964591954679,1.90197259659998));
#3842=CARTESIAN_POINT('Ctrl Pts',(1.35170167793814,0.205072090262172,1.90560218676086));
#3843=CARTESIAN_POINT('Ctrl Pts',(1.32489148691063,0.343041396830687,1.91463695028003));
#3844=CARTESIAN_POINT('Ctrl Pts',(1.30129239579022,0.423852524379415,1.92003701397138));
#3845=CARTESIAN_POINT('Ctrl Pts',(1.26217639524908,0.522848184741809,1.92717449023204));
#3846=CARTESIAN_POINT('Ctrl Pts',(1.25341822028006,0.543509105631328,1.92869355971991));
#3847=CARTESIAN_POINT('Ctrl Pts',(1.23869791154941,0.575984587447113,1.93113411475356));
#3848=CARTESIAN_POINT('Ctrl Pts',(1.23306590808666,0.587944900843358,1.93204459117415));
#3849=CARTESIAN_POINT('Ctrl Pts',(1.22200704329029,0.610571838066217,1.93379045723406));
#3850=CARTESIAN_POINT('Ctrl Pts',(1.2166118329917,0.621252617789063,1.93462470437699));
#3851=CARTESIAN_POINT('Ctrl Pts',(1.20381411363676,0.645781793014084,1.93656493148445));
#3852=CARTESIAN_POINT('Ctrl Pts',(1.19631187273207,0.659575932750349,1.9376742749992));
#3853=CARTESIAN_POINT('Ctrl Pts',(1.17060348511937,0.704963080259483,1.94138719796597));
#3854=CARTESIAN_POINT('Ctrl Pts',(1.15137173673887,0.735953908320155,1.9440259052185));
#3855=CARTESIAN_POINT('Ctrl Pts',(1.09931637092046,0.812794978268084,1.95084060671881));
#3856=CARTESIAN_POINT('Ctrl Pts',(1.0648532977811,0.857448858384555,1.95506497107772));
#3857=CARTESIAN_POINT('Ctrl Pts',(0.97198001816735,0.963521857650683,1.96571313500633));
#3858=CARTESIAN_POINT('Ctrl Pts',(0.910424313975098,1.02188509508412,1.97216107519307));
#3859=CARTESIAN_POINT('Ctrl Pts',(0.832965640074657,1.0827354817752,1.9793286607213));
#3860=CARTESIAN_POINT('Ctrl Pts',(0.821942712968765,1.0911269838918,1.9803281836888));
#3861=CARTESIAN_POINT('Ctrl Pts',(0.804579128565239,1.10393299191961,1.98186880073366));
#3862=CARTESIAN_POINT('Ctrl Pts',(0.798325792568124,1.10846360387413,1.98241696122259));
#3863=CARTESIAN_POINT('Ctrl Pts',(0.786480772432027,1.11689321525958,1.98344228041507));
#3864=CARTESIAN_POINT('Ctrl Pts',(0.780898070023141,1.12080358050575,1.9839201165184));
#3865=CARTESIAN_POINT('Ctrl Pts',(0.767249847624264,1.13021190000869,1.98507567572538));
#3866=CARTESIAN_POINT('Ctrl Pts',(0.759154260638993,1.13566548340149,1.98575056024861));
#3867=CARTESIAN_POINT('Ctrl Pts',(0.728766168739874,1.15566621548915,1.98824761649419));
#3868=CARTESIAN_POINT('Ctrl Pts',(0.706106970783736,1.16964853497552,1.99003782705513));
#3869=CARTESIAN_POINT('Ctrl Pts',(0.642893686895688,1.20614844093588,1.99488014891978));
#3870=CARTESIAN_POINT('Ctrl Pts',(0.601578013534652,1.2272778063075,1.99788046743877));
#3871=CARTESIAN_POINT('Ctrl Pts',(0.467865890469464,1.2872814860074,2.0073183310386));
#3872=CARTESIAN_POINT('Ctrl Pts',(0.372241759951797,1.31811454171755,2.01369950851955));
#3873=CARTESIAN_POINT('Ctrl Pts',(0.253102911053024,1.34251805575169,2.02186737679989));
#3874=CARTESIAN_POINT('Ctrl Pts',(0.231998414634837,1.34632554247638,2.0233209684485));
#3875=CARTESIAN_POINT('Ctrl Pts',(0.19795103780313,1.35164376901594,2.02568160787958));
#3876=CARTESIAN_POINT('Ctrl Pts',(0.185060443848407,1.35346891495904,2.0265789113278));
#3877=CARTESIAN_POINT('Ctrl Pts',(0.160216336675511,1.35662498191178,2.02831610033631));
#3878=CARTESIAN_POINT('Ctrl Pts',(0.148267424505036,1.35798283150136,2.02915506856913));
#3879=CARTESIAN_POINT('Ctrl Pts',(0.120237313492564,1.36079376586956,2.03113198252251));
#3880=CARTESIAN_POINT('Ctrl Pts',(0.104145496440448,1.36211980409619,2.03227371218323));
#3881=CARTESIAN_POINT('Ctrl Pts',(0.0485481285201941,1.36571034984221,2.03624365673629));
#3882=CARTESIAN_POINT('Ctrl Pts',(0.00897336138771308,1.36654330793505,
2.0391141343248));
#3883=CARTESIAN_POINT('Ctrl Pts',(-0.0953385835039811,1.36420765506473,
2.04679903771023));
#3884=CARTESIAN_POINT('Ctrl Pts',(-0.159907984497101,1.35815315521377,2.0516805162905));
#3885=CARTESIAN_POINT('Ctrl Pts',(-0.293053759337824,1.33604046037419,2.06188999303428));
#3886=CARTESIAN_POINT('Ctrl Pts',(-0.361325348218605,1.3192157736059,2.067206460136));
#3887=CARTESIAN_POINT('Ctrl Pts',(-0.442124991239913,1.29255659660808,2.07341046631218));
#3888=CARTESIAN_POINT('Ctrl Pts',(-0.456168240006155,1.28766752133638,2.07448514832784));
#3889=CARTESIAN_POINT('Ctrl Pts',(-0.477582906572202,1.27981779329343,2.07611556313191));
#3890=CARTESIAN_POINT('Ctrl Pts',(-0.485012534794449,1.27702069904108,2.07667965378334));
#3891=CARTESIAN_POINT('Ctrl Pts',(-0.498089499043235,1.27196691244003,2.07766922508382));
#3892=CARTESIAN_POINT('Ctrl Pts',(-0.503746533230021,1.26973714124726,2.07809616572091));
#3893=CARTESIAN_POINT('Ctrl Pts',(-0.517648016565792,1.26415021374995,2.07914272288182));
#3894=CARTESIAN_POINT('Ctrl Pts',(-0.525874841512708,1.2607501314389,2.07975985848602));
#3895=CARTESIAN_POINT('Ctrl Pts',(-0.55309880478091,1.24918582642946,2.08179657972262));
#3896=CARTESIAN_POINT('Ctrl Pts',(-0.571944739123921,1.24067032008993,2.08319757661226));
#3897=CARTESIAN_POINT('Ctrl Pts',(-0.695623101784743,1.18136886689752,2.092378884129));
#3898=CARTESIAN_POINT('Ctrl Pts',(-0.793791368570804,1.11777680002107,2.09964087603822));
#3899=CARTESIAN_POINT('Ctrl Pts',(-0.918239182809894,1.0124034241297,2.11028161895936));
#3900=CARTESIAN_POINT('Ctrl Pts',(-0.952208118340535,0.980521758778849,
2.11336147694505));
#3901=CARTESIAN_POINT('Ctrl Pts',(-0.996540189408266,0.934433651826953,
2.11768905763102));
#3902=CARTESIAN_POINT('Ctrl Pts',(-1.00835835459753,0.921668043105,2.11887550204496));
#3903=CARTESIAN_POINT('Ctrl Pts',(-1.02798277302616,0.899641037135389,2.12090485927624));
#3904=CARTESIAN_POINT('Ctrl Pts',(-1.03591567987304,0.890494955191887,2.12174247284238));
#3905=CARTESIAN_POINT('Ctrl Pts',(-1.05184157065017,0.871632704057748,2.12346059308518));
#3906=CARTESIAN_POINT('Ctrl Pts',(-1.05982396606316,0.861909161563552,2.12434141147899));
#3907=CARTESIAN_POINT('Ctrl Pts',(-1.06844721718715,0.85110404404337,2.12531527796639));
#3908=CARTESIAN_POINT('Ctrl Pts',(-1.06922240375786,0.850129990640251,2.12540302600043));
#3909=CARTESIAN_POINT('Ctrl Pts',(-1.07074439071018,0.848212177559546,2.12557570809491));
#3910=CARTESIAN_POINT('Ctrl Pts',(-1.07149127765662,0.847268487722126,2.12566063868679));
#3911=CARTESIAN_POINT('Ctrl Pts',(-1.07299582710629,0.845362321983506,2.12583210977877));
#3912=CARTESIAN_POINT('Ctrl Pts',(-1.0737534439973,0.84439981164343,2.12591865193961));
#3913=CARTESIAN_POINT('Ctrl Pts',(-1.07531538819257,0.842409946713103,2.12609748159864));
#3914=CARTESIAN_POINT('Ctrl Pts',(-1.0761195399428,0.841382456518589,2.12618977574813));
#3915=CARTESIAN_POINT('Ctrl Pts',(-1.07781382997867,0.839211206101592,2.12638471021053));
#3916=CARTESIAN_POINT('Ctrl Pts',(-1.0787036220003,0.838067178926906,2.12648736366916));
#3917=CARTESIAN_POINT('Ctrl Pts',(-1.08061786038151,0.835597897090972,2.12670880997662));
#3918=CARTESIAN_POINT('Ctrl Pts',(-1.08164169217297,0.834272171121222,2.12682762609339));
#3919=CARTESIAN_POINT('Ctrl Pts',(-1.08388919555604,0.831350861566436,2.12708927897632));
#3920=CARTESIAN_POINT('Ctrl Pts',(-1.08511178592161,0.829754454792491,2.12723215646491));
#3921=CARTESIAN_POINT('Ctrl Pts',(-1.10677711903415,0.801335005219596,2.12977378257878));
#3922=CARTESIAN_POINT('Ctrl Pts',(-1.1262214474394,0.773768885370967,2.13220954871428));
#3923=CARTESIAN_POINT('Ctrl Pts',(-1.14554557903622,0.744099572673573,2.13480218152378));
#3924=CARTESIAN_POINT('Ctrl Pts',(-1.14646391675869,0.742683872827873,2.13492582294454));
#3925=CARTESIAN_POINT('Ctrl Pts',(-1.14737960371854,0.741266514130168,2.135049540568));
#3926=CARTESIAN_POINT('Origin',(0.,0.,-1.10921167016993));
#3927=CARTESIAN_POINT('',(-1.14737960323804,0.741266514873919,2.85523392653093));
#3928=CARTESIAN_POINT('',(-1.1473796034465,0.741266514551254,2.73724103392041));
#3929=CARTESIAN_POINT('',(-1.14737960344596,0.741266514552077,-1.10921167016993));
#3930=CARTESIAN_POINT('Ctrl Pts',(-1.14737960323804,0.741266514873919,2.85523392653093));
#3931=CARTESIAN_POINT('Ctrl Pts',(-1.14653083367509,0.742580294553478,2.85511804770569));
#3932=CARTESIAN_POINT('Ctrl Pts',(-1.14567979272863,0.743892639525033,2.85500210777706));
#3933=CARTESIAN_POINT('Ctrl Pts',(-1.08129912223108,0.842798095947521,2.84625010182325));
#3934=CARTESIAN_POINT('Ctrl Pts',(-1.00556037785319,0.931859337276389,2.83727237967739));
#3935=CARTESIAN_POINT('Ctrl Pts',(-0.904171665713376,1.02413687155565,2.82718320205455));
#3936=CARTESIAN_POINT('Ctrl Pts',(-0.88857982526168,1.03769395230865,2.82567864389195));
#3937=CARTESIAN_POINT('Ctrl Pts',(-0.865838834274635,1.05657858949772,2.82355704704619));
#3938=CARTESIAN_POINT('Ctrl Pts',(-0.858936549220571,1.06219735365717,2.82292237596522));
#3939=CARTESIAN_POINT('Ctrl Pts',(-0.847225704348335,1.07154169035215,2.82186172145223));
#3940=CARTESIAN_POINT('Ctrl Pts',(-0.842446466710632,1.07530318719371,2.82143333968576));
#3941=CARTESIAN_POINT('Ctrl Pts',(-0.831367093837753,1.08390398893679,2.82045061638249));
#3942=CARTESIAN_POINT('Ctrl Pts',(-0.825049645711192,1.08872043795629,2.81989781566776));
#3943=CARTESIAN_POINT('Ctrl Pts',(-0.806772771386808,1.10240434426697,2.81831890463741));
#3944=CARTESIAN_POINT('Ctrl Pts',(-0.794709520561203,1.11113206496247,2.81730152337101));
#3945=CARTESIAN_POINT('Ctrl Pts',(-0.725947839445159,1.15918801575539,2.81162516326725));
#3946=CARTESIAN_POINT('Ctrl Pts',(-0.666469695326698,1.19437745373598,2.80717474218855));
#3947=CARTESIAN_POINT('Ctrl Pts',(-0.545782316230265,1.25394461302342,2.79851780933413));
#3948=CARTESIAN_POINT('Ctrl Pts',(-0.484973822923106,1.27869279043026,2.79432057740742));
#3949=CARTESIAN_POINT('Ctrl Pts',(-0.38473775364833,1.31130479169281,2.78739934982316));
#3950=CARTESIAN_POINT('Ctrl Pts',(-0.346332381085573,1.32196702860901,2.78474801470412));
#3951=CARTESIAN_POINT('Ctrl Pts',(-0.29174828390894,1.33457892848013,2.78094656848575));
#3952=CARTESIAN_POINT('Ctrl Pts',(-0.275915121172672,1.33794199654319,2.77984014151979));
#3953=CARTESIAN_POINT('Ctrl Pts',(-0.248212421900609,1.34331359457473,2.77789576258713));
#3954=CARTESIAN_POINT('Ctrl Pts',(-0.236368940982478,1.34544807681726,2.77706181840495));
#3955=CARTESIAN_POINT('Ctrl Pts',(-0.211667885710037,1.34956360255032,2.77531618479486));
#3956=CARTESIAN_POINT('Ctrl Pts',(-0.198807170403423,1.35151799819961,2.77440375957859));
#3957=CARTESIAN_POINT('Ctrl Pts',(-0.164741464188319,1.35619809929917,2.77197660164922));
#3958=CARTESIAN_POINT('Ctrl Pts',(-0.143497774679793,1.35861007357041,2.77045244433473));
#3959=CARTESIAN_POINT('Ctrl Pts',(-0.0218578296249289,1.36953623210188,
2.76166010379382));
#3960=CARTESIAN_POINT('Ctrl Pts',(0.0791646933984834,1.36741850453304,2.75407190559131));
#3961=CARTESIAN_POINT('Ctrl Pts',(0.224687844743802,1.34818165795214,2.7429696788253));
#3962=CARTESIAN_POINT('Ctrl Pts',(0.270027868009202,1.33983722671712,2.73949165813805));
#3963=CARTESIAN_POINT('Ctrl Pts',(0.340661513831219,1.3231057106918,2.73411069261342));
#3964=CARTESIAN_POINT('Ctrl Pts',(0.366280154942863,1.31624391887726,2.73216725338979));
#3965=CARTESIAN_POINT('Ctrl Pts',(0.401023953141729,1.30584487022744,2.72955664218566));
#3966=CARTESIAN_POINT('Ctrl Pts',(0.410333402673673,1.30294955730597,2.72885964909161));
#3967=CARTESIAN_POINT('Ctrl Pts',(0.426097400193815,1.29786110851335,2.72768459000048));
#3968=CARTESIAN_POINT('Ctrl Pts',(0.432567842298856,1.29571892080389,2.72720379472912));
#3969=CARTESIAN_POINT('Ctrl Pts',(0.446343354796048,1.29104352380714,2.72618368530728));
#3970=CARTESIAN_POINT('Ctrl Pts',(0.453643340125955,1.28849660383361,2.72564513956115));
#3971=CARTESIAN_POINT('Ctrl Pts',(0.473996909333182,1.28120094508637,2.72414825045489));
#3972=CARTESIAN_POINT('Ctrl Pts',(0.487000671769003,1.27631473961987,2.72319729750435));
#3973=CARTESIAN_POINT('Ctrl Pts',(0.593568526577657,1.23440552707315,2.71543106598301));
#3974=CARTESIAN_POINT('Ctrl Pts',(0.682866157069123,1.18734157676016,2.70907912829546));
#3975=CARTESIAN_POINT('Ctrl Pts',(0.812638308661457,1.09941917507033,2.69897093736381));
#3976=CARTESIAN_POINT('Ctrl Pts',(0.857098405444911,1.06512207295732,2.69532373186021));
#3977=CARTESIAN_POINT('Ctrl Pts',(0.918910277749296,1.01105745337468,2.68984650770516));
#3978=CARTESIAN_POINT('Ctrl Pts',(0.938004193973587,0.993368643588955,2.68809212479594));
#3979=CARTESIAN_POINT('Ctrl Pts',(0.966523127121389,0.965392684445844,2.68536452447334));
#3980=CARTESIAN_POINT('Ctrl Pts',(0.976315858642235,0.955487995899881,2.68440739368148));
#3981=CARTESIAN_POINT('Ctrl Pts',(0.994171365316706,0.936867237025232,2.68262235359033));
#3982=CARTESIAN_POINT('Ctrl Pts',(1.00227532184794,0.928192376108285,2.68179630836139));
#3983=CARTESIAN_POINT('Ctrl Pts',(1.02009555147639,0.908611242047245,2.67994323585171));
#3984=CARTESIAN_POINT('Ctrl Pts',(1.02975190157295,0.897652669553067,2.6789138718951));
#3985=CARTESIAN_POINT('Ctrl Pts',(1.05418312195726,0.86901367283767,2.67624219348566));
#3986=CARTESIAN_POINT('Ctrl Pts',(1.06868919174816,0.851111107294155,2.67458960543642));
#3987=CARTESIAN_POINT('Ctrl Pts',(1.14563030251882,0.751085047189641,2.66544592974648));
#3988=CARTESIAN_POINT('Ctrl Pts',(1.19905248462926,0.662468202727034,2.65763112537259));
#3989=CARTESIAN_POINT('Ctrl Pts',(1.25841661819214,0.532823606047787,2.64686151420327));
#3990=CARTESIAN_POINT('Ctrl Pts',(1.27328480550014,0.496245440073111,2.64389413711922));
#3991=CARTESIAN_POINT('Ctrl Pts',(1.29463872594448,0.436401215179274,2.63919711517297));
#3992=CARTESIAN_POINT('Ctrl Pts',(1.30212846322436,0.413517937812812,2.6374371023121));
#3993=CARTESIAN_POINT('Ctrl Pts',(1.3117019096116,0.381422072786795,2.63502876280897));
#3994=CARTESIAN_POINT('Ctrl Pts',(1.31430054928348,0.372369139817996,2.63435604875521));
#3995=CARTESIAN_POINT('Ctrl Pts',(1.3186059736694,0.356763396622772,2.63320850667838));
#3996=CARTESIAN_POINT('Ctrl Pts',(1.32035800274831,0.350223624963691,2.63273127191815));
#3997=CARTESIAN_POINT('Ctrl Pts',(1.32405013281965,0.336020426347164,2.63170290125094));
#3998=CARTESIAN_POINT('Ctrl Pts',(1.32597244063254,0.328352821948098,2.63115272926185));
#3999=CARTESIAN_POINT('Ctrl Pts',(1.3312793380025,0.306377970144358,2.62958908472244));
#4000=CARTESIAN_POINT('Ctrl Pts',(1.33449977867376,0.292031711510687,2.62858408434089));
#4001=CARTESIAN_POINT('Ctrl Pts',(1.35156907257844,0.209801686377302,2.622899060866));
#4002=CARTESIAN_POINT('Ctrl Pts',(1.36047079662161,0.140986488007043,2.61843053621497));
#4003=CARTESIAN_POINT('Ctrl Pts',(1.36755948431215,0.00628367727474066,
2.60975413098043));
#4004=CARTESIAN_POINT('Ctrl Pts',(1.36628402753273,-0.0593785824087688,
2.60555549584965));
#4005=CARTESIAN_POINT('Ctrl Pts',(1.35665923117047,-0.164376839088424,2.59863230686157));
#4006=CARTESIAN_POINT('Ctrl Pts',(1.35128714060748,-0.20387894757638,2.59598047176616));
#4007=CARTESIAN_POINT('Ctrl Pts',(1.34131611813841,-0.259015603627945,2.59217843645943));
#4008=CARTESIAN_POINT('Ctrl Pts',(1.33815280691061,-0.274890959745322,2.59107193960064));
#4009=CARTESIAN_POINT('Ctrl Pts',(1.33214718152976,-0.302464394902681,2.58912748040693));
#4010=CARTESIAN_POINT('Ctrl Pts',(1.32943090435045,-0.314188284180502,2.58829352687372));
#4011=CARTESIAN_POINT('Ctrl Pts',(1.32345702899145,-0.338506561817742,2.58654791507393));
#4012=CARTESIAN_POINT('Ctrl Pts',(1.32017372444422,-0.351093316030731,2.58563552151683));
#4013=CARTESIAN_POINT('Ctrl Pts',(1.31102089210131,-0.384235818310119,2.58320854854815));
#4014=CARTESIAN_POINT('Ctrl Pts',(1.30484793580201,-0.404703245400948,2.58168454714169));
#4015=CARTESIAN_POINT('Ctrl Pts',(1.26684375796151,-0.520785657905018,2.57289112198094));
#4016=CARTESIAN_POINT('Ctrl Pts',(1.2249937366015,-0.612775905079113,2.56530154968322));
#4017=CARTESIAN_POINT('Ctrl Pts',(1.14984214518684,-0.738877928697974,2.55419870524363));
#4018=CARTESIAN_POINT('Ctrl Pts',(1.1242746112331,-0.777228784848023,2.5507214052825));
#4019=CARTESIAN_POINT('Ctrl Pts',(1.08101523291244,-0.835502772238854,2.54534139034468));
#4020=CARTESIAN_POINT('Ctrl Pts',(1.06459571506041,-0.85632645458842,2.54339819579169));
#4021=CARTESIAN_POINT('Ctrl Pts',(1.04132313674688,-0.884136388110229,2.54078785252486));
#4022=CARTESIAN_POINT('Ctrl Pts',(1.03498691711868,-0.891545356915325,2.54009089026485));
#4023=CARTESIAN_POINT('Ctrl Pts',(1.02408682544234,-0.904018044367269,2.53891586647293));
#4024=CARTESIAN_POINT('Ctrl Pts',(1.01956347714145,-0.909116480513805,2.53843507607641));
#4025=CARTESIAN_POINT('Ctrl Pts',(1.0098277536541,-0.919925911034869,2.53741495782153));
#4026=CARTESIAN_POINT('Ctrl Pts',(1.00460478726949,-0.925626816074157,2.53687639859961));
#4027=CARTESIAN_POINT('Ctrl Pts',(0.989863275108719,-0.941445513130695,
2.53537943278435));
#4028=CARTESIAN_POINT('Ctrl Pts',(0.980238094300213,-0.951463227465583,
2.53442841780528));
#4029=CARTESIAN_POINT('Ctrl Pts',(0.911199052646548,-1.02115783906046,2.52777524921006));
#4030=CARTESIAN_POINT('Ctrl Pts',(0.846523750799378,-1.07538286515854,2.52239677369653));
#4031=CARTESIAN_POINT('Ctrl Pts',(0.730728034773992,-1.15550601540192,2.5133437866314));
#4032=CARTESIAN_POINT('Ctrl Pts',(0.682244625442632,-1.18477816941618,2.50969993362544));
#4033=CARTESIAN_POINT('Ctrl Pts',(0.599684707391595,-1.22787228080641,2.50356532420787));
#4034=CARTESIAN_POINT('Ctrl Pts',(0.566617558370231,-1.24347749004527,2.50112616916176));
#4035=CARTESIAN_POINT('Ctrl Pts',(0.518494485839277,-1.26386966004305,2.49757562455074));
#4036=CARTESIAN_POINT('Ctrl Pts',(0.503918161040141,-1.2697517482131,2.49650016041877));
#4037=CARTESIAN_POINT('Ctrl Pts',(0.47806749438124,-1.27966822603475,2.49459100468783));
#4038=CARTESIAN_POINT('Ctrl Pts',(0.466835355641053,-1.28380840968344,2.49376087358823));
#4039=CARTESIAN_POINT('Ctrl Pts',(0.443089456702582,-1.29220835903634,2.49200387346505));
#4040=CARTESIAN_POINT('Ctrl Pts',(0.430565434103959,-1.29643514879154,2.49107603382018));
#4041=CARTESIAN_POINT('Ctrl Pts',(0.396640576764781,-1.30733881567284,2.48855860778375));
#4042=CARTESIAN_POINT('Ctrl Pts',(0.375134296022604,-1.31367145098252,2.48695829136088));
#4043=CARTESIAN_POINT('Ctrl Pts',(0.270718389550387,-1.34164419845191,2.47916284681783));
#4044=CARTESIAN_POINT('Ctrl Pts',(0.186063956604697,-1.35597693372624,2.4727482282083));
#4045=CARTESIAN_POINT('Ctrl Pts',(0.045444893860012,-1.36636517156687,2.46208671552133));
#4046=CARTESIAN_POINT('Ctrl Pts',(-0.00994806838753257,-1.36708468047476,
2.45789025712734));
#4047=CARTESIAN_POINT('Ctrl Pts',(-0.0947104808179618,-1.36303220484456,
2.45158030429225));
#4048=CARTESIAN_POINT('Ctrl Pts',(-0.124136373990518,-1.36066796622916,
2.44941103810261));
#4049=CARTESIAN_POINT('Ctrl Pts',(-0.163514733513941,-1.35621577324427,
2.44655511761264));
#4050=CARTESIAN_POINT('Ctrl Pts',(-0.173552098013563,-1.35496788766778,
2.44583129909112));
#4051=CARTESIAN_POINT('Ctrl Pts',(-0.190387088375231,-1.35268474297834,
2.44462525296046));
#4052=CARTESIAN_POINT('Ctrl Pts',(-0.197192303938863,-1.35170945889443,
2.44413993900791));
#4053=CARTESIAN_POINT('Ctrl Pts',(-0.211477117431756,-1.34955205926757,
2.44312617616002));
#4054=CARTESIAN_POINT('Ctrl Pts',(-0.218954692177259,-1.34835906999399,
2.44259830688548));
#4055=CARTESIAN_POINT('Ctrl Pts',(-0.239744179492438,-1.34486475816824,
2.44113752635005));
#4056=CARTESIAN_POINT('Ctrl Pts',(-0.253032855709848,-1.3424279860794,2.4402116050373));
#4057=CARTESIAN_POINT('Ctrl Pts',(-0.353784510116791,-1.32240361846912,
2.43323594435198));
#4058=CARTESIAN_POINT('Ctrl Pts',(-0.439383386724051,-1.2964803885036,2.42755539874409));
#4059=CARTESIAN_POINT('Ctrl Pts',(-0.59657267375393,-1.23150088251039,2.41661585361514));
#4060=CARTESIAN_POINT('Ctrl Pts',(-0.6683951088256,-1.19404319213079,2.41138729132463));
#4061=CARTESIAN_POINT('Ctrl Pts',(-0.752710411757752,-1.14006773181688,
2.40463765087472));
#4062=CARTESIAN_POINT('Ctrl Pts',(-0.768718780379926,-1.12933554469368,
2.40332722943582));
#4063=CARTESIAN_POINT('Ctrl Pts',(-0.794797134244905,-1.11104091229297,
2.4011405766563));
#4064=CARTESIAN_POINT('Ctrl Pts',(-0.804999453118168,-1.10367126249358,
2.40027153611508));
#4065=CARTESIAN_POINT('Ctrl Pts',(-0.82481531285194,-1.08893633003308,2.3985558035106));
#4066=CARTESIAN_POINT('Ctrl Pts',(-0.834435630017448,-1.08158207913001,
2.39770958675804));
#4067=CARTESIAN_POINT('Ctrl Pts',(-0.857633544623524,-1.06335471310932,
2.39563568753407));
#4068=CARTESIAN_POINT('Ctrl Pts',(-0.871103357674404,-1.05234853233427,
2.39440290321733));
#4069=CARTESIAN_POINT('Ctrl Pts',(-0.919804868299132,-1.01097874854762,
2.38983681183424));
#4070=CARTESIAN_POINT('Ctrl Pts',(-0.953686153425763,-0.979081654086912,
2.38644357172854));
#4071=CARTESIAN_POINT('Ctrl Pts',(-1.0665467465238,-0.861404780124572,2.3743526597629));
#4072=CARTESIAN_POINT('Ctrl Pts',(-1.1361165893462,-0.767317597823783,2.36536691413308));
#4073=CARTESIAN_POINT('Ctrl Pts',(-1.20297448753743,-0.647484519922585,
2.35526793587841));
#4074=CARTESIAN_POINT('Ctrl Pts',(-1.21264126062292,-0.629194013310627,
2.35376141243667));
#4075=CARTESIAN_POINT('Ctrl Pts',(-1.22587007589173,-0.602725340192119,
2.35163758550378));
#4076=CARTESIAN_POINT('Ctrl Pts',(-1.2297728455932,-0.594721815568319,2.35100260131887));
#4077=CARTESIAN_POINT('Ctrl Pts',(-1.23620947779529,-0.581187681579178,
2.34994159829172));
#4078=CARTESIAN_POINT('Ctrl Pts',(-1.23878506380021,-0.575677483767837,
2.3495131771138));
#4079=CARTESIAN_POINT('Ctrl Pts',(-1.24463829564584,-0.562933894261398,
2.34853061030841));
#4080=CARTESIAN_POINT('Ctrl Pts',(-1.24788979739124,-0.555688867819095,
2.3479780024788));
#4081=CARTESIAN_POINT('Ctrl Pts',(-1.25704957827883,-0.534793037739726,
2.34640021397833));
#4082=CARTESIAN_POINT('Ctrl Pts',(-1.26279852725655,-0.52107308495318,2.34538374334719));
#4083=CARTESIAN_POINT('Ctrl Pts',(-1.29228200719528,-0.447354544529492,
2.34001131754651));
#4084=CARTESIAN_POINT('Ctrl Pts',(-1.31196987232,-0.385818388774232,2.33583657202266));
#4085=CARTESIAN_POINT('Ctrl Pts',(-1.34259872947066,-0.260006441818594,
2.32750102290687));
#4086=CARTESIAN_POINT('Ctrl Pts',(-1.35344127489454,-0.195885179564962,
2.32334989436872));
#4087=CARTESIAN_POINT('Ctrl Pts',(-1.36388087542549,-0.0877259045414485,
2.31623926819673));
#4088=CARTESIAN_POINT('Ctrl Pts',(-1.36598924460494,-0.0440418313328702,
2.31333927938346));
#4089=CARTESIAN_POINT('Ctrl Pts',(-1.36600404927079,0.0163501997855103,
2.30924602844509));
#4090=CARTESIAN_POINT('Ctrl Pts',(-1.36570243894645,0.033033286908241,2.3081065629074));
#4091=CARTESIAN_POINT('Ctrl Pts',(-1.36465466392262,0.0618087103916622,
2.3061239323985));
#4092=CARTESIAN_POINT('Ctrl Pts',(-1.36405306326691,0.0739046187657651,
2.30528525914422));
#4093=CARTESIAN_POINT('Ctrl Pts',(-1.36248350611625,0.0987883005367717,
2.30354831021974));
#4094=CARTESIAN_POINT('Ctrl Pts',(-1.36149614205953,0.111573599444312,2.30264952065761));
#4095=CARTESIAN_POINT('Ctrl Pts',(-1.35846635477241,0.144719948123277,2.30030200332278));
#4096=CARTESIAN_POINT('Ctrl Pts',(-1.35614621387222,0.165051709732037,2.298844948199));
#4097=CARTESIAN_POINT('Ctrl Pts',(-1.34181863080126,0.269682828433087,2.29125401830345));
#4098=CARTESIAN_POINT('Ctrl Pts',(-1.32240649733088,0.352764312422965,2.28489767949591));
#4099=CARTESIAN_POINT('Ctrl Pts',(-1.26960619708709,0.510548536813381,2.27232432142413));
#4100=CARTESIAN_POINT('Ctrl Pts',(-1.23699115224955,0.585162017848858,2.26614210876987));
#4101=CARTESIAN_POINT('Ctrl Pts',(-1.19117302222158,0.668775569663828,2.25920115580365));
#4102=CARTESIAN_POINT('Ctrl Pts',(-1.18422164703187,0.681008855391917,2.25818561544659));
#4103=CARTESIAN_POINT('Ctrl Pts',(-1.17313969407658,0.699828283393194,2.25662572194617));
#4104=CARTESIAN_POINT('Ctrl Pts',(-1.16914003894161,0.70648987604062,2.25607403541721));
#4105=CARTESIAN_POINT('Ctrl Pts',(-1.16153149835778,0.718920632636567,2.25504597825618));
#4106=CARTESIAN_POINT('Ctrl Pts',(-1.15793618502672,0.724697241142232,2.25456887870297));
#4107=CARTESIAN_POINT('Ctrl Pts',(-1.15200861218155,0.734064357973069,2.25379598744767));
#4108=CARTESIAN_POINT('Ctrl Pts',(-1.14970257594817,0.737670869509345,2.25349858565013));
#4109=CARTESIAN_POINT('Ctrl Pts',(-1.14737960344529,0.741266514553124,2.25320219258599));
#4110=CARTESIAN_POINT('',(-1.36599953791183,0.00117996591060617,2.19095138131927));
#4111=CARTESIAN_POINT('Ctrl Pts',(-1.14737960371854,0.741266514130168,2.135049540568));
#4112=CARTESIAN_POINT('Ctrl Pts',(-1.17371791782586,0.700498391158188,2.13860808597731));
#4113=CARTESIAN_POINT('Ctrl Pts',(-1.19786310457235,0.658357968998659,2.1422315668744));
#4114=CARTESIAN_POINT('Ctrl Pts',(-1.25537449359362,0.544301663977534,2.15185451518902));
#4115=CARTESIAN_POINT('Ctrl Pts',(-1.2848175537371,0.470610192428532,2.15789704875815));
#4116=CARTESIAN_POINT('Ctrl Pts',(-1.31459053704653,0.37198739168062,2.16551368962053));
#4117=CARTESIAN_POINT('Ctrl Pts',(-1.32087503262053,0.349016059702377,2.16725510478538));
#4118=CARTESIAN_POINT('Ctrl Pts',(-1.32884726459755,0.316564638328336,2.16965941112887));
#4119=CARTESIAN_POINT('Ctrl Pts',(-1.3310400216991,0.307214415458845,2.17034573411801));
#4120=CARTESIAN_POINT('Ctrl Pts',(-1.33461520410095,0.291211953288213,2.17150852239933));
#4121=CARTESIAN_POINT('Ctrl Pts',(-1.33604691120638,0.28457126363952,2.1719875764289));
#4122=CARTESIAN_POINT('Ctrl Pts',(-1.33901597091823,0.270283301705197,2.17301060879284));
#4123=CARTESIAN_POINT('Ctrl Pts',(-1.34053745351382,0.262633160237652,2.17355373840162));
#4124=CARTESIAN_POINT('Ctrl Pts',(-1.34356997052004,0.246672007860385,2.17467809067034));
#4125=CARTESIAN_POINT('Ctrl Pts',(-1.34506961512004,0.238359149745227,2.17525871322365));
#4126=CARTESIAN_POINT('Ctrl Pts',(-1.34998212061336,0.209603886683836,2.17725173725914));
#4127=CARTESIAN_POINT('Ctrl Pts',(-1.3530069884155,0.189097085164622,2.17864622994722));
#4128=CARTESIAN_POINT('Ctrl Pts',(-1.36246580351747,0.113014678564882,2.18374728945422));
#4129=CARTESIAN_POINT('Ctrl Pts',(-1.36595118104071,0.0571264594019624,
2.18735323940492));
#4130=CARTESIAN_POINT('Ctrl Pts',(-1.3659994907434,0.00117952904397824,
2.19095149184204));
#4131=CARTESIAN_POINT('Ctrl Pts',(-1.36599949036158,0.00117997114881014,
2.19095146340787));
#4132=CARTESIAN_POINT('Ctrl Pts',(-1.36607646183637,-0.08792644085728,2.19668238319806));
#4133=CARTESIAN_POINT('Ctrl Pts',(-1.35743489945597,-0.176821291742645,
2.20238374650203));
#4134=CARTESIAN_POINT('Ctrl Pts',(-1.33687455700889,-0.28110092303994,2.20949613751109));
#4135=CARTESIAN_POINT('Ctrl Pts',(-1.33323261145016,-0.297896077059224,
2.21065444507774));
#4136=CARTESIAN_POINT('Ctrl Pts',(-1.32568879633879,-0.329769080175029,
2.21288030576275));
#4137=CARTESIAN_POINT('Ctrl Pts',(-1.32184400159832,-0.344857699669815,
2.21394599684218));
#4138=CARTESIAN_POINT('Ctrl Pts',(-1.31459400899412,-0.371404622689786,
2.21584399275958));
#4139=CARTESIAN_POINT('Ctrl Pts',(-1.31129470361084,-0.382890306403933,
2.21667287484779));
#4140=CARTESIAN_POINT('Ctrl Pts',(-1.30400968890188,-0.407051921202472,
2.21843361417204));
#4141=CARTESIAN_POINT('Ctrl Pts',(-1.29998888363092,-0.419715874918516,
2.21936651968309));
#4142=CARTESIAN_POINT('Ctrl Pts',(-1.28857731970357,-0.453919624669206,
2.22191454523546));
#4143=CARTESIAN_POINT('Ctrl Pts',(-1.28083192825725,-0.475335666865282,
2.2235408577773));
#4144=CARTESIAN_POINT('Ctrl Pts',(-1.2388896809886,-0.58282564361692,2.23186637088375));
#4145=CARTESIAN_POINT('Ctrl Pts',(-1.19654209088457,-0.665443522994749,
2.23882576515915));
#4146=CARTESIAN_POINT('Ctrl Pts',(-1.11901282319034,-0.785021644128266,
2.24960631527121));
#4147=CARTESIAN_POINT('Ctrl Pts',(-1.08957418588737,-0.825395199767631,
2.25338295966459));
#4148=CARTESIAN_POINT('Ctrl Pts',(-1.04039463163135,-0.88561208045601,2.25915435284955));
#4149=CARTESIAN_POINT('Ctrl Pts',(-1.02214392200986,-0.906615572066782,
2.26119583914786));
#4150=CARTESIAN_POINT('Ctrl Pts',(-0.996536920470781,-0.934327776795401,
2.26391332033117));
#4151=CARTESIAN_POINT('Ctrl Pts',(-0.98973143499818,-0.94153381762631,2.26462223904124));
#4152=CARTESIAN_POINT('Ctrl Pts',(-0.978098109267252,-0.953586317092375,
2.26581090723722));
#4153=CARTESIAN_POINT('Ctrl Pts',(-0.973311299893142,-0.958471646744947,
2.26629354565115));
#4154=CARTESIAN_POINT('Ctrl Pts',(-0.963090747458644,-0.968747015498945,
2.26731016472728));
#4155=CARTESIAN_POINT('Ctrl Pts',(-0.957648107806782,-0.974127649072518,
2.26784346609662));
#4156=CARTESIAN_POINT('Ctrl Pts',(-0.942189163193491,-0.989155682905238,
2.2693367029386));
#4157=CARTESIAN_POINT('Ctrl Pts',(-0.93207003498454,-0.998696586326021,
2.2702891341921));
#4158=CARTESIAN_POINT('Ctrl Pts',(-0.859168901304149,-1.06535857891352,
2.276990995642));
#4159=CARTESIAN_POINT('Ctrl Pts',(-0.791320699721666,-1.11668055654621,
2.28241036286789));
#4160=CARTESIAN_POINT('Ctrl Pts',(-0.671258474259176,-1.19102461038199,
2.29148951311705));
#4161=CARTESIAN_POINT('Ctrl Pts',(-0.621592482610981,-1.2176821327883,2.29511692499223));
#4162=CARTESIAN_POINT('Ctrl Pts',(-0.53730950319118,-1.25641665729695,2.30122765946126));
#4163=CARTESIAN_POINT('Ctrl Pts',(-0.503599929029577,-1.27030353564526,
2.30365994102189));
#4164=CARTESIAN_POINT('Ctrl Pts',(-0.454634103003027,-1.28821981992616,
2.3072021551681));
#4165=CARTESIAN_POINT('Ctrl Pts',(-0.439799234228894,-1.29335960639101,
2.30827639792034));
#4166=CARTESIAN_POINT('Ctrl Pts',(-0.4135074745571,-1.30196418724908,2.31018398347378));
#4167=CARTESIAN_POINT('Ctrl Pts',(-0.402087286265688,-1.30553627861508,
2.31101378107394));
#4168=CARTESIAN_POINT('Ctrl Pts',(-0.377953184439014,-1.31273842838228,
2.31277067601318));
#4169=CARTESIAN_POINT('Ctrl Pts',(-0.365230605971333,-1.3163348258283,2.31369875081637));
#4170=CARTESIAN_POINT('Ctrl Pts',(-0.330774218445289,-1.3255369283498,2.3162183490802));
#4171=CARTESIAN_POINT('Ctrl Pts',(-0.308951997726483,-1.33079235413189,
2.31782063931884));
#4172=CARTESIAN_POINT('Ctrl Pts',(-0.205421790578268,-1.35304182826893,
2.32545748847324));
#4173=CARTESIAN_POINT('Ctrl Pts',(-0.122409600565164,-1.36305984025793,
2.33169878629354));
#4174=CARTESIAN_POINT('Ctrl Pts',(0.0178985283095588,-1.36706894655092,
2.34230927371497));
#4175=CARTESIAN_POINT('Ctrl Pts',(0.0748605360730985,-1.36513523905382,
2.34662919684714));
#4176=CARTESIAN_POINT('Ctrl Pts',(0.161375927554686,-1.35676544997509,2.35309520711253));
#4177=CARTESIAN_POINT('Ctrl Pts',(0.191114013724558,-1.35289704298862,2.355299774167));
#4178=CARTESIAN_POINT('Ctrl Pts',(0.230734987908566,-1.34641030291933,2.35819357490472));
#4179=CARTESIAN_POINT('Ctrl Pts',(0.240748722971042,-1.34465586925658,2.35892118738686));
#4180=CARTESIAN_POINT('Ctrl Pts',(0.25750727920682,-1.34152650426607,2.36013155681761));
#4181=CARTESIAN_POINT('Ctrl Pts',(0.264262852953502,-1.34021211519801,2.36061745182815));
#4182=CARTESIAN_POINT('Ctrl Pts',(0.278406540718293,-1.33734915805822,2.36163017303405));
#4183=CARTESIAN_POINT('Ctrl Pts',(0.285792198632084,-1.33579032733665,2.36215644630473));
#4184=CARTESIAN_POINT('Ctrl Pts',(0.306253632952181,-1.33129422077803,2.36360830269464));
#4185=CARTESIAN_POINT('Ctrl Pts',(0.31930007208281,-1.32822554097555,2.36452703144254));
#4186=CARTESIAN_POINT('Ctrl Pts',(0.41970015891958,-1.30304530788675,2.37155798903011));
#4187=CARTESIAN_POINT('Ctrl Pts',(0.50472947988421,-1.27252816058713,2.37729238542969));
#4188=CARTESIAN_POINT('Ctrl Pts',(0.658573275720449,-1.19944464820414,2.38824774128926));
#4189=CARTESIAN_POINT('Ctrl Pts',(0.727825415521351,-1.15872956420119,2.39343552490092));
#4190=CARTESIAN_POINT('Ctrl Pts',(0.808776973810352,-1.10100245879927,2.40013916888293));
#4191=CARTESIAN_POINT('Ctrl Pts',(0.824212311974858,-1.08949557655875,2.40144823447628));
#4192=CARTESIAN_POINT('Ctrl Pts',(0.849322570160549,-1.06993710240308,2.40363307959904));
#4193=CARTESIAN_POINT('Ctrl Pts',(0.859138875451151,-1.06207090430935,2.40450168918216));
#4194=CARTESIAN_POINT('Ctrl Pts',(0.878187754022247,-1.04636937323252,2.40621689678582));
#4195=CARTESIAN_POINT('Ctrl Pts',(0.887427557938885,-1.03854461113943,2.40706302384555));
#4196=CARTESIAN_POINT('Ctrl Pts',(0.909689503117703,-1.01917798528235,2.40913728037559));
#4197=CARTESIAN_POINT('Ctrl Pts',(0.922597165485077,-1.00750840118373,2.41037051997282));
#4198=CARTESIAN_POINT('Ctrl Pts',(0.969252526263535,-0.963679648030682,
2.41494472308392));
#4199=CARTESIAN_POINT('Ctrl Pts',(1.00156742054044,-0.93004879390754,2.41834593192469));
#4200=CARTESIAN_POINT('Ctrl Pts',(1.10838421002038,-0.806847006720276,2.4304385193758));
#4201=CARTESIAN_POINT('Ctrl Pts',(1.17309903152954,-0.709474019122929,2.43941664640074));
#4202=CARTESIAN_POINT('Ctrl Pts',(1.23383120310332,-0.586552282893262,2.44950681363341));
#4203=CARTESIAN_POINT('Ctrl Pts',(1.24256368728954,-0.567819172986419,2.45101188686558));
#4204=CARTESIAN_POINT('Ctrl Pts',(1.25444423115412,-0.540744734715356,2.45313396511914));
#4205=CARTESIAN_POINT('Ctrl Pts',(1.25794059457768,-0.532560483598315,2.4537686166332));
#4206=CARTESIAN_POINT('Ctrl Pts',(1.26369079536452,-0.518727813279361,2.45482915093959));
#4207=CARTESIAN_POINT('Ctrl Pts',(1.26598726494741,-0.513097671931915,2.45525743281715));
#4208=CARTESIAN_POINT('Ctrl Pts',(1.27119567206641,-0.500080594415097,2.45623977733098));
#4209=CARTESIAN_POINT('Ctrl Pts',(1.27408091214045,-0.492683341367778,2.45679230186873));
#4210=CARTESIAN_POINT('Ctrl Pts',(1.28218562186744,-0.471356850874166,2.45837003997861));
#4211=CARTESIAN_POINT('Ctrl Pts',(1.28724247339092,-0.4573664934488,2.45938654179684));
#4212=CARTESIAN_POINT('Ctrl Pts',(1.31295533045673,-0.382421445280935,2.46474795759204));
#4213=CARTESIAN_POINT('Ctrl Pts',(1.3295149713477,-0.320140111734791,2.46891263054978));
#4214=CARTESIAN_POINT('Ctrl Pts',(1.35456290222315,-0.189339644744835,2.47748605796773));
#4215=CARTESIAN_POINT('Ctrl Pts',(1.36237903849839,-0.120884203031925,2.48188165161043));
#4216=CARTESIAN_POINT('Ctrl Pts',(1.36656615806065,-0.0112521408170147,
2.48907847432982));
#4217=CARTESIAN_POINT('Ctrl Pts',(1.36629008634054,0.0296747307462688,2.49179855063476));
#4218=CARTESIAN_POINT('Ctrl Pts',(1.36333532645016,0.0868293488464395,2.49568072268751));
#4219=CARTESIAN_POINT('Ctrl Pts',(1.36220021545034,0.103116841317082,2.49679644714451));
#4220=CARTESIAN_POINT('Ctrl Pts',(1.35972022305621,0.131385577778616,2.49875134257828));
#4221=CARTESIAN_POINT('Ctrl Pts',(1.35850812391533,0.143376832665842,2.49958636799586));
#4222=CARTESIAN_POINT('Ctrl Pts',(1.35566514611722,0.168213061224002,2.50132865344911));
#4223=CARTESIAN_POINT('Ctrl Pts',(1.35400999216437,0.181053978328443,2.50223658159003));
#4224=CARTESIAN_POINT('Ctrl Pts',(1.34917983277572,0.214742745771451,2.50463826111263));
#4225=CARTESIAN_POINT('Ctrl Pts',(1.34570426053134,0.235543252117025,2.50614108493688));
#4226=CARTESIAN_POINT('Ctrl Pts',(1.3224161729163,0.357479942047706,2.51507380921219));
#4227=CARTESIAN_POINT('Ctrl Pts',(1.2916934761076,0.456176611211052,2.52284148514849));
#4228=CARTESIAN_POINT('Ctrl Pts',(1.23209423391968,0.591535194512689,2.53402603477027));
#4229=CARTESIAN_POINT('Ctrl Pts',(1.21199522473418,0.631694612871495,2.53741189842259));
#4230=CARTESIAN_POINT('Ctrl Pts',(1.17714155224769,0.69352331364702,2.54267089216371));
#4231=CARTESIAN_POINT('Ctrl Pts',(1.16367880105885,0.715883144678285,2.54458263813417));
#4232=CARTESIAN_POINT('Ctrl Pts',(1.14434749565081,0.746001842165404,2.54715838784733));
#4233=CARTESIAN_POINT('Ctrl Pts',(1.13902537654685,0.754102874157724,2.54785124156434));
#4234=CARTESIAN_POINT('Ctrl Pts',(1.12982011718613,0.76779477740346,2.54902146450636));
#4235=CARTESIAN_POINT('Ctrl Pts',(1.12598068058318,0.773414399119225,2.5495015091841));
#4236=CARTESIAN_POINT('Ctrl Pts',(1.11767678546578,0.785375540075554,2.55052247273197));
#4237=CARTESIAN_POINT('Ctrl Pts',(1.11320010449364,0.791708071533136,2.55106259395232));
#4238=CARTESIAN_POINT('Ctrl Pts',(1.10048795402133,0.809369141217755,2.55256888136645));
#4239=CARTESIAN_POINT('Ctrl Pts',(1.0921315844605,0.820610007194054,2.55352750647935));
#4240=CARTESIAN_POINT('Ctrl Pts',(1.03329335926526,0.897267094340546,2.56007947175965));
#4241=CARTESIAN_POINT('Ctrl Pts',(0.977133054033637,0.958122092464455,2.56536239615268));
#4242=CARTESIAN_POINT('Ctrl Pts',(0.873161913583961,1.05206847222157,2.57437063874636));
#4243=CARTESIAN_POINT('Ctrl Pts',(0.828126524603272,1.08787208716941,2.57806983397526));
#4244=CARTESIAN_POINT('Ctrl Pts',(0.750697400048299,1.14182795161101,2.58428421288578));
#4245=CARTESIAN_POINT('Ctrl Pts',(0.719582273859238,1.16168784055319,2.58674586518172));
#4246=CARTESIAN_POINT('Ctrl Pts',(0.674080489329991,1.18820035519313,2.59032292805261));
#4247=CARTESIAN_POINT('Ctrl Pts',(0.660321668396492,1.19590127092951,2.59140162518712));
#4248=CARTESIAN_POINT('Ctrl Pts',(0.63588464373612,1.20902857671307,2.59331423046945));
#4249=CARTESIAN_POINT('Ctrl Pts',(0.625262434861344,1.2145559892951,2.59414452948381));
#4250=CARTESIAN_POINT('Ctrl Pts',(0.60279134771834,1.22587622286607,2.59589954688453));
#4251=CARTESIAN_POINT('Ctrl Pts',(0.590928547386279,1.23163848306527,2.59682520691561));
#4252=CARTESIAN_POINT('Ctrl Pts',(0.558804217754113,1.24667167942333,2.59933062356771));
#4253=CARTESIAN_POINT('Ctrl Pts',(0.538396981711344,1.25561977408922,2.60092093713052));
#4254=CARTESIAN_POINT('Ctrl Pts',(0.434127480452693,1.29833023665962,2.60904489385575));
#4255=CARTESIAN_POINT('Ctrl Pts',(0.347292113586577,1.32420210682373,2.61582661269119));
#4256=CARTESIAN_POINT('Ctrl Pts',(0.185721712651223,1.35534685734947,2.6282727065431));
#4257=CARTESIAN_POINT('Ctrl Pts',(0.111860261402536,1.3634320367304,2.63389294550674));
#4258=CARTESIAN_POINT('Ctrl Pts',(0.0244083580187489,1.36584665622211,2.64024919808147));
#4259=CARTESIAN_POINT('Ctrl Pts',(0.0111094020576111,1.36601957194127,2.64120748227421));
#4260=CARTESIAN_POINT('Ctrl Pts',(-0.00971714452040687,1.36598617363267,
2.64269307007227));
#4261=CARTESIAN_POINT('Ctrl Pts',(-0.0172437213387161,1.3659118970302,2.6432268600547));
#4262=CARTESIAN_POINT('Ctrl Pts',(-0.0315809791105177,1.3656518783728,2.64423730383272));
#4263=CARTESIAN_POINT('Ctrl Pts',(-0.0383914374033142,1.3654773930208,2.64471449440175));
#4264=CARTESIAN_POINT('Ctrl Pts',(-0.0553504021755864,1.36491591963152,
2.64589636959368));
#4265=CARTESIAN_POINT('Ctrl Pts',(-0.0654966887571556,1.36446668486708,
2.64659778472214));
#4266=CARTESIAN_POINT('Ctrl Pts',(-0.103249304131287,1.36237305574665,2.64918961210104));
#4267=CARTESIAN_POINT('Ctrl Pts',(-0.130810550317792,1.36000353022628,2.65104590518989));
#4268=CARTESIAN_POINT('Ctrl Pts',(-0.234006464636342,1.34796478700161,2.65792448349459));
#4269=CARTESIAN_POINT('Ctrl Pts',(-0.30886287185463,1.33280662544063,2.66277439570784));
#4270=CARTESIAN_POINT('Ctrl Pts',(-0.452350479051149,1.29100500999837,2.67240112038397));
#4271=CARTESIAN_POINT('Ctrl Pts',(-0.520865352393476,1.26491592751046,2.6771586256277));
#4272=CARTESIAN_POINT('Ctrl Pts',(-0.60412243008238,1.2252973177307,2.68337806233754));
#4273=CARTESIAN_POINT('Ctrl Pts',(-0.621115991490716,1.21677125768185,2.68467128740375));
#4274=CARTESIAN_POINT('Ctrl Pts',(-0.649006816212435,1.20204126407364,2.68683697369529));
#4275=CARTESIAN_POINT('Ctrl Pts',(-0.660006815532055,1.19603680272708,2.68770252971901));
#4276=CARTESIAN_POINT('Ctrl Pts',(-0.681498264492303,1.18391871623988,2.68941715435755));
#4277=CARTESIAN_POINT('Ctrl Pts',(-0.691993903453373,1.17781485470824,2.69026581910582));
#4278=CARTESIAN_POINT('Ctrl Pts',(-0.71749363730311,1.16252669694836,2.69235636132904));
#4279=CARTESIAN_POINT('Ctrl Pts',(-0.732403991128427,1.15319113042094,2.69360354224826));
#4280=CARTESIAN_POINT('Ctrl Pts',(-0.787347214267139,1.11729505879172,2.69829516395191));
#4281=CARTESIAN_POINT('Ctrl Pts',(-0.826146428853504,1.08891919775506,2.70180394607588));
#4282=CARTESIAN_POINT('Ctrl Pts',(-0.935272628256078,0.999915459480922,
2.71225949054176));
#4283=CARTESIAN_POINT('Ctrl Pts',(-1.00101373598797,0.934095958786727,2.71935360734661));
#4284=CARTESIAN_POINT('Ctrl Pts',(-1.08340050201359,0.832841597761097,2.72912570955183));
#4285=CARTESIAN_POINT('Ctrl Pts',(-1.10600946457868,0.802574216693599,2.7319206684085));
#4286=CARTESIAN_POINT('Ctrl Pts',(-1.13350576186215,0.762390985997101,2.73543780406233));
#4287=CARTESIAN_POINT('Ctrl Pts',(-1.13956648763224,0.753301777093282,2.73622113497334));
#4288=CARTESIAN_POINT('Ctrl Pts',(-1.14613957558168,0.743183272266232,2.73707895540836));
#4289=CARTESIAN_POINT('Ctrl Pts',(-1.14676018894998,0.742225283827124,2.73716003172249));
#4290=CARTESIAN_POINT('Ctrl Pts',(-1.1473796034465,0.741266514551254,2.73724103392041));
#4291=CARTESIAN_POINT('Origin',(0.,0.,-1.10921167016993));
#4292=CARTESIAN_POINT('',(-1.14737936922177,0.741266877099097,3.45490258866455));
#4293=CARTESIAN_POINT('',(-1.14737979714396,0.741266214733872,3.33530270583882));
#4294=CARTESIAN_POINT('',(-1.14737960344596,0.741266514552077,-1.10921167016993));
#4295=CARTESIAN_POINT('',(-1.3659998215671,-0.000698196705795024,2.90819715390762));
#4296=CARTESIAN_POINT('Ctrl Pts',(-1.14737936922177,0.741266877099097,3.45490258866455));
#4297=CARTESIAN_POINT('Ctrl Pts',(-1.11952596587337,0.784380121939649,3.45157440197762));
#4298=CARTESIAN_POINT('Ctrl Pts',(-1.08924219884794,0.825924191298115,3.44820368515017));
#4299=CARTESIAN_POINT('Ctrl Pts',(-1.04353816610939,0.881710130657872,3.44335396253766));
#4300=CARTESIAN_POINT('Ctrl Pts',(-1.03005527619933,0.897424487929018,3.44194906241363));
#4301=CARTESIAN_POINT('Ctrl Pts',(-1.00761943431487,0.922401627006729,3.43964762343261));
#4302=CARTESIAN_POINT('Ctrl Pts',(-0.998883160533326,0.931855191594713,
3.43875992684046));
#4303=CARTESIAN_POINT('Ctrl Pts',(-0.981685959800063,0.949944631053132,
3.43702769259532));
#4304=CARTESIAN_POINT('Ctrl Pts',(-0.973241389204758,0.95859444372604,3.43618389374785));
#4305=CARTESIAN_POINT('Ctrl Pts',(-0.952970205997118,0.978814328330803,
3.43417348411629));
#4306=CARTESIAN_POINT('Ctrl Pts',(-0.941046236186742,0.990283616741711,
3.43300270920174));
#4307=CARTESIAN_POINT('Ctrl Pts',(-0.897700566111386,1.03048652757841,3.4287861517702));
#4308=CARTESIAN_POINT('Ctrl Pts',(-0.865150400075602,1.05796167295573,3.42569059017237));
#4309=CARTESIAN_POINT('Ctrl Pts',(-0.776399187523272,1.12603756002686,3.4174289574481));
#4310=CARTESIAN_POINT('Ctrl Pts',(-0.718300540121299,1.16395837417859,3.41218970310328));
#4311=CARTESIAN_POINT('Ctrl Pts',(-0.603684223396136,1.22690775128098,3.40230006907409));
#4312=CARTESIAN_POINT('Ctrl Pts',(-0.547843889435548,1.25283904698977,3.39766236478986));
#4313=CARTESIAN_POINT('Ctrl Pts',(-0.476454819830723,1.28030128862273,3.39208379300223));
#4314=CARTESIAN_POINT('Ctrl Pts',(-0.462379542846903,1.28545158980115,3.39100037810259));
#4315=CARTESIAN_POINT('Ctrl Pts',(-0.440698293789413,1.29298277023957,3.38935947749768));
#4316=CARTESIAN_POINT('Ctrl Pts',(-0.433151983451155,1.29553031519802,3.38879347925848));
#4317=CARTESIAN_POINT('Ctrl Pts',(-0.419807567560481,1.29990559468693,3.38780213838708));
#4318=CARTESIAN_POINT('Ctrl Pts',(-0.41401914953979,1.30176076718246,3.38737531029461));
#4319=CARTESIAN_POINT('Ctrl Pts',(-0.399754189607378,1.30622787153547,3.38633104015039));
#4320=CARTESIAN_POINT('Ctrl Pts',(-0.39126428976378,1.30879598517655,3.38571604792524));
#4321=CARTESIAN_POINT('Ctrl Pts',(-0.363098380647745,1.31701732783122,3.38369538241295));
#4322=CARTESIAN_POINT('Ctrl Pts',(-0.343319331670952,1.32231124185327,3.38230789549032));
#4323=CARTESIAN_POINT('Ctrl Pts',(-0.19633467142663,1.35813128165645,3.37217749989463));
#4324=CARTESIAN_POINT('Ctrl Pts',(-0.0654425975497376,1.37069060462629,
3.36408625396289));
#4325=CARTESIAN_POINT('Ctrl Pts',(0.101041286051439,1.36272911653129,3.35310870086751));
#4326=CARTESIAN_POINT('Ctrl Pts',(0.136749279713942,1.3596099744566,3.35071857142971));
#4327=CARTESIAN_POINT('Ctrl Pts',(0.186641211857784,1.35326653324207,3.34730485105731));
#4328=CARTESIAN_POINT('Ctrl Pts',(0.200960869417467,1.35121425182602,3.34631648524208));
#4329=CARTESIAN_POINT('Ctrl Pts',(0.227162237245689,1.347033392174,3.34449073546578));
#4330=CARTESIAN_POINT('Ctrl Pts',(0.23905361500105,1.34497397545557,3.34365555244704));
#4331=CARTESIAN_POINT('Ctrl Pts',(0.263349696370282,1.34043386152849,3.34193485230474));
#4332=CARTESIAN_POINT('Ctrl Pts',(0.275750312982287,1.3379378705994,3.34104893384218));
#4333=CARTESIAN_POINT('Ctrl Pts',(0.307266506086722,1.33113755341733,3.33877687765412));
#4334=CARTESIAN_POINT('Ctrl Pts',(0.326326832066408,1.32659361526658,3.33738340755153));
#4335=CARTESIAN_POINT('Ctrl Pts',(0.430334887004992,1.29942126330434,3.32966858452517));
#4336=CARTESIAN_POINT('Ctrl Pts',(0.513029917941651,1.26904652813601,3.32310573772539));
#4337=CARTESIAN_POINT('Ctrl Pts',(0.664446318719396,1.19619858369405,3.31040605981962));
#4338=CARTESIAN_POINT('Ctrl Pts',(0.73347865816001,1.15515842671112,3.30431143572428));
#4339=CARTESIAN_POINT('Ctrl Pts',(0.809980461628674,1.10003966045376,3.29744639011927));
#4340=CARTESIAN_POINT('Ctrl Pts',(0.821314984340061,1.09160310494144,3.29642646717704));
#4341=CARTESIAN_POINT('Ctrl Pts',(0.838687172217952,1.07824876221461,3.29486132841733));
#4342=CARTESIAN_POINT('Ctrl Pts',(0.844816777322932,1.07345292695909,3.29430870521757));
#4343=CARTESIAN_POINT('Ctrl Pts',(0.856225282227469,1.06436859892801,3.29327995332105));
#4344=CARTESIAN_POINT('Ctrl Pts',(0.861513406191609,1.06009287399211,3.29280308154885));
#4345=CARTESIAN_POINT('Ctrl Pts',(0.874223891584747,1.04965785055443,3.29165639586456));
#4346=CARTESIAN_POINT('Ctrl Pts',(0.881613329402282,1.04345913520713,3.29098930470938));
#4347=CARTESIAN_POINT('Ctrl Pts',(0.908465109076654,1.0204453115064,3.28856091286791));
#4348=CARTESIAN_POINT('Ctrl Pts',(0.927518365159583,1.00315869654733,3.28682933073821));
#4349=CARTESIAN_POINT('Ctrl Pts',(0.977694467776746,0.954982299354946,3.28220909628167));
#4350=CARTESIAN_POINT('Ctrl Pts',(1.00783782006688,0.92311488980507,3.27936665356975));
#4351=CARTESIAN_POINT('Ctrl Pts',(1.1048713712067,0.810101160323626,3.2697648007979));
#4352=CARTESIAN_POINT('Ctrl Pts',(1.16390446942265,0.722723168632437,3.26308654107747));
#4353=CARTESIAN_POINT('Ctrl Pts',(1.22192481092492,0.610973728590381,3.25462072095394));
#4354=CARTESIAN_POINT('Ctrl Pts',(1.23109104241388,0.592287016308522,3.25320870657538));
#4355=CARTESIAN_POINT('Ctrl Pts',(1.24523875654687,0.561696258209988,3.25089859998073));
#4356=CARTESIAN_POINT('Ctrl Pts',(1.25048494755218,0.549917833617948,3.25000947942465));
#4357=CARTESIAN_POINT('Ctrl Pts',(1.26032130375748,0.52696499716382,3.2482765248527));
#4358=CARTESIAN_POINT('Ctrl Pts',(1.26493152895234,0.515800453191203,3.24743345619121));
#4359=CARTESIAN_POINT('Ctrl Pts',(1.275481594337,0.489259031831937,3.2454281471759));
#4360=CARTESIAN_POINT('Ctrl Pts',(1.28129222480163,0.473833188172663,3.24426180135614));
#4361=CARTESIAN_POINT('Ctrl Pts',(1.30094660852811,0.41864808440182,3.24008426157558));
#4362=CARTESIAN_POINT('Ctrl Pts',(1.313228810867,0.378361909673317,3.23702452433899));
#4363=CARTESIAN_POINT('Ctrl Pts',(1.34157596304562,0.267213311735129,3.22855580893986));
#4364=CARTESIAN_POINT('Ctrl Pts',(1.35388062846224,0.195536533686368,3.22305948959263));
#4365=CARTESIAN_POINT('Ctrl Pts',(1.36575687054721,0.0644244356058351,3.21310574377113));
#4366=CARTESIAN_POINT('Ctrl Pts',(1.3672655798415,0.00533101284859088,3.20865856982825));
#4367=CARTESIAN_POINT('Ctrl Pts',(1.36436194771161,-0.0685020762610586,
3.20327113986523));
#4368=CARTESIAN_POINT('Ctrl Pts',(1.3635375557866,-0.0833152919444829,3.20219896223031));
#4369=CARTESIAN_POINT('Ctrl Pts',(1.36190221834453,-0.106024864419903,3.20057143887855));
#4370=CARTESIAN_POINT('Ctrl Pts',(1.36126354269587,-0.113931995177353,3.20000778073755));
#4371=CARTESIAN_POINT('Ctrl Pts',(1.36001337906888,-0.127893012177758,3.19901842713312));
#4372=CARTESIAN_POINT('Ctrl Pts',(1.35943029989715,-0.133948780183741,3.19859127932164));
#4373=CARTESIAN_POINT('Ctrl Pts',(1.35789291934502,-0.148870143379656,3.19754348736508));
#4374=CARTESIAN_POINT('Ctrl Pts',(1.35689224499234,-0.157730613416601,3.19692533733126));
#4375=CARTESIAN_POINT('Ctrl Pts',(1.35327313049798,-0.18718664012045,3.19488189769329));
#4376=CARTESIAN_POINT('Ctrl Pts',(1.35027182307618,-0.20773329046104,3.19347536105528));
#4377=CARTESIAN_POINT('Ctrl Pts',(1.32728480686735,-0.343396431620855,3.1842661581634));
#4378=CARTESIAN_POINT('Ctrl Pts',(1.29306775888658,-0.455617894212942,3.17698369869951));
#4379=CARTESIAN_POINT('Ctrl Pts',(1.22598173093634,-0.604198678569807,3.16634275080618));
#4380=CARTESIAN_POINT('Ctrl Pts',(1.20486516005097,-0.645280201412293,3.16328820163393));
#4381=CARTESIAN_POINT('Ctrl Pts',(1.17300100941232,-0.700232926208892,3.15898916046204));
#4382=CARTESIAN_POINT('Ctrl Pts',(1.16400546042755,-0.715086541301879,3.15780476614719));
#4383=CARTESIAN_POINT('Ctrl Pts',(1.14826317073107,-0.739996079763346,3.15577765749067));
#4384=CARTESIAN_POINT('Ctrl Pts',(1.14166126251398,-0.75014135514566,3.15494020893623));
#4385=CARTESIAN_POINT('Ctrl Pts',(1.12791740261348,-0.770660052855567,3.15322132569112));
#4386=CARTESIAN_POINT('Ctrl Pts',(1.12076508546755,-0.781025088343883,3.15233956614868));
#4387=CARTESIAN_POINT('Ctrl Pts',(1.10228484173557,-0.807029743925583,3.15009205306045));
#4388=CARTESIAN_POINT('Ctrl Pts',(1.09076701920435,-0.822530316890012,3.14871928184725));
#4389=CARTESIAN_POINT('Ctrl Pts',(1.02835333040827,-0.90290896082275,3.14141976487176));
#4390=CARTESIAN_POINT('Ctrl Pts',(0.97199693635401,-0.963313519454494,3.13528262130146));
#4391=CARTESIAN_POINT('Ctrl Pts',(0.845616463623247,-1.07632551654564,3.12248340826263));
#4392=CARTESIAN_POINT('Ctrl Pts',(0.775274108763995,-1.12804963381647,3.11584084959659));
#4393=CARTESIAN_POINT('Ctrl Pts',(0.688671202598603,-1.17977845107784,3.10850449130767));
#4394=CARTESIAN_POINT('Ctrl Pts',(0.676755349651456,-1.18665388905116,3.10751247021067));
#4395=CARTESIAN_POINT('Ctrl Pts',(0.65807750653892,-1.19705810510458,3.10598659319119));
#4396=CARTESIAN_POINT('Ctrl Pts',(0.65138676501804,-1.20071203922276,3.10544569703378));
#4397=CARTESIAN_POINT('Ctrl Pts',(0.638623231183331,-1.20754434300906,3.10442512826929));
#4398=CARTESIAN_POINT('Ctrl Pts',(0.632556625004821,-1.21073328607801,3.10394487579284));
#4399=CARTESIAN_POINT('Ctrl Pts',(0.617589747883078,-1.21845749992736,3.10277135533876));
#4400=CARTESIAN_POINT('Ctrl Pts',(0.608663042524002,-1.22294116434434,3.10208113481952));
#4401=CARTESIAN_POINT('Ctrl Pts',(0.574130999300641,-1.23981396560229,3.09944512125668));
#4402=CARTESIAN_POINT('Ctrl Pts',(0.548188466376972,-1.25150099505823,3.09753607780207));
#4403=CARTESIAN_POINT('Ctrl Pts',(0.473959670343445,-1.28218918004764,3.09222045233245));
#4404=CARTESIAN_POINT('Ctrl Pts',(0.424928242181872,-1.29926269406566,3.08887863109367));
#4405=CARTESIAN_POINT('Ctrl Pts',(0.287750312819767,-1.33843070385525,3.07970452560338));
#4406=CARTESIAN_POINT('Ctrl Pts',(0.198201149326897,-1.35458892711181,3.07389272584933));
#4407=CARTESIAN_POINT('Ctrl Pts',(0.0855195448502148,-1.36350216601995,
3.06631124618276));
#4408=CARTESIAN_POINT('Ctrl Pts',(0.0632849461917286,-1.36471486865637,
3.06480354461368));
#4409=CARTESIAN_POINT('Ctrl Pts',(0.0278503386528507,-1.36577972677735,
3.06237670642066));
#4410=CARTESIAN_POINT('Ctrl Pts',(0.0146644093364811,-1.36598493320493,
3.06146835283433));
#4411=CARTESIAN_POINT('Ctrl Pts',(-0.0105006938828898,-1.36601216090849,
3.05972366376811));
#4412=CARTESIAN_POINT('Ctrl Pts',(-0.0224786525949524,-1.36586755669788,
3.05888843179733));
#4413=CARTESIAN_POINT('Ctrl Pts',(-0.0502284491741487,-1.36516743712146,
3.05694154201533));
#4414=CARTESIAN_POINT('Ctrl Pts',(-0.0659953691986541,-1.36449609845557,
3.05582644858491));
#4415=CARTESIAN_POINT('Ctrl Pts',(-0.118658299278119,-1.36133889317227,
3.05207045087925));
#4416=CARTESIAN_POINT('Ctrl Pts',(-0.155461625785447,-1.35762830206659,
3.04939328039257));
#4417=CARTESIAN_POINT('Ctrl Pts',(-0.249168995243895,-1.34432038473211,
3.04244015875177));
#4418=CARTESIAN_POINT('Ctrl Pts',(-0.305695718692348,-1.3326032753762,3.03811312551726));
#4419=CARTESIAN_POINT('Ctrl Pts',(-0.440674214949408,-1.29558290976022,
3.02753808668194));
#4420=CARTESIAN_POINT('Ctrl Pts',(-0.517916534412971,-1.26668595716403,
3.02127443261782));
#4421=CARTESIAN_POINT('Ctrl Pts',(-0.604730276651481,-1.22493018964236,
3.01426210347852));
#4422=CARTESIAN_POINT('Ctrl Pts',(-0.617274806783212,-1.2186568543032,3.01324986441966));
#4423=CARTESIAN_POINT('Ctrl Pts',(-0.636607407907734,-1.20861376257629,
3.01169392335762));
#4424=CARTESIAN_POINT('Ctrl Pts',(-0.64346332920066,-1.20497766385499,3.01114294351353));
#4425=CARTESIAN_POINT('Ctrl Pts',(-0.656274332310081,-1.19804271068511,
3.01011540607988));
#4426=CARTESIAN_POINT('Ctrl Pts',(-0.662236031260655,-1.19475762268562,
3.00963813027082));
#4427=CARTESIAN_POINT('Ctrl Pts',(-0.676624185980672,-1.1866884976963,3.00848799468822));
#4428=CARTESIAN_POINT('Ctrl Pts',(-0.685024726671796,-1.18185913594663,
3.00781790179144));
#4429=CARTESIAN_POINT('Ctrl Pts',(-0.71582422648948,-1.16371416260903,3.00536363552994));
#4430=CARTESIAN_POINT('Ctrl Pts',(-0.737893671034164,-1.14984699539792,
3.00361001357485));
#4431=CARTESIAN_POINT('Ctrl Pts',(-0.796769605218092,-1.11045892361194,
2.99890722233588));
#4432=CARTESIAN_POINT('Ctrl Pts',(-0.832740651735628,-1.08374552382827,
2.99600629735977));
#4433=CARTESIAN_POINT('Ctrl Pts',(-0.947096438791633,-0.989759125798017,
2.98646838246588));
#4434=CARTESIAN_POINT('Ctrl Pts',(-1.01915982252501,-0.91538286978294,2.97990266600291));
#4435=CARTESIAN_POINT('Ctrl Pts',(-1.09501017206169,-0.816916385130135,
2.97154936389669));
#4436=CARTESIAN_POINT('Ctrl Pts',(-1.10747571825278,-0.799935692344157,
2.97012080303913));
#4437=CARTESIAN_POINT('Ctrl Pts',(-1.12695990863045,-0.77206536143616,2.96779052875609));
#4438=CARTESIAN_POINT('Ctrl Pts',(-1.13422524723013,-0.761351841666792,
2.9668980907328));
#4439=CARTESIAN_POINT('Ctrl Pts',(-1.1479621778456,-0.740462175202806,2.96516336791937));
#4440=CARTESIAN_POINT('Ctrl Pts',(-1.15445344387798,-0.730300365731136,
2.96432190939742));
#4441=CARTESIAN_POINT('Ctrl Pts',(-1.16942615017782,-0.706162663715283,
2.9623280105459));
#4442=CARTESIAN_POINT('Ctrl Pts',(-1.17779273828415,-0.692118091694161,
2.96117159580155));
#4443=CARTESIAN_POINT('Ctrl Pts',(-1.206276986346,-0.642290312332412,2.95707991000993));
#4444=CARTESIAN_POINT('Ctrl Pts',(-1.22503027940676,-0.605756733735404,
2.95409875475125));
#4445=CARTESIAN_POINT('Ctrl Pts',(-1.27723982735175,-0.491672166178959,
2.94484482211019));
#4446=CARTESIAN_POINT('Ctrl Pts',(-1.30517592802723,-0.411820801235354,
2.93843026435818));
#4447=CARTESIAN_POINT('Ctrl Pts',(-1.3385806102332,-0.277603429747723,2.92799439333938));
#4448=CARTESIAN_POINT('Ctrl Pts',(-1.34849319317181,-0.224564073405041,
2.92395891538661));
#4449=CARTESIAN_POINT('Ctrl Pts',(-1.35675165708441,-0.159140176773375,
2.91918189821619));
#4450=CARTESIAN_POINT('Ctrl Pts',(-1.3581003123126,-0.147187709774169,2.91831736002777));
#4451=CARTESIAN_POINT('Ctrl Pts',(-1.36000948914384,-0.127995607518491,
2.91694386623046));
#4452=CARTESIAN_POINT('Ctrl Pts',(-1.36067043992439,-0.120766908941682,
2.91642987417944));
#4453=CARTESIAN_POINT('Ctrl Pts',(-1.36179481381425,-0.107285545018877,
2.91547791597109));
#4454=CARTESIAN_POINT('Ctrl Pts',(-1.36227286425605,-0.101034396492146,
2.91503917160784));
#4455=CARTESIAN_POINT('Ctrl Pts',(-1.36320052936008,-0.087696817401474,
2.91410832541328));
#4456=CARTESIAN_POINT('Ctrl Pts',(-1.36363796688507,-0.0806096504419577,
2.91361686864516));
#4457=CARTESIAN_POINT('Ctrl Pts',(-1.36458656073511,-0.0630101522076326,
2.91240357475843));
#4458=CARTESIAN_POINT('Ctrl Pts',(-1.36503153846035,-0.0524945305617169,
2.9116849495475));
#4459=CARTESIAN_POINT('Ctrl Pts',(-1.36577779296243,-0.0282201845049701,
2.91003846451426));
#4460=CARTESIAN_POINT('Ctrl Pts',(-1.36599278763656,-0.0144598598424152,
2.90911430339757));
#4461=CARTESIAN_POINT('Ctrl Pts',(-1.3659998215671,-0.000698196705795024,
2.90819715390762));
#4462=CARTESIAN_POINT('Ctrl Pts',(-1.36599982067117,-0.000699947383821987,
2.90819727058204));
#4463=CARTESIAN_POINT('Ctrl Pts',(-1.36603811834598,0.0740408376203964,
2.90321614895498));
#4464=CARTESIAN_POINT('Ctrl Pts',(-1.35994219632796,0.148668269478248,2.89844664933997));
#4465=CARTESIAN_POINT('Ctrl Pts',(-1.33468287822297,0.301721687836379,2.88846903957996));
#4466=CARTESIAN_POINT('Ctrl Pts',(-1.31462716037188,0.379694086415268,2.88327052164584));
#4467=CARTESIAN_POINT('Ctrl Pts',(-1.28141584216642,0.473603571526771,2.87655462545921));
#4468=CARTESIAN_POINT('Ctrl Pts',(-1.27461164296517,0.491621807866384,2.87524504963661));
#4469=CARTESIAN_POINT('Ctrl Pts',(-1.26273591880415,0.521164397471336,2.87305942050981));
#4470=CARTESIAN_POINT('Ctrl Pts',(-1.25788180213555,0.532773576182582,2.8721905437729));
#4471=CARTESIAN_POINT('Ctrl Pts',(-1.24804229519679,0.555421553639558,2.87047484834364));
#4472=CARTESIAN_POINT('Ctrl Pts',(-1.24306908319984,0.566464394811963,2.86962850142787));
#4473=CARTESIAN_POINT('Ctrl Pts',(-1.23059292474813,0.593211547522121,2.86755376085174));
#4474=CARTESIAN_POINT('Ctrl Pts',(-1.22293558005477,0.608841033446778,2.86632025539059));
#4475=CARTESIAN_POINT('Ctrl Pts',(-1.19438779833755,0.66439760440072,2.86185686834645));
#4476=CARTESIAN_POINT('Ctrl Pts',(-1.17182577137712,0.703427176205171,2.85857145578429));
#4477=CARTESIAN_POINT('Ctrl Pts',(-1.14737960323804,0.741266514873919,2.85523392653093));
#4478=CARTESIAN_POINT('Ctrl Pts',(-1.1473796034465,0.741266514551254,2.73724103392041));
#4479=CARTESIAN_POINT('Ctrl Pts',(-1.15057249896258,0.736324347167213,2.73765857589913));
#4480=CARTESIAN_POINT('Ctrl Pts',(-1.15373353944903,0.731361432152484,2.73807414686288));
#4481=CARTESIAN_POINT('Ctrl Pts',(-1.16026311675626,0.720962132331392,2.73893695727811));
#4482=CARTESIAN_POINT('Ctrl Pts',(-1.16362572187677,0.715522242863275,2.73938382129083));
#4483=CARTESIAN_POINT('Ctrl Pts',(-1.17280678645064,0.700433571122158,2.74061157363299));
#4484=CARTESIAN_POINT('Ctrl Pts',(-1.17854441742851,0.690735856122947,2.74138755581199));
#4485=CARTESIAN_POINT('Ctrl Pts',(-1.20330086510121,0.647685901691912,2.7447799985362));
#4486=CARTESIAN_POINT('Ctrl Pts',(-1.22103035859875,0.613608532537429,2.74732882893174));
#4487=CARTESIAN_POINT('Ctrl Pts',(-1.27685745433803,0.494272259371022,2.75594952402163));
#4488=CARTESIAN_POINT('Ctrl Pts',(-1.30764233936883,0.405885139262189,2.76183557573808));
#4489=CARTESIAN_POINT('Ctrl Pts',(-1.34008007110202,0.269031176714398,2.77101307531492));
#4490=CARTESIAN_POINT('Ctrl Pts',(-1.34858896758189,0.222484750179486,2.77414179489373));
#4491=CARTESIAN_POINT('Ctrl Pts',(-1.35686483943027,0.158638384962662,2.77850137814088));
#4492=CARTESIAN_POINT('Ctrl Pts',(-1.3587440561424,0.141643481867952,2.77966813280422));
#4493=CARTESIAN_POINT('Ctrl Pts',(-1.36141459506357,0.1124925369886,2.78168258205061));
#4494=CARTESIAN_POINT('Ctrl Pts',(-1.36236323578757,0.100352716433346,2.78252537308681));
#4495=CARTESIAN_POINT('Ctrl Pts',(-1.36387126562964,0.0770463730733692,
2.78415157395397));
#4496=CARTESIAN_POINT('Ctrl Pts',(-1.36445610548622,0.0658824399349569,
2.78493413232573));
#4497=CARTESIAN_POINT('Ctrl Pts',(-1.36564197883456,0.0362988520802211,
2.7870179949882));
#4498=CARTESIAN_POINT('Ctrl Pts',(-1.36600736889497,0.0178726187264417,
2.78832636254868));
#4499=CARTESIAN_POINT('Ctrl Pts',(-1.3659745287301,-0.063015633370386,2.79411859118324));
#4500=CARTESIAN_POINT('Ctrl Pts',(-1.36166519990677,-0.125392567677053,
2.79871756855995));
#4501=CARTESIAN_POINT('Ctrl Pts',(-1.34640244543437,-0.235685188781841,
2.80705880593072));
#4502=CARTESIAN_POINT('Ctrl Pts',(-1.33710375098041,-0.283725777890929,
2.8107632978638));
#4503=CARTESIAN_POINT('Ctrl Pts',(-1.31119822309319,-0.387394812160237,
2.81884133500443));
#4504=CARTESIAN_POINT('Ctrl Pts',(-1.29358040563398,-0.442680994410301,
2.8232043163905));
#4505=CARTESIAN_POINT('Ctrl Pts',(-1.26712512982714,-0.510459150288916,
2.82850871912857));
#4506=CARTESIAN_POINT('Ctrl Pts',(-1.26152512388556,-0.524146015205151,
2.82957734877268));
#4507=CARTESIAN_POINT('Ctrl Pts',(-1.25258546779407,-0.545021458220617,
2.83120055473033));
#4508=CARTESIAN_POINT('Ctrl Pts',(-1.24940386325231,-0.552275962268128,
2.83176338169252));
#4509=CARTESIAN_POINT('Ctrl Pts',(-1.24338855546033,-0.565673632377859,
2.83279993500512));
#4510=CARTESIAN_POINT('Ctrl Pts',(-1.2405721839201,-0.571823764171653,2.83327455847943));
#4511=CARTESIAN_POINT('Ctrl Pts',(-1.23374047548147,-0.586454144960777,
2.83440110910919));
#4512=CARTESIAN_POINT('Ctrl Pts',(-1.22968327380125,-0.594914349884119,
2.83505057069143));
#4513=CARTESIAN_POINT('Ctrl Pts',(-1.21501317789129,-0.624713472981697,
2.83733346368826));
#4514=CARTESIAN_POINT('Ctrl Pts',(-1.20392877965059,-0.64581700368879,2.83894162828406));
#4515=CARTESIAN_POINT('Ctrl Pts',(-1.17333534496054,-0.700535434287843,
2.84311698613099));
#4516=CARTESIAN_POINT('Ctrl Pts',(-1.1529339608084,-0.73362756498671,2.84564814583357));
#4517=CARTESIAN_POINT('Ctrl Pts',(-1.07471074880778,-0.849168516378234,
2.85466710124961));
#4518=CARTESIAN_POINT('Ctrl Pts',(-1.0092355419046,-0.926030734968269,2.86104017769009));
#4519=CARTESIAN_POINT('Ctrl Pts',(-0.916029546794738,-1.01370157143677,
2.86955628946027));
#4520=CARTESIAN_POINT('Ctrl Pts',(-0.895593024092759,-1.03180132756153,
2.87139288122427));
#4521=CARTESIAN_POINT('Ctrl Pts',(-0.863621214967416,-1.05845158846678,
2.87423108898476));
#4522=CARTESIAN_POINT('Ctrl Pts',(-0.852469948114355,-1.06745319769899,
2.87521479979023));
#4523=CARTESIAN_POINT('Ctrl Pts',(-0.831834799922186,-1.08358088259662,
2.87702529084324));
#4524=CARTESIAN_POINT('Ctrl Pts',(-0.822395670488086,-1.09076212308067,
2.87784981684258));
#4525=CARTESIAN_POINT('Ctrl Pts',(-0.801481092155196,-1.10624802056063,
2.87966955596181));
#4526=CARTESIAN_POINT('Ctrl Pts',(-0.789967688479182,-1.11449883286375,
2.88066669211616));
#4527=CARTESIAN_POINT('Ctrl Pts',(-0.755903603844608,-1.13811702415164,
2.88360469779057));
#4528=CARTESIAN_POINT('Ctrl Pts',(-0.733019426725775,-1.15298870429551,
2.88556332060396));
#4529=CARTESIAN_POINT('Ctrl Pts',(-0.678564999796174,-1.18610029787644,
2.89019217367044));
#4530=CARTESIAN_POINT('Ctrl Pts',(-0.646680362495519,-1.2037809217233,2.89287890613758));
#4531=CARTESIAN_POINT('Ctrl Pts',(-0.564956533945809,-1.24491389256219,
2.89969835570477));
#4532=CARTESIAN_POINT('Ctrl Pts',(-0.514334978053881,-1.26666705716267,
2.90386449078473));
#4533=CARTESIAN_POINT('Ctrl Pts',(-0.4048977017204,-1.30605017463155,2.91266055266583));
#4534=CARTESIAN_POINT('Ctrl Pts',(-0.345917798957106,-1.32289508640888,
2.91728041824287));
#4535=CARTESIAN_POINT('Ctrl Pts',(-0.271366749303691,-1.33885775432365,
2.92284067970463));
#4536=CARTESIAN_POINT('Ctrl Pts',(-0.256680592094837,-1.34175076627224,
2.92392264665069));
#4537=CARTESIAN_POINT('Ctrl Pts',(-0.234116020779326,-1.34581166345596,
2.9255617331797));
#4538=CARTESIAN_POINT('Ctrl Pts',(-0.226270501485679,-1.3471529285501,2.92612734041623));
#4539=CARTESIAN_POINT('Ctrl Pts',(-0.212414345430657,-1.34939730230734,
2.92711820123959));
#4540=CARTESIAN_POINT('Ctrl Pts',(-0.206408995988884,-1.35032894594766,
2.92754493626115));
#4541=CARTESIAN_POINT('Ctrl Pts',(-0.191622369869683,-1.35252192577307,
2.92858921803193));
#4542=CARTESIAN_POINT('Ctrl Pts',(-0.182834709098554,-1.35373785211867,
2.9292043124781));
#4543=CARTESIAN_POINT('Ctrl Pts',(-0.153712808649518,-1.35747861863225,
2.93122632690644));
#4544=CARTESIAN_POINT('Ctrl Pts',(-0.13333260208096,-1.35963169758096,2.93261502340063));
#4545=CARTESIAN_POINT('Ctrl Pts',(0.0175150984547588,-1.37214323300134,
2.94275041707114));
#4546=CARTESIAN_POINT('Ctrl Pts',(0.148827953610968,-1.3641633544585,2.95084519227101));
#4547=CARTESIAN_POINT('Ctrl Pts',(0.31204062511948,-1.33036325500022,2.96182354270446));
#4548=CARTESIAN_POINT('Ctrl Pts',(0.346769730847836,-1.32173603977694,2.96420984717898));
#4549=CARTESIAN_POINT('Ctrl Pts',(0.394998533707071,-1.30772362809998,2.96761887308816));
#4550=CARTESIAN_POINT('Ctrl Pts',(0.408813589097488,-1.30347088650567,2.9686064966643));
#4551=CARTESIAN_POINT('Ctrl Pts',(0.434029661415569,-1.29526822475088,2.9704311624269));
#4552=CARTESIAN_POINT('Ctrl Pts',(0.44545092535273,-1.29138490698756,2.97126601046926));
#4553=CARTESIAN_POINT('Ctrl Pts',(0.468738901745412,-1.28312112388687,2.97298631726014));
#4554=CARTESIAN_POINT('Ctrl Pts',(0.480599161747456,-1.27872608610648,2.97387218068276));
#4555=CARTESIAN_POINT('Ctrl Pts',(0.510679213563483,-1.26710178097673,2.97614471684802));
#4556=CARTESIAN_POINT('Ctrl Pts',(0.52880701281505,-1.2596440986052,2.97753873231356));
#4557=CARTESIAN_POINT('Ctrl Pts',(0.627854233867203,-1.21638174868616,2.98529561246204));
#4558=CARTESIAN_POINT('Ctrl Pts',(0.705294364260077,-1.17317531635511,2.99190346626583));
#4559=CARTESIAN_POINT('Ctrl Pts',(0.84329641083693,-1.0775516623371,3.00459406735545));
#4560=CARTESIAN_POINT('Ctrl Pts',(0.904525071478661,-1.02669506984421,3.01063288450529));
#4561=CARTESIAN_POINT('Ctrl Pts',(0.971078448516087,-0.960814325811905,
3.01745201832386));
#4562=CARTESIAN_POINT('Ctrl Pts',(0.981011492183948,-0.950670297217601,
3.01847695239219));
#4563=CARTESIAN_POINT('Ctrl Pts',(0.996151718747177,-0.934718420631223,
3.0200479962254));
#4564=CARTESIAN_POINT('Ctrl Pts',(1.0014700375319,-0.929018053739657,3.0206015993165));
#4565=CARTESIAN_POINT('Ctrl Pts',(1.0113316910845,-0.918264871241324,3.02163090804709));
#4566=CARTESIAN_POINT('Ctrl Pts',(1.01588635868133,-0.913223451104482,3.02210737355179));
#4567=CARTESIAN_POINT('Ctrl Pts',(1.02679301870335,-0.900968626094434,3.02325135913853));
#4568=CARTESIAN_POINT('Ctrl Pts',(1.03310681882641,-0.893721815111771,3.02391618846292));
#4569=CARTESIAN_POINT('Ctrl Pts',(1.05587779426728,-0.867022085361121,3.02632608500185));
#4570=CARTESIAN_POINT('Ctrl Pts',(1.07186735888629,-0.847175172507116,3.02804201635865));
#4571=CARTESIAN_POINT('Ctrl Pts',(1.11343370739737,-0.792518859752084,3.03260443673468));
#4572=CARTESIAN_POINT('Ctrl Pts',(1.13793113154398,-0.756924035589029,3.03540610824553));
#4573=CARTESIAN_POINT('Ctrl Pts',(1.21682910194141,-0.629773630375466,3.04505501390468));
#4574=CARTESIAN_POINT('Ctrl Pts',(1.26218515869129,-0.533079991672298,3.05181367991454));
#4575=CARTESIAN_POINT('Ctrl Pts',(1.30237933359725,-0.412540193491741,3.06035963767341));
#4576=CARTESIAN_POINT('Ctrl Pts',(1.30845900324475,-0.392831137265044,3.06175924281031));
#4577=CARTESIAN_POINT('Ctrl Pts',(1.31759959786085,-0.36062793598177,3.0640540693177));
#4578=CARTESIAN_POINT('Ctrl Pts',(1.3209344631474,-0.348214493133696,3.06494054230761));
#4579=CARTESIAN_POINT('Ctrl Pts',(1.3270656085596,-0.324035608728886,3.06667181060787));
#4580=CARTESIAN_POINT('Ctrl Pts',(1.32988180854566,-0.312276422259023,3.06751588589142));
#4581=CARTESIAN_POINT('Ctrl Pts',(1.33618892316195,-0.284306362902053,3.06952927688713));
#4582=CARTESIAN_POINT('Ctrl Pts',(1.33954141633956,-0.268066591267152,3.07070279522731));
#4583=CARTESIAN_POINT('Ctrl Pts',(1.35050381205793,-0.209608244295557,3.07494525000009));
#4584=CARTESIAN_POINT('Ctrl Pts',(1.35641903399939,-0.167101401659893,3.078064804932));
#4585=CARTESIAN_POINT('Ctrl Pts',(1.36672588145937,-0.0543865423439802,
3.08642721913703));
#4586=CARTESIAN_POINT('Ctrl Pts',(1.36771338807098,0.0160018991397118,3.09174584904177));
#4587=CARTESIAN_POINT('Ctrl Pts',(1.35948339321396,0.146242111334113,3.10161413065164));
#4588=CARTESIAN_POINT('Ctrl Pts',(1.35171610898976,0.206025975189913,3.1061523014105));
#4589=CARTESIAN_POINT('Ctrl Pts',(1.33713707255443,0.279718259830903,3.11163009487079));
#4590=CARTESIAN_POINT('Ctrl Pts',(1.33400741289273,0.294282387568384,3.11270674781424));
#4591=CARTESIAN_POINT('Ctrl Pts',(1.32884422774793,0.316531394697004,3.11433950934974));
#4592=CARTESIAN_POINT('Ctrl Pts',(1.32698093367108,0.324254090403611,3.11490401083776));
#4593=CARTESIAN_POINT('Ctrl Pts',(1.32357282599314,0.337857866811323,3.11589393031033));
#4594=CARTESIAN_POINT('Ctrl Pts',(1.32205602872183,0.343745287991373,3.11632081409706));
#4595=CARTESIAN_POINT('Ctrl Pts',(1.31822376260552,0.358219480599451,3.11736674976889));
#4596=CARTESIAN_POINT('Ctrl Pts',(1.31586367027127,0.366794079412151,3.11798332854142));
#4597=CARTESIAN_POINT('Ctrl Pts',(1.3077525433972,0.395176785611726,3.12001602859977));
#4598=CARTESIAN_POINT('Ctrl Pts',(1.30163636083861,0.414878658174687,3.12141366138616));
#4599=CARTESIAN_POINT('Ctrl Pts',(1.25324121162077,0.559147174512248,3.13160051610739));
#4600=CARTESIAN_POINT('Ctrl Pts',(1.19361024750254,0.677171541597833,3.13973389522076));
#4601=CARTESIAN_POINT('Ctrl Pts',(1.0976971803934,0.813798084122,3.15073596507826));
#4602=CARTESIAN_POINT('Ctrl Pts',(1.07626515710295,0.841937887114607,3.15309618846417));
#4603=CARTESIAN_POINT('Ctrl Pts',(1.04377119156495,0.88133107610186,3.15656382151183));
#4604=CARTESIAN_POINT('Ctrl Pts',(1.03356744969989,0.89327546634832,3.15763822013523));
#4605=CARTESIAN_POINT('Ctrl Pts',(1.01520768007995,0.914031422738658,3.15954817729045));
#4606=CARTESIAN_POINT('Ctrl Pts',(1.00713709203345,0.922916538657451,3.16038021350373));
#4607=CARTESIAN_POINT('Ctrl Pts',(0.990024454408335,0.94126449706572,3.16212967074029));
#4608=CARTESIAN_POINT('Ctrl Pts',(0.980961434869913,0.950706009220624,3.16304792153868));
#4609=CARTESIAN_POINT('Ctrl Pts',(0.956456834724979,0.975510501706488,3.1655099232792));
#4610=CARTESIAN_POINT('Ctrl Pts',(0.940781651515177,0.990636261914579,3.16706359918743));
#4611=CARTESIAN_POINT('Ctrl Pts',(0.875437028320698,1.05074048906373,3.17345955134833));
#4612=CARTESIAN_POINT('Ctrl Pts',(0.822857985305066,1.09240470288447,3.17842876831727));
#4613=CARTESIAN_POINT('Ctrl Pts',(0.705343641828679,1.17221204938615,3.18912003054992));
#4614=CARTESIAN_POINT('Ctrl Pts',(0.63987476205376,1.20919448707235,3.19484396343836));
#4615=CARTESIAN_POINT('Ctrl Pts',(0.545242003403673,1.25280315506044,3.20259259402316));
#4616=CARTESIAN_POINT('Ctrl Pts',(0.518399995913137,1.26414647351902,3.20473453284266));
#4617=CARTESIAN_POINT('Ctrl Pts',(0.48156244253946,1.27834290974406,3.20758154611282));
#4618=CARTESIAN_POINT('Ctrl Pts',(0.471868859243252,1.28195272038424,3.20832220613323));
#4619=CARTESIAN_POINT('Ctrl Pts',(0.455693228407617,1.28776804549336,3.20954299682627));
#4620=CARTESIAN_POINT('Ctrl Pts',(0.449234052998387,1.29003551552824,3.21002649461239));
#4621=CARTESIAN_POINT('Ctrl Pts',(0.435702735611525,1.29467167378254,3.21103072984589));
#4622=CARTESIAN_POINT('Ctrl Pts',(0.428627797448005,1.29703116179964,3.21155095906299));
#4623=CARTESIAN_POINT('Ctrl Pts',(0.409195801019743,1.30333535254139,3.21296750886231));
#4624=CARTESIAN_POINT('Ctrl Pts',(0.396800970735034,1.30716229490686,3.21385750935968));
#4625=CARTESIAN_POINT('Ctrl Pts',(0.316981576031758,1.33056672917876,3.21951361071622));
#4626=CARTESIAN_POINT('Ctrl Pts',(0.248178453989884,1.34510041011198,3.22404993716046));
#4627=CARTESIAN_POINT('Ctrl Pts',(0.0837636912153136,1.36677769667172,3.23472109346056));
#4628=CARTESIAN_POINT('Ctrl Pts',(-0.0120680235703268,1.3692880583612,3.24082597838604));
#4629=CARTESIAN_POINT('Ctrl Pts',(-0.12922758754514,1.36005030865457,3.24871295417904));
#4630=CARTESIAN_POINT('Ctrl Pts',(-0.151036884180881,1.35780130462963,3.25019811507849));
#4631=CARTESIAN_POINT('Ctrl Pts',(-0.18579211726466,1.35336961446285,3.25259727778144));
#4632=CARTESIAN_POINT('Ctrl Pts',(-0.198777602106361,1.35152338811212,3.25350093331701));
#4633=CARTESIAN_POINT('Ctrl Pts',(-0.223583558708352,1.34763135098632,3.25524213044176));
#4634=CARTESIAN_POINT('Ctrl Pts',(-0.235407659257654,1.34561624682529,3.25607864441217));
#4635=CARTESIAN_POINT('Ctrl Pts',(-0.262861939000636,1.3405644683166,3.2580369576039));
#4636=CARTESIAN_POINT('Ctrl Pts',(-0.278468324252178,1.33740975286302,3.25916232772686));
#4637=CARTESIAN_POINT('Ctrl Pts',(-0.33109248919721,1.32581116750349,3.26300009297437));
#4638=CARTESIAN_POINT('Ctrl Pts',(-0.367809283287446,1.31609776749508,3.26575099263491));
#4639=CARTESIAN_POINT('Ctrl Pts',(-0.461666145365464,1.28703366773176,3.27297632277202));
#4640=CARTESIAN_POINT('Ctrl Pts',(-0.518012192281605,1.26540642870932,3.27750746389944));
#4641=CARTESIAN_POINT('Ctrl Pts',(-0.643110514770034,1.2076311568008,3.2879249969103));
#4642=CARTESIAN_POINT('Ctrl Pts',(-0.710591852759295,1.16919854512066,3.29381331393724));
#4643=CARTESIAN_POINT('Ctrl Pts',(-0.786388251548101,1.1170315373354,3.30051754913645));
#4644=CARTESIAN_POINT('Ctrl Pts',(-0.798192944264324,1.10862708047793,3.3015641839305));
#4645=CARTESIAN_POINT('Ctrl Pts',(-0.816190485307102,1.09537703279293,3.30316115873663));
#4646=CARTESIAN_POINT('Ctrl Pts',(-0.822478602137293,1.0906634261262,3.30371936451729));
#4647=CARTESIAN_POINT('Ctrl Pts',(-0.834114353457998,1.08178333884228,3.30475221749119));
#4648=CARTESIAN_POINT('Ctrl Pts',(-0.839471933883153,1.07763111566948,3.30522769340953));
#4649=CARTESIAN_POINT('Ctrl Pts',(-0.852258654810983,1.0675679389301,3.30636266090605));
#4650=CARTESIAN_POINT('Ctrl Pts',(-0.859657448699566,1.06161914207697,3.30701957774967));
#4651=CARTESIAN_POINT('Ctrl Pts',(-0.886017679348187,1.0399686115815,3.30936319281732));
#4652=CARTESIAN_POINT('Ctrl Pts',(-0.904617026419111,1.02383116504975,3.3110228108336));
#4653=CARTESIAN_POINT('Ctrl Pts',(-0.952913445246717,0.979583140827175,
3.31538032904864));
#4654=CARTESIAN_POINT('Ctrl Pts',(-0.981802780023006,0.950626585495604,
3.31803818661512));
#4655=CARTESIAN_POINT('Ctrl Pts',(-1.06027487272279,0.864572112582399,3.32555670272216));
#4656=CARTESIAN_POINT('Ctrl Pts',(-1.10643401002204,0.804644752684246,3.33036227633641));
#4657=CARTESIAN_POINT('Ctrl Pts',(-1.14737979714392,0.741266214733938,3.33530270583882));
#4658=CARTESIAN_POINT('Origin',(0.,0.,-1.10921167016993));
#4659=CARTESIAN_POINT('',(-1.14737960320836,0.74126651491986,4.05331207395161));
#4660=CARTESIAN_POINT('',(-1.14737996054503,0.741265961811063,3.93545337707765));
#4661=CARTESIAN_POINT('',(-1.14737960344596,0.741266514552077,-1.10921167016993));
#4662=CARTESIAN_POINT('Ctrl Pts',(-1.14737960320835,0.741266514919876,4.0533120739516));
#4663=CARTESIAN_POINT('Ctrl Pts',(-1.14208271428851,0.749465377521597,4.05260232715036));
#4664=CARTESIAN_POINT('Ctrl Pts',(-1.13669776340969,0.757607746088199,4.05189678629783));
#4665=CARTESIAN_POINT('Ctrl Pts',(-1.12623276791154,0.773068621195708,4.05055677229775));
#4666=CARTESIAN_POINT('Ctrl Pts',(-1.12116768136847,0.780396297951655,4.04992153297595));
#4667=CARTESIAN_POINT('Ctrl Pts',(-1.11252365663574,0.792643748789292,4.04886024585331));
#4668=CARTESIAN_POINT('Ctrl Pts',(-1.10898301203017,0.797589921894349,4.04843179245646));
#4669=CARTESIAN_POINT('Ctrl Pts',(-1.10074545301862,0.808936627221012,4.04744935267161));
#4670=CARTESIAN_POINT('Ctrl Pts',(-1.09602561976999,0.815320101528871,4.04689690162227));
#4671=CARTESIAN_POINT('Ctrl Pts',(-1.08231009944922,0.83353569409133,4.04532002524266));
#4672=CARTESIAN_POINT('Ctrl Pts',(-1.0731762985526,0.845263025136454,4.04430429451972));
#4673=CARTESIAN_POINT('Ctrl Pts',(-1.02646981293868,0.903253824884703,4.03926567098439));
#4674=CARTESIAN_POINT('Ctrl Pts',(-0.986085436215801,0.947177293421521,
4.03539596949304));
#4675=CARTESIAN_POINT('Ctrl Pts',(-0.891756768900862,1.03717577497354,4.02699261472622));
#4676=CARTESIAN_POINT('Ctrl Pts',(-0.836840198185006,1.0819712594372,4.02247995630053));
#4677=CARTESIAN_POINT('Ctrl Pts',(-0.743334435194101,1.1468491245818,4.01502833824987));
#4678=CARTESIAN_POINT('Ctrl Pts',(-0.706830231939513,1.16970058840442,4.01217111700904));
#4679=CARTESIAN_POINT('Ctrl Pts',(-0.654837484535871,1.1989243193653,4.00812789062007));
#4680=CARTESIAN_POINT('Ctrl Pts',(-0.640217648957412,1.20679450470004,4.00699386359582));
#4681=CARTESIAN_POINT('Ctrl Pts',(-0.614703614391421,1.21993516911713,4.00501756884494));
#4682=CARTESIAN_POINT('Ctrl Pts',(-0.603875911347207,1.22533106455954,4.00417971366749));
#4683=CARTESIAN_POINT('Ctrl Pts',(-0.581401026284826,1.23616099315731,4.00244154325445));
#4684=CARTESIAN_POINT('Ctrl Pts',(-0.569746001559793,1.2415758648254,4.00154067930209));
#4685=CARTESIAN_POINT('Ctrl Pts',(-0.539212367616805,1.25524119221851,3.99918104018996));
#4686=CARTESIAN_POINT('Ctrl Pts',(-0.520221057498316,1.26323014434989,3.99771377386539));
#4687=CARTESIAN_POINT('Ctrl Pts',(-0.401854854599082,1.30990065568995,3.9885660718615));
#4688=CARTESIAN_POINT('Ctrl Pts',(-0.298429681328461,1.33725790159594,3.98051900895684));
#4689=CARTESIAN_POINT('Ctrl Pts',(-0.150236307247837,1.35839697366796,3.96920211135042));
#4690=CARTESIAN_POINT('Ctrl Pts',(-0.10730545511775,1.36246072458844,3.96595408418624));
#4691=CARTESIAN_POINT('Ctrl Pts',(-0.0388316021290574,1.3656850844737,3.9608785237859));
#4692=CARTESIAN_POINT('Ctrl Pts',(-0.0133804685179279,1.36617158561613,
3.95901515310712));
#4693=CARTESIAN_POINT('Ctrl Pts',(0.0216790831681687,1.36586175577261,3.9564924867223));
#4694=CARTESIAN_POINT('Ctrl Pts',(0.031286155222495,1.36567547704529,3.95580580095057));
#4695=CARTESIAN_POINT('Ctrl Pts',(0.0476829726300942,1.36518442306701,3.95464249476632));
#4696=CARTESIAN_POINT('Ctrl Pts',(0.0544737087200887,1.36493032723659,3.95416328198851));
#4697=CARTESIAN_POINT('Ctrl Pts',(0.0690557680303902,1.36427568891862,3.9531399970622));
#4698=CARTESIAN_POINT('Ctrl Pts',(0.0768459492642894,1.36385906974782,3.9525967730755));
#4699=CARTESIAN_POINT('Ctrl Pts',(0.0988194919360919,1.36249504875585,3.95107316458252));
#4700=CARTESIAN_POINT('Ctrl Pts',(0.112992696456738,1.36139294106664,3.95010059541585));
#4701=CARTESIAN_POINT('Ctrl Pts',(0.206076618152484,1.35269094425106,3.94376495437454));
#4702=CARTESIAN_POINT('Ctrl Pts',(0.284224704194373,1.33845428421515,3.9386853819621));
#4703=CARTESIAN_POINT('Ctrl Pts',(0.418027768507446,1.30182220376946,3.92976785574138));
#4704=CARTESIAN_POINT('Ctrl Pts',(0.474263493616308,1.28240470081501,3.9259480926769));
#4705=CARTESIAN_POINT('Ctrl Pts',(0.563762887828581,1.24480712250549,3.91956057669029));
#4706=CARTESIAN_POINT('Ctrl Pts',(0.597852180167037,1.22879849714789,3.91705067584516));
#4707=CARTESIAN_POINT('Ctrl Pts',(0.645315937264399,1.20406621876125,3.91341627069128));
#4708=CARTESIAN_POINT('Ctrl Pts',(0.659267630754048,1.19648413018064,3.91233019116378));
#4709=CARTESIAN_POINT('Ctrl Pts',(0.683518133697531,1.18275219471639,3.91040903882213));
#4710=CARTESIAN_POINT('Ctrl Pts',(0.693874193412884,1.17670658236707,3.90957767915763));
#4711=CARTESIAN_POINT('Ctrl Pts',(0.715409870394442,1.16375143936165,3.90782498122307));
#4712=CARTESIAN_POINT('Ctrl Pts',(0.726571998716415,1.15681537187092,3.90690275625596));
#4713=CARTESIAN_POINT('Ctrl Pts',(0.756180610067992,1.13781921000519,3.90441827227017));
#4714=CARTESIAN_POINT('Ctrl Pts',(0.774437519508722,1.12547238895604,3.90284576740652));
#4715=CARTESIAN_POINT('Ctrl Pts',(0.86919202278311,1.05799427049293,3.89446210697466));
#4716=CARTESIAN_POINT('Ctrl Pts',(0.940115451856715,0.995501844818055,3.88737737808013));
#4717=CARTESIAN_POINT('Ctrl Pts',(1.05234617737867,0.873842881775787,3.87485639201078));
#4718=CARTESIAN_POINT('Ctrl Pts',(1.09649570494904,0.817760932135827,3.86946611340806));
#4719=CARTESIAN_POINT('Ctrl Pts',(1.14329340629184,0.747666636609126,3.86334664153477));
#4720=CARTESIAN_POINT('Ctrl Pts',(1.15036175866152,0.73674491384644,3.86240979884508));
#4721=CARTESIAN_POINT('Ctrl Pts',(1.16124025729096,0.719397538031531,3.86094972245166));
#4722=CARTESIAN_POINT('Ctrl Pts',(1.16515537050219,0.713039074835206,3.86042034670374));
#4723=CARTESIAN_POINT('Ctrl Pts',(1.17255871320137,0.700791626263941,3.85941220200326));
#4724=CARTESIAN_POINT('Ctrl Pts',(1.17605511838829,0.694908051639531,3.85893296885762));
#4725=CARTESIAN_POINT('Ctrl Pts',(1.18471601775466,0.680081320179104,3.85773737078964));
#4726=CARTESIAN_POINT('Ctrl Pts',(1.18982372780428,0.671105176515035,3.85702444775258));
#4727=CARTESIAN_POINT('Ctrl Pts',(1.20887819267441,0.636717909648691,3.8543310925829));
#4728=CARTESIAN_POINT('Ctrl Pts',(1.22211765267857,0.61092135060804,3.85238832599843));
#4729=CARTESIAN_POINT('Ctrl Pts',(1.26670573313672,0.516782102638326,3.84550368836485));
#4730=CARTESIAN_POINT('Ctrl Pts',(1.29322326128214,0.446298428134795,3.84072116467038));
#4731=CARTESIAN_POINT('Ctrl Pts',(1.33216551338004,0.309495122593954,3.83155770492004));
#4732=CARTESIAN_POINT('Ctrl Pts',(1.34574835656394,0.243746039092624,3.82720187021231));
#4733=CARTESIAN_POINT('Ctrl Pts',(1.35727655445153,0.155663679178198,3.8212389552559));
#4734=CARTESIAN_POINT('Ctrl Pts',(1.35958683732327,0.13399392273707,3.81976250220164));
#4735=CARTESIAN_POINT('Ctrl Pts',(1.36245381306657,0.0992320132374689,3.81737380587953));
#4736=CARTESIAN_POINT('Ctrl Pts',(1.36334222009293,0.0861705038528794,3.81647173942253));
#4737=CARTESIAN_POINT('Ctrl Pts',(1.3646852321018,0.061109487253447,3.81473125139453));
#4738=CARTESIAN_POINT('Ctrl Pts',(1.36516961348148,0.0491127518764308,3.81389382642674));
#4739=CARTESIAN_POINT('Ctrl Pts',(1.3659226523147,0.0214051459700489,3.8119491641948));
#4740=CARTESIAN_POINT('Ctrl Pts',(1.36607848364207,0.00569318591026028,
3.81083858586827));
#4741=CARTESIAN_POINT('Ctrl Pts',(1.36570829514905,-0.0447853615416102,
3.80724383510106));
#4742=CARTESIAN_POINT('Ctrl Pts',(1.36412602245752,-0.0795279528043798,
3.80472851984214));
#4743=CARTESIAN_POINT('Ctrl Pts',(1.35220396878944,-0.221671866906366,3.7942647253221));
#4744=CARTESIAN_POINT('Ctrl Pts',(1.33048410786226,-0.327720530562291,3.78601210613619));
#4745=CARTESIAN_POINT('Ctrl Pts',(1.28398875824084,-0.467882817824271,3.77494227704189));
#4746=CARTESIAN_POINT('Ctrl Pts',(1.26980423902497,-0.505113120920413,3.77199031408476));
#4747=CARTESIAN_POINT('Ctrl Pts',(1.2496141265528,-0.551854625200745,3.76831076386427));
#4748=CARTESIAN_POINT('Ctrl Pts',(1.245092411278,-0.561982117374848,3.76751519229196));
#4749=CARTESIAN_POINT('Ctrl Pts',(1.23749092837609,-0.578465254763044,3.76622438433666));
#4750=CARTESIAN_POINT('Ctrl Pts',(1.23448441474231,-0.584853901383183,3.76572509068309));
#4751=CARTESIAN_POINT('Ctrl Pts',(1.22828628854823,-0.597763747123393,3.76471860349242));
#4752=CARTESIAN_POINT('Ctrl Pts',(1.22509197531668,-0.604283346014246,3.76421158099726));
#4753=CARTESIAN_POINT('Ctrl Pts',(1.21646542919891,-0.621540548594131,3.76287205557516));
#4754=CARTESIAN_POINT('Ctrl Pts',(1.21094289942153,-0.632232641821085,3.76204476736161));
#4755=CARTESIAN_POINT('Ctrl Pts',(1.18005482482532,-0.690144623905229,3.75757075799206));
#4756=CARTESIAN_POINT('Ctrl Pts',(1.15206524884962,-0.735918462828498,3.75405872010642));
#4757=CARTESIAN_POINT('Ctrl Pts',(1.07552641805855,-0.845972513716948,3.74537992768325));
#4758=CARTESIAN_POINT('Ctrl Pts',(1.02385599755088,-0.9078245429899,3.74027461564287));
#4759=CARTESIAN_POINT('Ctrl Pts',(0.935755798912973,-0.996132303607631,
3.73211587373916));
#4760=CARTESIAN_POINT('Ctrl Pts',(0.902963622464841,-1.02595057475716,3.72917832519551));
#4761=CARTESIAN_POINT('Ctrl Pts',(0.855852805372316,-1.06477826029701,3.72504118545221));
#4762=CARTESIAN_POINT('Ctrl Pts',(0.842727860078257,-1.07519601968212,3.72389701753201));
#4763=CARTESIAN_POINT('Ctrl Pts',(0.819783281569719,-1.09272975537118,3.72190889579552));
#4764=CARTESIAN_POINT('Ctrl Pts',(0.810054215651539,-1.09996140764752,3.72106950492588));
#4765=CARTESIAN_POINT('Ctrl Pts',(0.789857185221242,-1.11456065571255,3.71933355074658));
#4766=CARTESIAN_POINT('Ctrl Pts',(0.779379358715203,-1.12191248491214,3.71843650312691));
#4767=CARTESIAN_POINT('Ctrl Pts',(0.751983224858947,-1.14056615203839,3.7160991701994));
#4768=CARTESIAN_POINT('Ctrl Pts',(0.734913510345819,-1.15163881975122,3.7146506943042));
#4769=CARTESIAN_POINT('Ctrl Pts',(0.625347417565087,-1.21928339982075,3.70539712076858));
#4770=CARTESIAN_POINT('Ctrl Pts',(0.52665296724612,-1.26504528002418,3.69721042016922));
#4771=CARTESIAN_POINT('Ctrl Pts',(0.383456552088563,-1.31175500748649,3.68582538989112));
#4772=CARTESIAN_POINT('Ctrl Pts',(0.342711785579238,-1.3229849390831,3.68264363424592));
#4773=CARTESIAN_POINT('Ctrl Pts',(0.284602036170661,-1.33613554930096,3.67823387564487));
#4774=CARTESIAN_POINT('Ctrl Pts',(0.267621793092662,-1.33963993639185,3.67696053573363));
#4775=CARTESIAN_POINT('Ctrl Pts',(0.237340589885816,-1.34529059801129,3.67472165685656));
#4776=CARTESIAN_POINT('Ctrl Pts',(0.2240660780003,-1.34756512869085,3.67375098439123));
#4777=CARTESIAN_POINT('Ctrl Pts',(0.203287084045003,-1.3508099643597,3.67225053306896));
#4778=CARTESIAN_POINT('Ctrl Pts',(0.195804893242241,-1.35191480839153,3.67171406710795));
#4779=CARTESIAN_POINT('Ctrl Pts',(0.181578765653415,-1.35389489612398,3.67070179801365));
#4780=CARTESIAN_POINT('Ctrl Pts',(0.174836925363774,-1.35478200811832,3.67022541829852));
#4781=CARTESIAN_POINT('Ctrl Pts',(0.158093345505703,-1.35685811170385,3.6690500585778));
#4782=CARTESIAN_POINT('Ctrl Pts',(0.148084307728478,-1.35798692714812,3.66835426286463));
#4783=CARTESIAN_POINT('Ctrl Pts',(0.111189533953986,-1.36173512179498,3.66581148366647));
#4784=CARTESIAN_POINT('Ctrl Pts',(0.0842385544339021,-1.36366775507627,
3.66399696632538));
#4785=CARTESIAN_POINT('Ctrl Pts',(-0.019443266028587,-1.36801664787397,
3.65712067915906));
#4786=CARTESIAN_POINT('Ctrl Pts',(-0.0962727424055962,-1.36476404760319,
3.65223780242633));
#4787=CARTESIAN_POINT('Ctrl Pts',(-0.221135549751428,-1.34887583653217,
3.64413073758124));
#4788=CARTESIAN_POINT('Ctrl Pts',(-0.26947205565319,-1.34005644581843,3.64095052757975));
#4789=CARTESIAN_POINT('Ctrl Pts',(-0.339819345587557,-1.32326050189445,
3.63617065003189));
#4790=CARTESIAN_POINT('Ctrl Pts',(-0.362270082488954,-1.31729109870488,
3.63462218416654));
#4791=CARTESIAN_POINT('Ctrl Pts',(-0.4033346413958,-1.30524332028537,3.63173847237445));
#4792=CARTESIAN_POINT('Ctrl Pts',(-0.421991092386243,-1.29933152507113,
3.63040840594825));
#4793=CARTESIAN_POINT('Ctrl Pts',(-0.452482205282357,-1.28894365039595,
3.62819794925531));
#4794=CARTESIAN_POINT('Ctrl Pts',(-0.464393491762242,-1.28470017760663,
3.62732508311039));
#4795=CARTESIAN_POINT('Ctrl Pts',(-0.487557531635201,-1.27608360413919,
3.62560832775299));
#4796=CARTESIAN_POINT('Ctrl Pts',(-0.498814630864025,-1.27172546524865,
3.6247649946738));
#4797=CARTESIAN_POINT('Ctrl Pts',(-0.523443209477178,-1.26181330577374,
3.62289926627383));
#4798=CARTESIAN_POINT('Ctrl Pts',(-0.536786969811317,-1.25619478291802,
3.62187482287878));
#4799=CARTESIAN_POINT('Ctrl Pts',(-0.582914280927707,-1.23590327854429,
3.61828456741328));
#4800=CARTESIAN_POINT('Ctrl Pts',(-0.615204050231333,-1.22015144023272,
3.61568375923047));
#4801=CARTESIAN_POINT('Ctrl Pts',(-0.761996032589823,-1.1412334505094,3.60344290419936));
#4802=CARTESIAN_POINT('Ctrl Pts',(-0.867653545564788,-1.06311889650848,
3.59333082567513));
#4803=CARTESIAN_POINT('Ctrl Pts',(-0.975135212519098,-0.956810119947042,
3.58220864934236));
#4804=CARTESIAN_POINT('Ctrl Pts',(-0.989352285032393,-0.94210214585143,
3.58071942172653));
#4805=CARTESIAN_POINT('Ctrl Pts',(-1.00925185925515,-0.9205679189021,3.57861523452353));
#4806=CARTESIAN_POINT('Ctrl Pts',(-1.01520583026031,-0.913997670562352,
3.57798301730475));
#4807=CARTESIAN_POINT('Ctrl Pts',(-1.02513296918479,-0.902826305626476,
3.57692508918283));
#4808=CARTESIAN_POINT('Ctrl Pts',(-1.02914000414453,-0.898255976777378,
3.57649701131207));
#4809=CARTESIAN_POINT('Ctrl Pts',(-1.03832843977742,-0.887633660887679,
3.57551303732085));
#4810=CARTESIAN_POINT('Ctrl Pts',(-1.04348759392396,-0.881562881559416,
3.57495870596985));
#4811=CARTESIAN_POINT('Ctrl Pts',(-1.0582045244594,-0.863935228960948,3.5733708738656));
#4812=CARTESIAN_POINT('Ctrl Pts',(-1.0676258131772,-0.85226525467405,3.57234625392496));
#4813=CARTESIAN_POINT('Ctrl Pts',(-1.11474723850734,-0.791888838203964,
3.56716523136413));
#4814=CARTESIAN_POINT('Ctrl Pts',(-1.14931828578632,-0.740822855988824,
3.56317243354008));
#4815=CARTESIAN_POINT('Ctrl Pts',(-1.20839521058935,-0.639410895328169,
3.55561232545762));
#4816=CARTESIAN_POINT('Ctrl Pts',(-1.23348606879065,-0.589556823505201,
3.55204751233129));
#4817=CARTESIAN_POINT('Ctrl Pts',(-1.27643807509572,-0.489383012109559,
3.54496457633142));
#4818=CARTESIAN_POINT('Ctrl Pts',(-1.29453646541553,-0.439277009436666,
3.54145785384923));
#4819=CARTESIAN_POINT('Ctrl Pts',(-1.31469513353201,-0.371276192092175,
3.53666116900418));
#4820=CARTESIAN_POINT('Ctrl Pts',(-1.319395445904,-0.354210268267431,3.53545455005704));
#4821=CARTESIAN_POINT('Ctrl Pts',(-1.32679414353658,-0.325152640008996,
3.53339268606863));
#4822=CARTESIAN_POINT('Ctrl Pts',(-1.32966477699609,-0.313206804550987,
3.53254295312185));
#4823=CARTESIAN_POINT('Ctrl Pts',(-1.3351384253474,-0.288995782869566,3.53081574687679));
#4824=CARTESIAN_POINT('Ctrl Pts',(-1.33773447463021,-0.276730255366954,
3.52993814606494));
#4825=CARTESIAN_POINT('Ctrl Pts',(-1.34384418853653,-0.245765658863391,
3.52771529941282));
#4826=CARTESIAN_POINT('Ctrl Pts',(-1.34713659244508,-0.227026207366572,
3.52636334799685));
#4827=CARTESIAN_POINT('Ctrl Pts',(-1.36072517230166,-0.138923985954145,
3.51997258211696));
#4828=CARTESIAN_POINT('Ctrl Pts',(-1.36606043483702,-0.0689134526760029,
3.51478621825296));
#4829=CARTESIAN_POINT('Ctrl Pts',(-1.36591336273895,0.100237112258158,3.50206631011594));
#4830=CARTESIAN_POINT('Ctrl Pts',(-1.35505465627204,0.198985499722037,3.49447306626828));
#4831=CARTESIAN_POINT('Ctrl Pts',(-1.33054415173034,0.309530476555009,3.48622831422803));
#4832=CARTESIAN_POINT('Ctrl Pts',(-1.32726100393754,0.32331891812312,3.48520511786736));
#4833=CARTESIAN_POINT('Ctrl Pts',(-1.32184107198603,0.344605418343624,3.48363606264008));
#4834=CARTESIAN_POINT('Ctrl Pts',(-1.31985381764948,0.352140059614764,3.48308274092917));
#4835=CARTESIAN_POINT('Ctrl Pts',(-1.31601228328548,0.366215623071584,3.48205346665481));
#4836=CARTESIAN_POINT('Ctrl Pts',(-1.3141735713459,0.372760028651765,3.48157676048259));
#4837=CARTESIAN_POINT('Ctrl Pts',(-1.3096132146034,0.388538137378118,3.48043151329544));
#4838=CARTESIAN_POINT('Ctrl Pts',(-1.30684269579416,0.397757260168607,3.4797656766112));
#4839=CARTESIAN_POINT('Ctrl Pts',(-1.29635441351563,0.431364751593982,3.47734801008214));
#4840=CARTESIAN_POINT('Ctrl Pts',(-1.28804901717805,0.455565846818251,3.47562555715607));
#4841=CARTESIAN_POINT('Ctrl Pts',(-1.2638145937603,0.520208419083282,3.47103923109373));
#4842=CARTESIAN_POINT('Ctrl Pts',(-1.24662722097694,0.560147477642661,3.46822074503088));
#4843=CARTESIAN_POINT('Ctrl Pts',(-1.20366875163054,0.648155048570496,3.4619067818998));
#4844=CARTESIAN_POINT('Ctrl Pts',(-1.17688798654137,0.69559158824865,3.45842855588962));
#4845=CARTESIAN_POINT('Ctrl Pts',(-1.14737936922177,0.741266877099097,3.45490258866455));
#4846=CARTESIAN_POINT('',(-1.36599991081998,-0.000493598843714221,3.39184234729853));
#4847=CARTESIAN_POINT('Ctrl Pts',(-1.14737979714392,0.741266214733938,3.33530270583882));
#4848=CARTESIAN_POINT('Ctrl Pts',(-1.16553173502964,0.713169471087583,3.33749287913283));
#4849=CARTESIAN_POINT('Ctrl Pts',(-1.18265914426148,0.684394393768033,3.33970818833468));
#4850=CARTESIAN_POINT('Ctrl Pts',(-1.2088152291256,0.636525520319797,3.34337429489948));
#4851=CARTESIAN_POINT('Ctrl Pts',(-1.21847876351361,0.617825558236379,3.34480181944772));
#4852=CARTESIAN_POINT('Ctrl Pts',(-1.23337896702955,0.587281651913514,3.34713066806653));
#4853=CARTESIAN_POINT('Ctrl Pts',(-1.23888622487875,0.575573033670965,3.34802273391502));
#4854=CARTESIAN_POINT('Ctrl Pts',(-1.24920175812161,0.552807650407034,3.34975690199215));
#4855=CARTESIAN_POINT('Ctrl Pts',(-1.25403162017598,0.541761949615154,3.35059818068308));
#4856=CARTESIAN_POINT('Ctrl Pts',(-1.26506497396007,0.515590770887915,3.35259190912998));
#4857=CARTESIAN_POINT('Ctrl Pts',(-1.27114425800465,0.50041529309827,3.35374833556806));
#4858=CARTESIAN_POINT('Ctrl Pts',(-1.291535404168,0.446742671110167,3.35784152285206));
#4859=CARTESIAN_POINT('Ctrl Pts',(-1.30438099998516,0.407715971275957,3.36082422281042));
#4860=CARTESIAN_POINT('Ctrl Pts',(-1.34904172740674,0.248147434709551,3.37304616914902));
#4861=CARTESIAN_POINT('Ctrl Pts',(-1.36604493655855,0.124111950090538,3.38267270765495));
#4862=CARTESIAN_POINT('Ctrl Pts',(-1.36599991081998,-0.000493598843714221,
3.39184234729853));
#4863=CARTESIAN_POINT('Ctrl Pts',(-1.36599991021368,-0.000495273880241242,
3.39184247056333));
#4864=CARTESIAN_POINT('Ctrl Pts',(-1.36599590393764,-0.0115448626693739,
3.39265560201651));
#4865=CARTESIAN_POINT('Ctrl Pts',(-1.36585782719199,-0.0225944159718812,
3.39346426080702));
#4866=CARTESIAN_POINT('Ctrl Pts',(-1.36535745340085,-0.0429057471209498,
3.39494118066293));
#4867=CARTESIAN_POINT('Ctrl Pts',(-1.36503495032421,-0.0521677491801081,
3.3956110004149));
#4868=CARTESIAN_POINT('Ctrl Pts',(-1.36429798411226,-0.0685399176910465,
3.39678775934093));
#4869=CARTESIAN_POINT('Ctrl Pts',(-1.36392213285538,-0.0756513768739628,
3.39729647374242));
#4870=CARTESIAN_POINT('Ctrl Pts',(-1.36311177424707,-0.0890022657562773,
3.39824657357646));
#4871=CARTESIAN_POINT('Ctrl Pts',(-1.36268999543079,-0.0952422897295007,
3.39868860374223));
#4872=CARTESIAN_POINT('Ctrl Pts',(-1.36168841013103,-0.108687234500898,
3.3996363238915));
#4873=CARTESIAN_POINT('Ctrl Pts',(-1.36109424530452,-0.115890909044641,
3.40014121252018));
#4874=CARTESIAN_POINT('Ctrl Pts',(-1.35937157385279,-0.134930645165359,
3.40146881798367));
#4875=CARTESIAN_POINT('Ctrl Pts',(-1.35814564580875,-0.146757568167012,
3.40228648122653));
#4876=CARTESIAN_POINT('Ctrl Pts',(-1.35093711826357,-0.208436551116047,
3.40652114110718));
#4877=CARTESIAN_POINT('Ctrl Pts',(-1.34236309956909,-0.257952189750895,
3.40982029434804));
#4878=CARTESIAN_POINT('Ctrl Pts',(-1.30891028491174,-0.403048675850838,
3.41947895855282));
#4879=CARTESIAN_POINT('Ctrl Pts',(-1.27638634794584,-0.496519961800821,
3.4257101206697));
#4880=CARTESIAN_POINT('Ctrl Pts',(-1.22406380928573,-0.606769439937662,
3.43377357347458));
#4881=CARTESIAN_POINT('Ctrl Pts',(-1.2135123105183,-0.627605880511909,3.43533005965148));
#4882=CARTESIAN_POINT('Ctrl Pts',(-1.19310952938806,-0.665456002229991,
3.43822705981652));
#4883=CARTESIAN_POINT('Ctrl Pts',(-1.18341504237,-0.682547297101288,3.43956230899738));
#4884=CARTESIAN_POINT('Ctrl Pts',(-1.16687473620726,-0.71029540683938,3.44177888727376));
#4885=CARTESIAN_POINT('Ctrl Pts',(-1.16024314379836,-0.721077002636595,
3.44265260148688));
#4886=CARTESIAN_POINT('Ctrl Pts',(-1.1470036537035,-0.741946091713442,3.44436921744094));
#4887=CARTESIAN_POINT('Ctrl Pts',(-1.14041010181182,-0.75204133389026,3.44521154088886));
#4888=CARTESIAN_POINT('Ctrl Pts',(-1.12563396406584,-0.774023514954371,
3.44707278857188));
#4889=CARTESIAN_POINT('Ctrl Pts',(-1.11739499914696,-0.785870606613262,
3.44809372593308));
#4890=CARTESIAN_POINT('Ctrl Pts',(-1.08817729054475,-0.82649522359816,3.45165840230394));
#4891=CARTESIAN_POINT('Ctrl Pts',(-1.06626363181038,-0.854579215413105,
3.45423648440195));
#4892=CARTESIAN_POINT('Ctrl Pts',(-0.958663113371388,-0.981887973037428,
3.46647542244677));
#4893=CARTESIAN_POINT('Ctrl Pts',(-0.860093335543366,-1.06928526187117,
3.47661358361265));
#4894=CARTESIAN_POINT('Ctrl Pts',(-0.733445674074164,-1.15257745967072,
3.4877669224401));
#4895=CARTESIAN_POINT('Ctrl Pts',(-0.716042083561599,-1.16346946749612,
3.48926173826627));
#4896=CARTESIAN_POINT('Ctrl Pts',(-0.690769491677209,-1.1785042679643,3.49137217147332));
#4897=CARTESIAN_POINT('Ctrl Pts',(-0.683096150379825,-1.18296849513451,
3.49200518411794));
#4898=CARTESIAN_POINT('Ctrl Pts',(-0.670096600703223,-1.19036275376725,
3.49306389611154));
#4899=CARTESIAN_POINT('Ctrl Pts',(-0.664793574219285,-1.19333249718736,
3.49349197360485));
#4900=CARTESIAN_POINT('Ctrl Pts',(-0.652504229050625,-1.20010729082176,
3.49447514654437));
#4901=CARTESIAN_POINT('Ctrl Pts',(-0.645504247622066,-1.20388685211977,
3.49502868797276));
#4902=CARTESIAN_POINT('Ctrl Pts',(-0.625257865745741,-1.21459129155047,
3.49661234869313));
#4903=CARTESIAN_POINT('Ctrl Pts',(-0.61192985471768,-1.22136043104996,3.49763365570756));
#4904=CARTESIAN_POINT('Ctrl Pts',(-0.543687372610899,-1.25462234635429,
3.50276984381055));
#4905=CARTESIAN_POINT('Ctrl Pts',(-0.487148698063449,-1.27763883255426,
3.50672435641322));
#4906=CARTESIAN_POINT('Ctrl Pts',(-0.377227444142663,-1.31402396401995,
3.51418421326014));
#4907=CARTESIAN_POINT('Ctrl Pts',(-0.324210935829117,-1.32809889352064,
3.51768782599946));
#4908=CARTESIAN_POINT('Ctrl Pts',(-0.234467292565063,-1.34622876762799,
3.5236325436535));
#4909=CARTESIAN_POINT('Ctrl Pts',(-0.198164846547003,-1.3520492661629,3.52604046544842));
#4910=CARTESIAN_POINT('Ctrl Pts',(-0.134416205208806,-1.35964767799476,
3.53031418761997));
#4911=CARTESIAN_POINT('Ctrl Pts',(-0.107068639935826,-1.36207403084053,
3.53216184110225));
#4912=CARTESIAN_POINT('Ctrl Pts',(-0.0654976611379493,-1.36450267109421,
3.53500254817122));
#4913=CARTESIAN_POINT('Ctrl Pts',(-0.0513157789751146,-1.36510957370476,
3.53597726131334));
#4914=CARTESIAN_POINT('Ctrl Pts',(-0.0252719685231917,-1.36581769795545,
3.53777884746831));
#4915=CARTESIAN_POINT('Ctrl Pts',(-0.0134131268667021,-1.3659856254572,
3.53860359623135));
#4916=CARTESIAN_POINT('Ctrl Pts',(0.0127452574109342,-1.36601538249126,
3.54043329222531));
#4917=CARTESIAN_POINT('Ctrl Pts',(0.0270433075364403,-1.36580712355398,
3.54144029060256));
#4918=CARTESIAN_POINT('Ctrl Pts',(0.0684568887477681,-1.36455337976784,
3.54437820817033));
#4919=CARTESIAN_POINT('Ctrl Pts',(0.0955464838194545,-1.36292441382573,
3.54632646322206));
#4920=CARTESIAN_POINT('Ctrl Pts',(0.223030629400899,-1.35143923130649,3.55562546791917));
#4921=CARTESIAN_POINT('Ctrl Pts',(0.322169169590384,-1.33128952242584,3.56327227169015));
#4922=CARTESIAN_POINT('Ctrl Pts',(0.455203198504137,-1.28851056039669,3.57382485878223));
#4923=CARTESIAN_POINT('Ctrl Pts',(0.491714713228076,-1.27502407883675,3.57674892830087));
#4924=CARTESIAN_POINT('Ctrl Pts',(0.549601951149589,-1.25078476467622,3.58138684311496));
#4925=CARTESIAN_POINT('Ctrl Pts',(0.571357955372071,-1.24099761615838,3.58313023950591));
#4926=CARTESIAN_POINT('Ctrl Pts',(0.601302874754913,-1.22657202304881,3.58552000240874));
#4927=CARTESIAN_POINT('Ctrl Pts',(0.609715879559031,-1.22241181025489,3.58619028972989));
#4928=CARTESIAN_POINT('Ctrl Pts',(0.624118089656554,-1.21510426268439,3.58733500580171));
#4929=CARTESIAN_POINT('Ctrl Pts',(0.630127847530296,-1.21199862320992,3.58781181027507));
#4930=CARTESIAN_POINT('Ctrl Pts',(0.643123128445849,-1.20516030513938,3.58884077540917));
#4931=CARTESIAN_POINT('Ctrl Pts',(0.650099596850043,-1.20141135399056,3.58939195358872));
#4932=CARTESIAN_POINT('Ctrl Pts',(0.670000402713599,-1.19049312508178,3.5909618661344));
#4933=CARTESIAN_POINT('Ctrl Pts',(0.682841959688594,-1.18317425709462,3.59197202074394));
#4934=CARTESIAN_POINT('Ctrl Pts',(0.755582149701171,-1.14013810094253,3.59769223977836));
#4935=CARTESIAN_POINT('Ctrl Pts',(0.812801468170653,-1.10007970158708,3.60218837885737));
#4936=CARTESIAN_POINT('Ctrl Pts',(0.917105573820877,-1.01445722826584,3.61086776528305));
#4937=CARTESIAN_POINT('Ctrl Pts',(0.964466749904116,-0.969540828489386,
3.61504184624491));
#4938=CARTESIAN_POINT('Ctrl Pts',(1.03522581527352,-0.892098958042945,3.62193059556457));
#4939=CARTESIAN_POINT('Ctrl Pts',(1.06071960904808,-0.86163014194861,3.62457355439362));
#4940=CARTESIAN_POINT('Ctrl Pts',(1.09467192920382,-0.817258029479973,3.6283649546594));
#4941=CARTESIAN_POINT('Ctrl Pts',(1.10426633390737,-0.804246943399908,3.62947003048228));
#4942=CARTESIAN_POINT('Ctrl Pts',(1.12059310783276,-0.781262933244479,3.63141266985506));
#4943=CARTESIAN_POINT('Ctrl Pts',(1.12742893162224,-0.771365459600188,3.63224624312655));
#4944=CARTESIAN_POINT('Ctrl Pts',(1.14138492625693,-0.750576932412514,3.63399170797769));
#4945=CARTESIAN_POINT('Ctrl Pts',(1.1484819429641,-0.739671878146143,3.63490434229904));
#4946=CARTESIAN_POINT('Ctrl Pts',(1.16683910735932,-0.71056357912917,3.63733350796976));
#4947=CARTESIAN_POINT('Ctrl Pts',(1.17782864122889,-0.692194844544361,3.6388594965795));
#4948=CARTESIAN_POINT('Ctrl Pts',(1.23795244952326,-0.586119236691234,3.64763783672259));
#4949=CARTESIAN_POINT('Ctrl Pts',(1.27770942655118,-0.49347122671628,3.65520850989065));
#4950=CARTESIAN_POINT('Ctrl Pts',(1.32037549052948,-0.353126416749277,3.66630314156843));
#4951=CARTESIAN_POINT('Ctrl Pts',(1.33156146138188,-0.308276192986346,3.66979062979937));
#4952=CARTESIAN_POINT('Ctrl Pts',(1.34556562266081,-0.236884662234721,3.67518397886225));
#4953=CARTESIAN_POINT('Ctrl Pts',(1.34991674418092,-0.210680302780619,3.67713053355291));
#4954=CARTESIAN_POINT('Ctrl Pts',(1.35481762374498,-0.174700646966227,3.67974444137898));
#4955=CARTESIAN_POINT('Ctrl Pts',(1.35603039832201,-0.165023279093229,3.68044171414854));
#4956=CARTESIAN_POINT('Ctrl Pts',(1.3579143844052,-0.148562995015698,3.68161698966298));
#4957=CARTESIAN_POINT('Ctrl Pts',(1.35863865136182,-0.141786679083786,3.68209772654906));
#4958=CARTESIAN_POINT('Ctrl Pts',(1.36007574950981,-0.127317083786312,3.68311739354062));
#4959=CARTESIAN_POINT('Ctrl Pts',(1.36077407516135,-0.11962277366247,3.68365555954664));
#4960=CARTESIAN_POINT('Ctrl Pts',(1.3625435325228,-0.0980994234155056,3.68515070585198));
#4961=CARTESIAN_POINT('Ctrl Pts',(1.36346941298701,-0.0842589563290845,
3.68610032068763));
#4962=CARTESIAN_POINT('Ctrl Pts',(1.36853611040705,0.0139130226736218,3.69276751680514));
#4963=CARTESIAN_POINT('Ctrl Pts',(1.36506151870747,0.0984655037191526,3.6981594842981));
#4964=CARTESIAN_POINT('Ctrl Pts',(1.34626919687876,0.23812495429526,3.70721932970824));
#4965=CARTESIAN_POINT('Ctrl Pts',(1.33527715486039,0.293561904997251,3.71085588256634));
#4966=CARTESIAN_POINT('Ctrl Pts',(1.31158314690899,0.383455632897793,3.71697984121087));
#4967=CARTESIAN_POINT('Ctrl Pts',(1.30086864009321,0.418364668187871,3.71941589234884));
#4968=CARTESIAN_POINT('Ctrl Pts',(1.28356289872946,0.467620604524368,3.72296258118187));
#4969=CARTESIAN_POINT('Ctrl Pts',(1.27810093328913,0.482349162796248,3.72403739850416));
#4970=CARTESIAN_POINT('Ctrl Pts',(1.268032640941,0.50812638564804,3.72594563063877));
#4971=CARTESIAN_POINT('Ctrl Pts',(1.26353273571693,0.519214996137751,3.72677549200968));
#4972=CARTESIAN_POINT('Ctrl Pts',(1.25375755346116,0.542422966530153,3.72853214012195));
#4973=CARTESIAN_POINT('Ctrl Pts',(1.2484509209254,0.554527685322951,3.72945989966749));
#4974=CARTESIAN_POINT('Ctrl Pts',(1.23366978006981,0.586956257984964,3.73197764540899));
#4975=CARTESIAN_POINT('Ctrl Pts',(1.22386947130074,0.6071261707956,3.73357837087617));
#4976=CARTESIAN_POINT('Ctrl Pts',(1.17449220752656,0.702690557446264,3.74133560899769));
#4977=CARTESIAN_POINT('Ctrl Pts',(1.12842558306736,0.774504603228048,3.74770851068264));
#4978=CARTESIAN_POINT('Ctrl Pts',(1.04165183636111,0.885450800707789,3.75835788231333));
#4979=CARTESIAN_POINT('Ctrl Pts',(1.00466374234151,0.927207042255812,3.76258409997924));
#4980=CARTESIAN_POINT('Ctrl Pts',(0.94426543338702,0.987520293450898,3.76893167161489));
#4981=CARTESIAN_POINT('Ctrl Pts',(0.92262669958857,1.00776673976217,3.77110945391525));
#4982=CARTESIAN_POINT('Ctrl Pts',(0.892730303081213,1.03396862930749,3.77397442990409));
#4983=CARTESIAN_POINT('Ctrl Pts',(0.88504139699246,1.04055766863373,3.77469908113244));
#4984=CARTESIAN_POINT('Ctrl Pts',(0.872009912232269,1.0514760945688,3.77590599794318));
#4985=CARTESIAN_POINT('Ctrl Pts',(0.866706726745205,1.05585165765819,3.77639136204842));
#4986=CARTESIAN_POINT('Ctrl Pts',(0.855500007999725,1.06495678169794,3.77740462625131));
#4987=CARTESIAN_POINT('Ctrl Pts',(0.849589884403435,1.06967763642221,3.77793195413955));
#4988=CARTESIAN_POINT('Ctrl Pts',(0.833041458879929,1.08267240904025,3.77938999568114));
#4989=CARTESIAN_POINT('Ctrl Pts',(0.822319152640842,1.09083860538404,3.78031375946463));
#4990=CARTESIAN_POINT('Ctrl Pts',(0.739502471477243,1.15199722447806,3.78730551441112));
#4991=CARTESIAN_POINT('Ctrl Pts',(0.662469481435449,1.19795662710755,3.79300179560354));
#4992=CARTESIAN_POINT('Ctrl Pts',(0.508495851634213,1.27039145424832,3.80394614091116));
#4993=CARTESIAN_POINT('Ctrl Pts',(0.432617423839096,1.29819198807891,3.80916299178731));
#4994=CARTESIAN_POINT('Ctrl Pts',(0.336132386309956,1.3241382520869,3.81589928524886));
#4995=CARTESIAN_POINT('Ctrl Pts',(0.317426613634589,1.32874654299215,3.81720918059708));
#4996=CARTESIAN_POINT('Ctrl Pts',(0.286353251965,1.33570809263181,3.81939503016453));
#4997=CARTESIAN_POINT('Ctrl Pts',(0.274039060475738,1.33828878377039,3.8202638004783));
#4998=CARTESIAN_POINT('Ctrl Pts',(0.249809535384183,1.34301815016927,3.82197904448198));
#4999=CARTESIAN_POINT('Ctrl Pts',(0.237897790069512,1.34517923731474,3.82282504374344));
#5000=CARTESIAN_POINT('Ctrl Pts',(0.20880856103766,1.35005829695095,3.8248984743046));
#5001=CARTESIAN_POINT('Ctrl Pts',(0.191605266156183,1.3526070356324,3.82613100596007));
#5002=CARTESIAN_POINT('Ctrl Pts',(0.128238249493952,1.36076202019167,3.83069628795973));
#5003=CARTESIAN_POINT('Ctrl Pts',(0.0818499355370338,1.36433795355393,3.83408895335321));
#5004=CARTESIAN_POINT('Ctrl Pts',(-0.0811414757157418,1.368560200967,3.84617946892474));
#5005=CARTESIAN_POINT('Ctrl Pts',(-0.19755208203603,1.35665440610863,3.85516547647375));
#5006=CARTESIAN_POINT('Ctrl Pts',(-0.331179380679531,1.32540722161005,3.86526526453535));
#5007=CARTESIAN_POINT('Ctrl Pts',(-0.351217838482758,1.32023870093808,3.86677226365154));
#5008=CARTESIAN_POINT('Ctrl Pts',(-0.37970093514585,1.31219757332659,3.86889652713996));
#5009=CARTESIAN_POINT('Ctrl Pts',(-0.388245927499615,1.30969476687042,3.86953148534938));
#5010=CARTESIAN_POINT('Ctrl Pts',(-0.402584791431123,1.30534227775591,3.87059236111436));
#5011=CARTESIAN_POINT('Ctrl Pts',(-0.408391666412527,1.30353719877729,3.87102068167333));
#5012=CARTESIAN_POINT('Ctrl Pts',(-0.421749818543827,1.2992867595422,3.87200287326152));
#5013=CARTESIAN_POINT('Ctrl Pts',(-0.429292111715352,1.2968142826657,3.87255520914989));
#5014=CARTESIAN_POINT('Ctrl Pts',(-0.450893441651801,1.28952392612613,3.87413184967456));
#5015=CARTESIAN_POINT('Ctrl Pts',(-0.464896449607035,1.28454201474701,3.8751474611269));
#5016=CARTESIAN_POINT('Ctrl Pts',(-0.539905106977256,1.25646850381103,3.8805670161767));
#5017=CARTESIAN_POINT('Ctrl Pts',(-0.599285387177935,1.22925571090017,3.88478546734755));
#5018=CARTESIAN_POINT('Ctrl Pts',(-0.71631776752998,1.16511710113681,3.89337526959117));
#5019=CARTESIAN_POINT('Ctrl Pts',(-0.773594151092775,1.12790095317371,3.8977345822808));
#5020=CARTESIAN_POINT('Ctrl Pts',(-0.860239278385417,1.06188625681575,3.90488121619118));
#5021=CARTESIAN_POINT('Ctrl Pts',(-0.891506318635939,1.03577509280707,3.90758897541789));
#5022=CARTESIAN_POINT('Ctrl Pts',(-0.933591065331616,0.997311106591054,
3.91145666486047));
#5023=CARTESIAN_POINT('Ctrl Pts',(-0.945425281133438,0.98609975171272,3.91257071098413));
#5024=CARTESIAN_POINT('Ctrl Pts',(-0.965652492257582,0.966238287242019,
3.91452367020683));
#5025=CARTESIAN_POINT('Ctrl Pts',(-0.974137048655124,0.957683746254458,
3.91535846228015));
#5026=CARTESIAN_POINT('Ctrl Pts',(-0.99150868888105,0.939699098821539,3.91710122539235));
#5027=CARTESIAN_POINT('Ctrl Pts',(-1.00037693777964,0.930252566967899,3.91800987610551));
#5028=CARTESIAN_POINT('Ctrl Pts',(-1.0233546244042,0.905067969813148,3.92041577486997));
#5029=CARTESIAN_POINT('Ctrl Pts',(-1.0372349984114,0.889126642916958,3.92192215404341));
#5030=CARTESIAN_POINT('Ctrl Pts',(-1.0855819584618,0.830927800972093,3.92736687910065));
#5031=CARTESIAN_POINT('Ctrl Pts',(-1.11784827311584,0.786977040024542,3.93138133830545));
#5032=CARTESIAN_POINT('Ctrl Pts',(-1.14737996054503,0.741265961811063,3.93545337707765));
#5033=CARTESIAN_POINT('Origin',(0.,0.,-1.10921167016993));
#5034=CARTESIAN_POINT('',(-1.14737959883991,0.741266521681617,4.6555522104354));
#5035=CARTESIAN_POINT('',(-1.1473796037955,0.741266514011044,4.53716884124631));
#5036=CARTESIAN_POINT('',(-1.14737960344596,0.741266514552077,-1.10921167016993));
#5037=CARTESIAN_POINT('',(-1.36599977587709,-0.000782498403878971,4.11011263784981));
#5038=CARTESIAN_POINT('Ctrl Pts',(-1.14737959883991,0.741266521681617,4.6555522104354));
#5039=CARTESIAN_POINT('Ctrl Pts',(-1.13681643246464,0.757616864296101,4.65414490266099));
#5040=CARTESIAN_POINT('Ctrl Pts',(-1.1259043798636,0.773740481038852,4.6527258208392));
#5041=CARTESIAN_POINT('Ctrl Pts',(-1.08172649896303,0.83610277291328,4.6471130366888));
#5042=CARTESIAN_POINT('Ctrl Pts',(-1.04593062863914,0.880470380959298,4.64284200642283));
#5043=CARTESIAN_POINT('Ctrl Pts',(-0.951056440806476,0.98408693736181,4.63222931054489));
#5044=CARTESIAN_POINT('Ctrl Pts',(-0.889101729298465,1.04040165390782,4.6258675472562));
#5045=CARTESIAN_POINT('Ctrl Pts',(-0.811250672179,1.09910091524944,4.61877142843508));
#5046=CARTESIAN_POINT('Ctrl Pts',(-0.799987245637843,1.10732602239255,4.61776500923298));
#5047=CARTESIAN_POINT('Ctrl Pts',(-0.78227681786195,1.11984772900455,4.61621603862062));
#5048=CARTESIAN_POINT('Ctrl Pts',(-0.775916248168164,1.12426417679661,4.6156663068812));
#5049=CARTESIAN_POINT('Ctrl Pts',(-0.763889898073782,1.13246396359275,4.61463967784272));
#5050=CARTESIAN_POINT('Ctrl Pts',(-0.758233111151425,1.13625919425788,4.61416208127374));
#5051=CARTESIAN_POINT('Ctrl Pts',(-0.744432702333554,1.14536915625704,4.61300926228246));
#5052=CARTESIAN_POINT('Ctrl Pts',(-0.736260312412042,1.15063952594443,4.61233684099016));
#5053=CARTESIAN_POINT('Ctrl Pts',(-0.705759840928751,1.16985123280071,4.60986229597919));
#5054=CARTESIAN_POINT('Ctrl Pts',(-0.683085057620925,1.18323449780022,4.60809138498994));
#5055=CARTESIAN_POINT('Ctrl Pts',(-0.620180296323417,1.21795102444348,4.60332312854167));
#5056=CARTESIAN_POINT('Ctrl Pts',(-0.579247259535045,1.23794242849322,4.60037567311025));
#5057=CARTESIAN_POINT('Ctrl Pts',(-0.443810095535263,1.29589709102148,4.59088609784645));
#5058=CARTESIAN_POINT('Ctrl Pts',(-0.346057739725599,1.32535220373791,4.58440798163169));
#5059=CARTESIAN_POINT('Ctrl Pts',(-0.225042257599612,1.3475027011048,4.57614248565504));
#5060=CARTESIAN_POINT('Ctrl Pts',(-0.204054451250564,1.35084020051338,4.574701642616));
#5061=CARTESIAN_POINT('Ctrl Pts',(-0.170133159265685,1.35542585307797,4.57235639167771));
#5062=CARTESIAN_POINT('Ctrl Pts',(-0.157244331800852,1.3569814793507,4.57146148718378));
#5063=CARTESIAN_POINT('Ctrl Pts',(-0.132359519535727,1.35962568561049,4.56972537298692));
#5064=CARTESIAN_POINT('Ctrl Pts',(-0.120367421591689,1.3607397675028,4.56888503404971));
#5065=CARTESIAN_POINT('Ctrl Pts',(-0.0921632903585972,1.36298422728454,
4.56689921662262));
#5066=CARTESIAN_POINT('Ctrl Pts',(-0.0759430267644908,1.36398412460856,
4.56574985641495));
#5067=CARTESIAN_POINT('Ctrl Pts',(-0.0194266633236217,1.36645688151918,
4.56171784915685));
#5068=CARTESIAN_POINT('Ctrl Pts',(0.0209103912782695,1.36643477079933,4.55879111787919));
#5069=CARTESIAN_POINT('Ctrl Pts',(0.128114878321844,1.36162818728456,4.55088143233744));
#5070=CARTESIAN_POINT('Ctrl Pts',(0.194728674362897,1.35370749435882,4.54582596883842));
#5071=CARTESIAN_POINT('Ctrl Pts',(0.325920811446947,1.32822244903224,4.53571621447658));
#5072=CARTESIAN_POINT('Ctrl Pts',(0.390342837070776,1.31073766780952,4.53067607025463));
#5073=CARTESIAN_POINT('Ctrl Pts',(0.467436171292611,1.28362223534042,4.52471499749282));
#5074=CARTESIAN_POINT('Ctrl Pts',(0.481554408691499,1.27839274705169,4.52362657289817));
#5075=CARTESIAN_POINT('Ctrl Pts',(0.503018878159732,1.27003608765898,4.52197971303324));
#5076=CARTESIAN_POINT('Ctrl Pts',(0.510428475592943,1.26707633359795,4.52141267539273));
#5077=CARTESIAN_POINT('Ctrl Pts',(0.52343477606493,1.26174837304377,4.52042044274694));
#5078=CARTESIAN_POINT('Ctrl Pts',(0.529042004989777,1.25940759127332,4.51999374761097));
#5079=CARTESIAN_POINT('Ctrl Pts',(0.542776754327717,1.25356599260113,4.51895100167646));
#5080=CARTESIAN_POINT('Ctrl Pts',(0.550886169778131,1.25002349637814,4.51833738146309));
#5081=CARTESIAN_POINT('Ctrl Pts',(0.5775261024892,1.23807656762518,4.51632654325638));
#5082=CARTESIAN_POINT('Ctrl Pts',(0.595904209868544,1.2293365142362,4.51494726991068));
#5083=CARTESIAN_POINT('Ctrl Pts',(0.7304104455655,1.16164388859076,4.50486205028363));
#5084=CARTESIAN_POINT('Ctrl Pts',(0.837779074871426,1.08676111512157,4.49680444163767));
#5085=CARTESIAN_POINT('Ctrl Pts',(0.959489801573599,0.972963350166433,4.48583621152266));
#5086=CARTESIAN_POINT('Ctrl Pts',(0.985047900184815,0.947079005440055,4.48341176641356));
#5087=CARTESIAN_POINT('Ctrl Pts',(1.01933962101197,0.909458239407976,4.47995731823536));
#5088=CARTESIAN_POINT('Ctrl Pts',(1.02896512996194,0.898553441101538,4.47896371240582));
#5089=CARTESIAN_POINT('Ctrl Pts',(1.04626719573852,0.878309196263678,4.47713149029872));
#5090=CARTESIAN_POINT('Ctrl Pts',(1.05399748853746,0.869017472231356,4.47629513664676));
#5091=CARTESIAN_POINT('Ctrl Pts',(1.06954465518556,0.849817321543008,4.47457542698254));
#5092=CARTESIAN_POINT('Ctrl Pts',(1.07734952679881,0.839900724881466,4.47369170978825));
#5093=CARTESIAN_POINT('Ctrl Pts',(1.0968280738694,0.814433684968138,4.47143263039334));
#5094=CARTESIAN_POINT('Ctrl Pts',(1.10830882513432,0.798739963982603,4.47005010274079));
#5095=CARTESIAN_POINT('Ctrl Pts',(1.13264863027497,0.763932928039307,4.4670028050395));
#5096=CARTESIAN_POINT('Ctrl Pts',(1.14536687068168,0.744728851046618,4.46533351654632));
#5097=CARTESIAN_POINT('Ctrl Pts',(1.18328761437629,0.684199376747995,4.46010817097348));
#5098=CARTESIAN_POINT('Ctrl Pts',(1.20678213764331,0.641852379674511,4.4565016010922));
#5099=CARTESIAN_POINT('Ctrl Pts',(1.26999417017976,0.512124274974056,4.44564099771009));
#5100=CARTESIAN_POINT('Ctrl Pts',(1.30281216369449,0.421709056477101,4.43829572754769));
#5101=CARTESIAN_POINT('Ctrl Pts',(1.32942669054545,0.314320016964369,4.43023094353458));
#5102=CARTESIAN_POINT('Ctrl Pts',(1.33273468117738,0.29998452002598,4.42916793594976));
#5103=CARTESIAN_POINT('Ctrl Pts',(1.33746363795136,0.277866025369277,4.42755133915668));
#5104=CARTESIAN_POINT('Ctrl Pts',(1.33904956777796,0.270119924939434,4.42698959938482));
#5105=CARTESIAN_POINT('Ctrl Pts',(1.341868480566,0.255716276301144,4.42595376099447));
#5106=CARTESIAN_POINT('Ctrl Pts',(1.34311930527297,0.249062978836249,4.42547878321777));
#5107=CARTESIAN_POINT('Ctrl Pts',(1.34599134840036,0.233134994403005,4.42434966150155));
#5108=CARTESIAN_POINT('Ctrl Pts',(1.34756623140728,0.223852407307993,4.42369801386201));
#5109=CARTESIAN_POINT('Ctrl Pts',(1.35282233699995,0.1908037341714,4.42139823026359));
#5110=CARTESIAN_POINT('Ctrl Pts',(1.35597202933726,0.166956171167324,4.41977585413383));
#5111=CARTESIAN_POINT('Ctrl Pts',(1.36261666114558,0.103848588476881,4.41555083998215));
#5112=CARTESIAN_POINT('Ctrl Pts',(1.36504545563517,0.0644981095171581,4.41298530146863));
#5113=CARTESIAN_POINT('Ctrl Pts',(1.36765996790229,-0.0777920679294303,
4.4037896401327));
#5114=CARTESIAN_POINT('Ctrl Pts',(1.35791888273026,-0.180555856577663,4.39727444877455));
#5115=CARTESIAN_POINT('Ctrl Pts',(1.33195221857356,-0.30397104968724,4.38885948732663));
#5116=CARTESIAN_POINT('Ctrl Pts',(1.3265933442415,-0.326565628578373,4.38729538207649));
#5117=CARTESIAN_POINT('Ctrl Pts',(1.3169170553905,-0.363180744624295,4.38471535134865));
#5118=CARTESIAN_POINT('Ctrl Pts',(1.31294493195247,-0.37728816786237,4.38371016219692));
#5119=CARTESIAN_POINT('Ctrl Pts',(1.3053452573232,-0.40270428043604,4.3818775052349));
#5120=CARTESIAN_POINT('Ctrl Pts',(1.3017957078565,-0.414034899214241,4.38105259665002));
#5121=CARTESIAN_POINT('Ctrl Pts',(1.29377502551484,-0.438514587195286,4.37925244511929));
#5122=CARTESIAN_POINT('Ctrl Pts',(1.28925019547755,-0.451644515137716,4.37827554829125));
#5123=CARTESIAN_POINT('Ctrl Pts',(1.27574494493506,-0.488975576304179,4.37546423455226));
#5124=CARTESIAN_POINT('Ctrl Pts',(1.26627810241333,-0.512993067533084,4.37361435210378));
#5125=CARTESIAN_POINT('Ctrl Pts',(1.23606819680581,-0.583695328186959,4.3680413947036));
#5126=CARTESIAN_POINT('Ctrl Pts',(1.21338284804615,-0.62949653486628,4.36426009006419));
#5127=CARTESIAN_POINT('Ctrl Pts',(1.14783121367799,-0.745071361790101,4.35429497627933));
#5128=CARTESIAN_POINT('Ctrl Pts',(1.10116444459002,-0.812455839623985,4.34804675116188));
#5129=CARTESIAN_POINT('Ctrl Pts',(1.02902102992214,-0.898899197982087,4.33966077509498));
#5130=CARTESIAN_POINT('Ctrl Pts',(1.00849684888504,-0.92186683995035,4.3373933838686));
#5131=CARTESIAN_POINT('Ctrl Pts',(0.979925962112418,-0.951741690410964,
4.33441056898041));
#5132=CARTESIAN_POINT('Ctrl Pts',(0.972551431938664,-0.959276220021634,
4.33365529095072));
#5133=CARTESIAN_POINT('Ctrl Pts',(0.960218942040365,-0.97158785501711,4.33241723406193));
#5134=CARTESIAN_POINT('Ctrl Pts',(0.955310882376777,-0.976414104141062,
4.3319308922147));
#5135=CARTESIAN_POINT('Ctrl Pts',(0.945055027142969,-0.986347641615543,
4.33092813061226));
#5136=CARTESIAN_POINT('Ctrl Pts',(0.939701889510002,-0.991448959784946,
4.33041213613678));
#5137=CARTESIAN_POINT('Ctrl Pts',(0.925068266991029,-1.0051691908097,4.32902063739346));
#5138=CARTESIAN_POINT('Ctrl Pts',(0.915708659453455,-1.01370315212288,4.32815108288754));
#5139=CARTESIAN_POINT('Ctrl Pts',(0.894272035590667,-1.03270953492134,4.3262014641812));
#5140=CARTESIAN_POINT('Ctrl Pts',(0.882127040891523,-1.04310276954036,4.32512606377035));
#5141=CARTESIAN_POINT('Ctrl Pts',(0.841344647310729,-1.07678096719485,4.32159919205269));
#5142=CARTESIAN_POINT('Ctrl Pts',(0.811944801192098,-1.09911967552151,4.3191902522613));
#5143=CARTESIAN_POINT('Ctrl Pts',(0.688244605706175,-1.185434359558,4.30942702802883));
#5144=CARTESIAN_POINT('Ctrl Pts',(0.5870344929767,-1.23867846599605,4.30223992629826));
#5145=CARTESIAN_POINT('Ctrl Pts',(0.460069897703798,-1.28637588929564,4.29313469518001));
#5146=CARTESIAN_POINT('Ctrl Pts',(0.439570429978327,-1.29352425204126,4.29166366973095));
#5147=CARTESIAN_POINT('Ctrl Pts',(0.406465475513297,-1.30419046404805,4.28928159701591));
#5148=CARTESIAN_POINT('Ctrl Pts',(0.393964168330396,-1.30802108663231,4.28838062272838));
#5149=CARTESIAN_POINT('Ctrl Pts',(0.369876287948202,-1.31502540285413,4.28664083163194));
#5150=CARTESIAN_POINT('Ctrl Pts',(0.358299013010455,-1.31822686955318,4.28580299253496));
#5151=CARTESIAN_POINT('Ctrl Pts',(0.331178906505499,-1.32534274913988,4.2838357449521));
#5152=CARTESIAN_POINT('Ctrl Pts',(0.315606697845275,-1.32913702991996,4.28270266753585));
#5153=CARTESIAN_POINT('Ctrl Pts',(0.262221462452358,-1.34115368472101,4.27880454595813));
#5154=CARTESIAN_POINT('Ctrl Pts',(0.224130576277147,-1.34804238554939,4.27599931312125));
#5155=CARTESIAN_POINT('Ctrl Pts',(0.124094649932641,-1.36177680421504,4.26856851591045));
#5156=CARTESIAN_POINT('Ctrl Pts',(0.0618856865027673,-1.36601771434405,
4.26388176148126));
#5157=CARTESIAN_POINT('Ctrl Pts',(-0.0748175337652816,-1.3659787068457,
4.25354350693301));
#5158=CARTESIAN_POINT('Ctrl Pts',(-0.149125041604392,-1.35987463167423,
4.24789735128025));
#5159=CARTESIAN_POINT('Ctrl Pts',(-0.236919152496719,-1.34537609042737,
4.24141320960069));
#5160=CARTESIAN_POINT('Ctrl Pts',(-0.251230151135062,-1.34277733201691,
4.24036256969299));
#5161=CARTESIAN_POINT('Ctrl Pts',(-0.273218541546837,-1.33842055483616,
4.23876072398793));
#5162=CARTESIAN_POINT('Ctrl Pts',(-0.28092634628775,-1.33682397825462,4.23820158388203));
#5163=CARTESIAN_POINT('Ctrl Pts',(-0.295245046626378,-1.33372872146579,
4.23716782325992));
#5164=CARTESIAN_POINT('Ctrl Pts',(-0.301858932691299,-1.33224739714465,
4.23669236209439));
#5165=CARTESIAN_POINT('Ctrl Pts',(-0.317694402964717,-1.32857671387481,
4.23555848812507));
#5166=CARTESIAN_POINT('Ctrl Pts',(-0.326904673722462,-1.32634051644428,
4.2349026332455));
#5167=CARTESIAN_POINT('Ctrl Pts',(-0.359831502033754,-1.31798224798194,
4.2325685325624));
#5168=CARTESIAN_POINT('Ctrl Pts',(-0.38340713535126,-1.3113180620359,4.23091707357985));
#5169=CARTESIAN_POINT('Ctrl Pts',(-0.445503517139512,-1.29194697747711,
4.22658895415234));
#5170=CARTESIAN_POINT('Ctrl Pts',(-0.483660300729215,-1.27815238628299,
4.22395166915638));
#5171=CARTESIAN_POINT('Ctrl Pts',(-0.620688760291736,-1.22159627851947,
4.21437971757785));
#5172=CARTESIAN_POINT('Ctrl Pts',(-0.71501261877081,-1.16889141522903,4.20755944987793));
#5173=CARTESIAN_POINT('Ctrl Pts',(-0.820011769853555,-1.09271347013798,
4.19885552123938));
#5174=CARTESIAN_POINT('Ctrl Pts',(-0.837539286400239,-1.07933770648205,
4.19736224866106));
#5175=CARTESIAN_POINT('Ctrl Pts',(-0.864986868265193,-1.05732041342426,
4.19495302376748));
#5176=CARTESIAN_POINT('Ctrl Pts',(-0.875119499246772,-1.04894927444347,
4.19404757277319));
#5177=CARTESIAN_POINT('Ctrl Pts',(-0.894262513316769,-1.03266371052275,
4.19230486194445));
#5178=CARTESIAN_POINT('Ctrl Pts',(-0.903292589406051,-1.02477425005016,
4.19146865663819));
#5179=CARTESIAN_POINT('Ctrl Pts',(-0.924033494738829,-1.00616604222044,
4.18951402617379));
#5180=CARTESIAN_POINT('Ctrl Pts',(-0.935663444940012,-0.995360178040924,
4.18839207664489));
#5181=CARTESIAN_POINT('Ctrl Pts',(-0.974213788749859,-0.958268755222606,
4.18458256971323));
#5182=CARTESIAN_POINT('Ctrl Pts',(-1.00023379076665,-0.931076475877344,
4.18185729477677));
#5183=CARTESIAN_POINT('Ctrl Pts',(-1.06433567242301,-0.858294939275736,
4.17472770586481));
#5184=CARTESIAN_POINT('Ctrl Pts',(-1.10062520476704,-0.8112358428113,4.17026870815185));
#5185=CARTESIAN_POINT('Ctrl Pts',(-1.17802757691521,-0.696068789739845,
4.15978016187041));
#5186=CARTESIAN_POINT('Ctrl Pts',(-1.21649205425785,-0.626426182775873,
4.15374414733136));
#5187=CARTESIAN_POINT('Ctrl Pts',(-1.25444773757453,-0.540849841815934,
4.14692715153952));
#5188=CARTESIAN_POINT('Ctrl Pts',(-1.26000302676748,-0.527778448052726,
4.1459018126505));
#5189=CARTESIAN_POINT('Ctrl Pts',(-1.26829155491539,-0.50739860312754,4.14433019460683));
#5190=CARTESIAN_POINT('Ctrl Pts',(-1.27116757610949,-0.500149789361644,
4.14377641621747));
#5191=CARTESIAN_POINT('Ctrl Pts',(-1.27643366120105,-0.486538074328516,
4.1427467984679));
#5192=CARTESIAN_POINT('Ctrl Pts',(-1.27883844365662,-0.480181659896265,
4.14227019862244));
#5193=CARTESIAN_POINT('Ctrl Pts',(-1.28453041719027,-0.464790308060041,
4.14112588309805));
#5194=CARTESIAN_POINT('Ctrl Pts',(-1.28776983832396,-0.455738170571644,
4.14046085980594));
#5195=CARTESIAN_POINT('Ctrl Pts',(-1.29924798291507,-0.422564058269026,
4.13805012019792));
#5196=CARTESIAN_POINT('Ctrl Pts',(-1.30690721005451,-0.398245456948158,
4.13633356127149));
#5197=CARTESIAN_POINT('Ctrl Pts',(-1.34838760953678,-0.252415373972079,
4.12625992727964));
#5198=CARTESIAN_POINT('Ctrl Pts',(-1.3659275236544,-0.126912493698488,4.11843313937027));
#5199=CARTESIAN_POINT('Ctrl Pts',(-1.36599977587709,-0.000782498403878971,
4.11011263784981));
#5200=CARTESIAN_POINT('Ctrl Pts',(-1.36599977678399,-0.000780913632299608,
4.1101125333061));
#5201=CARTESIAN_POINT('Ctrl Pts',(-1.36601137218235,0.0195021380629541,
4.10877450718365));
#5202=CARTESIAN_POINT('Ctrl Pts',(-1.36557120786974,0.0397823578990402,
4.10742655868002));
#5203=CARTESIAN_POINT('Ctrl Pts',(-1.36397231189203,0.0761215963178287,
4.10498718936274));
#5204=CARTESIAN_POINT('Ctrl Pts',(-1.36298093129678,0.0921841185697551,
4.10390051557796));
#5205=CARTESIAN_POINT('Ctrl Pts',(-1.36075157624018,0.120234292919318,4.10198572787291));
#5206=CARTESIAN_POINT('Ctrl Pts',(-1.35963829236043,0.132230238279988,4.10116136067351));
#5207=CARTESIAN_POINT('Ctrl Pts',(-1.35718028794476,0.155383145088946,4.09955876113539));
#5208=CARTESIAN_POINT('Ctrl Pts',(-1.35585626841899,0.166541352542645,4.09878121928405));
#5209=CARTESIAN_POINT('Ctrl Pts',(-1.35276476363943,0.190106629894382,4.09712745553751));
#5210=CARTESIAN_POINT('Ctrl Pts',(-1.35096389741556,0.202508187176493,4.09625027262785));
#5211=CARTESIAN_POINT('Ctrl Pts',(-1.34600440558525,0.233642910845264,4.09402991284754));
#5212=CARTESIAN_POINT('Ctrl Pts',(-1.34262522273736,0.252337703479607,4.09268006163803));
#5213=CARTESIAN_POINT('Ctrl Pts',(-1.32449797592249,0.341908983755579,4.08612884092479));
#5214=CARTESIAN_POINT('Ctrl Pts',(-1.30452318297912,0.411598060741742,4.08076902519247));
#5215=CARTESIAN_POINT('Ctrl Pts',(-1.24858407822589,0.560863874792138,4.06877243336367));
#5216=CARTESIAN_POINT('Ctrl Pts',(-1.21032339876078,0.639256304739435,4.06212012760547));
#5217=CARTESIAN_POINT('Ctrl Pts',(-1.15914692479946,0.722809922827223,4.05490893509864));
#5218=CARTESIAN_POINT('Ctrl Pts',(-1.1533186175403,0.732073729638883,4.05410786115583));
#5219=CARTESIAN_POINT('Ctrl Pts',(-1.14737960320835,0.741266514919876,4.0533120739516));
#5220=CARTESIAN_POINT('Ctrl Pts',(-1.14737996054503,0.741265961811063,3.93545337707765));
#5221=CARTESIAN_POINT('Ctrl Pts',(-1.17686458301595,0.695627733819701,3.9395189261992));
#5222=CARTESIAN_POINT('Ctrl Pts',(-1.20362337238171,0.64823483442225,3.94364170049026));
#5223=CARTESIAN_POINT('Ctrl Pts',(-1.24542367906319,0.562622997095374,3.95084044159456));
#5224=CARTESIAN_POINT('Ctrl Pts',(-1.26169221740402,0.525126553894161,3.95391492532671));
#5225=CARTESIAN_POINT('Ctrl Pts',(-1.2823143737366,0.471078161299187,3.95819399034062));
#5226=CARTESIAN_POINT('Ctrl Pts',(-1.28807583568596,0.455088435384634,3.95944149461941));
#5227=CARTESIAN_POINT('Ctrl Pts',(-1.2978007737332,0.426433018885614,3.96163992568542));
#5228=CARTESIAN_POINT('Ctrl Pts',(-1.30188086972375,0.413809379061976,3.96259574175867));
#5229=CARTESIAN_POINT('Ctrl Pts',(-1.30798474047843,0.393939668809511,3.96407838463171));
#5230=CARTESIAN_POINT('Ctrl Pts',(-1.31013355021347,0.386733282114039,3.96461165791519));
#5231=CARTESIAN_POINT('Ctrl Pts',(-1.3141163828407,0.372961910005135,3.96562179630003));
#5232=CARTESIAN_POINT('Ctrl Pts',(-1.31596093938591,0.366400412343076,3.96609919001826));
#5233=CARTESIAN_POINT('Ctrl Pts',(-1.32000247667041,0.351599446310775,3.96716781213017));
#5234=CARTESIAN_POINT('Ctrl Pts',(-1.32217160980735,0.343352519509725,3.96775752826322));
#5235=CARTESIAN_POINT('Ctrl Pts',(-1.32977416240038,0.313307110930736,3.96988712136449));
#5236=CARTESIAN_POINT('Ctrl Pts',(-1.3347471792539,0.29139453280524,3.97140432418455));
#5237=CARTESIAN_POINT('Ctrl Pts',(-1.3569392860437,0.181065183732163,3.97890981395983));
#5238=CARTESIAN_POINT('Ctrl Pts',(-1.36592523621316,0.091214549048413,3.98460781304651));
#5239=CARTESIAN_POINT('Ctrl Pts',(-1.3660542545431,-0.065220445816803,3.99470471777367));
#5240=CARTESIAN_POINT('Ctrl Pts',(-1.3612753222363,-0.131475850328248,3.99903426838739));
#5241=CARTESIAN_POINT('Ctrl Pts',(-1.34897092127529,-0.215851565304085,
4.00478679124949));
#5242=CARTESIAN_POINT('Ctrl Pts',(-1.34584982351778,-0.234526414197535,
4.00607482564002));
#5243=CARTESIAN_POINT('Ctrl Pts',(-1.34002235318472,-0.265429381020699,
4.00823424120534));
#5244=CARTESIAN_POINT('Ctrl Pts',(-1.33753407816726,-0.277696300204813,
4.00909880321475));
#5245=CARTESIAN_POINT('Ctrl Pts',(-1.33226797087516,-0.301942438501289,
4.01082320542476));
#5246=CARTESIAN_POINT('Ctrl Pts',(-1.32949625024192,-0.313921782533165,
4.01168277983731));
#5247=CARTESIAN_POINT('Ctrl Pts',(-1.32232457328612,-0.343117242041366,
4.01379711485718));
#5248=CARTESIAN_POINT('Ctrl Pts',(-1.31774978069312,-0.360287637378731,
4.01505725815142));
#5249=CARTESIAN_POINT('Ctrl Pts',(-1.29791964289822,-0.429276419625299,
4.02019057785221));
#5250=CARTESIAN_POINT('Ctrl Pts',(-1.27993361653671,-0.480252292864776,
4.02414773228192));
#5251=CARTESIAN_POINT('Ctrl Pts',(-1.23756794631427,-0.580884491175013,
4.03228539256636));
#5252=CARTESIAN_POINT('Ctrl Pts',(-1.21309480138948,-0.630397992141128,
4.03646159574186));
#5253=CARTESIAN_POINT('Ctrl Pts',(-1.1552666155397,-0.731485057930364,4.04526909171857));
#5254=CARTESIAN_POINT('Ctrl Pts',(-1.1212896358817,-0.782574099851696,4.04989031637467));
#5255=CARTESIAN_POINT('Ctrl Pts',(-1.07488559205689,-0.843090151186601,
4.05545196101681));
#5256=CARTESIAN_POINT('Ctrl Pts',(-1.06558249923752,-0.854818122514659,
4.05653402714784));
#5257=CARTESIAN_POINT('Ctrl Pts',(-1.05103987542027,-0.872544858113575,
4.05817323170261));
#5258=CARTESIAN_POINT('Ctrl Pts',(-1.04593786048779,-0.878654283098264,
4.05873885955268));
#5259=CARTESIAN_POINT('Ctrl Pts',(-1.03684651036115,-0.889349339133849,
4.05972973798537));
#5260=CARTESIAN_POINT('Ctrl Pts',(-1.03287971049476,-0.89395326443013,4.06015647029394));
#5261=CARTESIAN_POINT('Ctrl Pts',(-1.02304723997169,-0.905212146332767,
4.06120072149934));
#5262=CARTESIAN_POINT('Ctrl Pts',(-1.01714726453985,-0.911836683896,4.06181578847821));
#5263=CARTESIAN_POINT('Ctrl Pts',(-0.997408810723819,-0.933569166832068,
4.06383760562203));
#5264=CARTESIAN_POINT('Ctrl Pts',(-0.983294311541937,-0.948424024411138,
4.06522613717319));
#5265=CARTESIAN_POINT('Ctrl Pts',(-0.876599880226736,-1.05577144002512,
4.07536060128387));
#5266=CARTESIAN_POINT('Ctrl Pts',(-0.771485137672042,-1.13485635751599,
4.08345468157651));
#5267=CARTESIAN_POINT('Ctrl Pts',(-0.625335788538119,-1.21498628435347,
4.0944328321397));
#5268=CARTESIAN_POINT('Ctrl Pts',(-0.593296576566292,-1.23094896508899,
4.09681983849976));
#5269=CARTESIAN_POINT('Ctrl Pts',(-0.547487453505306,-1.2515680023658,4.10022969785596));
#5270=CARTESIAN_POINT('Ctrl Pts',(-0.534212316889764,-1.25729159316498,
4.1012174292611));
#5271=CARTESIAN_POINT('Ctrl Pts',(-0.509697032176887,-1.26740303990136,
4.1030422279827));
#5272=CARTESIAN_POINT('Ctrl Pts',(-0.498484684929161,-1.27185476093218,
4.10387709988814));
#5273=CARTESIAN_POINT('Ctrl Pts',(-0.47539943033689,-1.28066831865745,4.10559738510303));
#5274=CARTESIAN_POINT('Ctrl Pts',(-0.463521992871846,-1.28501490415164,
4.10648320225115));
#5275=CARTESIAN_POINT('Ctrl Pts',(-0.433090702643553,-1.29567453579113,
4.10875546596742));
#5276=CARTESIAN_POINT('Ctrl Pts',(-0.414458766812318,-1.30175417014612,
4.1101492517404));
#5277=CARTESIAN_POINT('Ctrl Pts',(-0.311181635169446,-1.33301173992622,
4.11789320099946));
#5278=CARTESIAN_POINT('Ctrl Pts',(-0.224392813245597,-1.35033224301864,
4.12448728392731));
#5279=CARTESIAN_POINT('Ctrl Pts',(-0.0572901278553481,-1.36712115043768,
4.13718131252452));
#5280=CARTESIAN_POINT('Ctrl Pts',(0.0225256901831294,-1.36813630502074,
4.14323785004908));
#5281=CARTESIAN_POINT('Ctrl Pts',(0.116110979418365,-1.3611300623866,4.15007125961564));
#5282=CARTESIAN_POINT('Ctrl Pts',(0.130225441746699,-1.35985226416382,4.151094328248));
#5283=CARTESIAN_POINT('Ctrl Pts',(0.152064817222435,-1.35753194428155,4.15266314069585));
#5284=CARTESIAN_POINT('Ctrl Pts',(0.159804554870582,-1.35664262067354,4.15321634615987));
#5285=CARTESIAN_POINT('Ctrl Pts',(0.17428101997003,-1.35485361177475,4.15424535576591));
#5286=CARTESIAN_POINT('Ctrl Pts',(0.181018969914569,-1.35396983645719,4.15472191378779));
#5287=CARTESIAN_POINT('Ctrl Pts',(0.197280538402448,-1.35171334249654,4.15586671028654));
#5288=CARTESIAN_POINT('Ctrl Pts',(0.206796723594013,-1.35029022795657,4.1565322476128));
#5289=CARTESIAN_POINT('Ctrl Pts',(0.241533176060523,-1.34471965338847,4.15894817127509));
#5290=CARTESIAN_POINT('Ctrl Pts',(0.266652311106611,-1.33996491109726,4.16066923086076));
#5291=CARTESIAN_POINT('Ctrl Pts',(0.334021930735694,-1.32524287723734,4.16525061338459));
#5292=CARTESIAN_POINT('Ctrl Pts',(0.375956134820818,-1.31396225799737,4.16806566275548));
#5293=CARTESIAN_POINT('Ctrl Pts',(0.518228708108931,-1.26831915516917,4.17769908236273));
#5294=CARTESIAN_POINT('Ctrl Pts',(0.615049771833946,-1.22429817111525,4.18443135808958));
#5295=CARTESIAN_POINT('Ctrl Pts',(0.723515021132719,-1.15883989587187,4.19295098079844));
#5296=CARTESIAN_POINT('Ctrl Pts',(0.740979438059369,-1.14775140494888,4.19435465476035));
#5297=CARTESIAN_POINT('Ctrl Pts',(0.768886699671401,-1.12913009517841,4.19665443727495));
#5298=CARTESIAN_POINT('Ctrl Pts',(0.779487027569744,-1.12183843900621,4.19754172383603));
#5299=CARTESIAN_POINT('Ctrl Pts',(0.799842332619613,-1.10740882835426,4.1992733911417));
#5300=CARTESIAN_POINT('Ctrl Pts',(0.809608702437597,-1.10028896321933,4.20011703656367));
#5301=CARTESIAN_POINT('Ctrl Pts',(0.832518821891377,-1.08311688377658,4.20212744739932));
#5302=CARTESIAN_POINT('Ctrl Pts',(0.845576659062321,-1.07295379384322,4.20329838114384));
#5303=CARTESIAN_POINT('Ctrl Pts',(0.89159447047512,-1.03577570720895,4.20751782670116));
#5304=CARTESIAN_POINT('Ctrl Pts',(0.923467989486754,-1.0074612709108,4.21061621933805));
#5305=CARTESIAN_POINT('Ctrl Pts',(1.00364148205996,-0.929234718765019,4.21889002510683));
#5306=CARTESIAN_POINT('Ctrl Pts',(1.04954908381356,-0.8770510708807,4.22413894089452));
#5307=CARTESIAN_POINT('Ctrl Pts',(1.12818525910111,-0.772604040496414,4.23402649902302));
#5308=CARTESIAN_POINT('Ctrl Pts',(1.16174177587119,-0.721163197076716,4.23865258277058));
#5309=CARTESIAN_POINT('Ctrl Pts',(1.19904670025467,-0.654574055545382,4.24421917564556));
#5310=CARTESIAN_POINT('Ctrl Pts',(1.20614980368215,-0.641391363306888,4.24530159923716));
#5311=CARTESIAN_POINT('Ctrl Pts',(1.21669522150949,-0.621025042319853,4.24694122914452));
#5312=CARTESIAN_POINT('Ctrl Pts',(1.22029363380583,-0.613924116314866,4.24750693127685));
#5313=CARTESIAN_POINT('Ctrl Pts',(1.22652938879071,-0.601347311882647,4.24849787318347));
#5314=CARTESIAN_POINT('Ctrl Pts',(1.22919245614337,-0.59588492102953,4.2489245957329));
#5315=CARTESIAN_POINT('Ctrl Pts',(1.23565244683517,-0.582406807658691,4.2499687368707));
#5316=CARTESIAN_POINT('Ctrl Pts',(1.23940789998477,-0.574371593312753,4.25058370492795));
#5317=CARTESIAN_POINT('Ctrl Pts',(1.25157455093782,-0.547664586248167,4.2526048117014));
#5318=CARTESIAN_POINT('Ctrl Pts',(1.25964457183646,-0.528839310491383,4.25399274934889));
#5319=CARTESIAN_POINT('Ctrl Pts',(1.31611456944933,-0.388473703458829,4.26412387237895));
#5320=CARTESIAN_POINT('Ctrl Pts',(1.34725804255815,-0.260715801187346,4.27221545571499));
#5321=CARTESIAN_POINT('Ctrl Pts',(1.36317677128747,-0.094807217177443,4.28319289038459));
#5322=CARTESIAN_POINT('Ctrl Pts',(1.36519394558755,-0.0590294077737234,
4.28558242098447));
#5323=CARTESIAN_POINT('Ctrl Pts',(1.36604848992067,-0.00875608421296452,
4.28899527744985));
#5324=CARTESIAN_POINT('Ctrl Pts',(1.36606462453103,0.00570621309900732,
4.2899833963028));
#5325=CARTESIAN_POINT('Ctrl Pts',(1.36567303550315,0.0322292269052108,4.29180867283752));
#5326=CARTESIAN_POINT('Ctrl Pts',(1.3653351149267,0.0442896236608912,4.29264363055542));
#5327=CARTESIAN_POINT('Ctrl Pts',(1.36431591388661,0.0689781939574303,4.29436383860246));
#5328=CARTESIAN_POINT('Ctrl Pts',(1.36361893096982,0.0816045110707339,4.29524948977124));
#5329=CARTESIAN_POINT('Ctrl Pts',(1.36139583676563,0.113758488019315,4.29752077615866));
#5330=CARTESIAN_POINT('Ctrl Pts',(1.35962487060949,0.133265744908264,4.29891373796646));
#5331=CARTESIAN_POINT('Ctrl Pts',(1.3476311098609,0.239865880797861,4.30661224723844));
#5332=CARTESIAN_POINT('Ctrl Pts',(1.32946098069089,0.325843267923269,4.31315797790196));
#5333=CARTESIAN_POINT('Ctrl Pts',(1.27907901323818,0.48618851179931,4.32586062198181));
#5334=CARTESIAN_POINT('Ctrl Pts',(1.24824531601337,0.560631785938357,4.33197600490831));
#5335=CARTESIAN_POINT('Ctrl Pts',(1.20451205171405,0.644442211880982,4.3388585840369));
#5336=CARTESIAN_POINT('Ctrl Pts',(1.19779155385011,0.656848901940175,4.33987705308452));
#5337=CARTESIAN_POINT('Ctrl Pts',(1.18707010329398,0.675929767431114,4.3414403620864));
#5338=CARTESIAN_POINT('Ctrl Pts',(1.18320254032671,0.682677256663986,4.34199258581071));
#5339=CARTESIAN_POINT('Ctrl Pts',(1.17584584913866,0.695261657938206,4.34302086189557));
#5340=CARTESIAN_POINT('Ctrl Pts',(1.17237060851043,0.701105835417373,4.34349765333229));
#5341=CARTESIAN_POINT('Ctrl Pts',(1.16385885780103,0.715179443591657,4.34464447462523));
#5342=CARTESIAN_POINT('Ctrl Pts',(1.15877855705498,0.723381881663049,4.34531177740591));
#5343=CARTESIAN_POINT('Ctrl Pts',(1.13981904443955,0.753280738179314,4.34774280108668));
#5344=CARTESIAN_POINT('Ctrl Pts',(1.12541304933812,0.774638621350271,4.34947671407069));
#5345=CARTESIAN_POINT('Ctrl Pts',(1.08482019028821,0.831295226687552,4.35410585305907));
#5346=CARTESIAN_POINT('Ctrl Pts',(1.05751955571855,0.865759491866431,4.35695464627477));
#5347=CARTESIAN_POINT('Ctrl Pts',(0.959568696447125,0.977850070039799,4.36654980763222));
#5348=CARTESIAN_POINT('Ctrl Pts',(0.881670374969121,1.04862669573488,4.37321611636102));
#5349=CARTESIAN_POINT('Ctrl Pts',(0.779514351489243,1.1219392004832,4.38166987475214));
#5350=CARTESIAN_POINT('Ctrl Pts',(0.762310351224321,1.13369883378771,4.38308355304672));
#5351=CARTESIAN_POINT('Ctrl Pts',(0.734034310397959,1.15209198822856,4.38539552463061));
#5352=CARTESIAN_POINT('Ctrl Pts',(0.723125057876148,1.15897042642793,4.38628481393576));
#5353=CARTESIAN_POINT('Ctrl Pts',(0.701817996184934,1.17198688120895,4.38801749737081));
#5354=CARTESIAN_POINT('Ctrl Pts',(0.691432946879422,1.17814354515878,4.38886011888069));
#5355=CARTESIAN_POINT('Ctrl Pts',(0.666698304548748,1.1923675318315,4.39086337199337));
#5356=CARTESIAN_POINT('Ctrl Pts',(0.652282082227506,1.20031454355063,4.39202808963276));
#5357=CARTESIAN_POINT('Ctrl Pts',(0.600633365409873,1.22758091639615,4.39619284684034));
#5358=CARTESIAN_POINT('Ctrl Pts',(0.562661944173404,1.2454421852721,4.39924103792595));
#5359=CARTESIAN_POINT('Ctrl Pts',(0.457335927424326,1.28918576809465,4.40765998120004));
#5360=CARTESIAN_POINT('Ctrl Pts',(0.388658927051677,1.31152530517119,4.41311669140555));
#5361=CARTESIAN_POINT('Ctrl Pts',(0.260491452627298,1.34226095313113,4.42308277970975));
#5362=CARTESIAN_POINT('Ctrl Pts',(0.201580359965802,1.35236344734108,4.4275809784457));
#5363=CARTESIAN_POINT('Ctrl Pts',(0.127407832465253,1.36012654905985,4.43301887215503));
#5364=CARTESIAN_POINT('Ctrl Pts',(0.112597970738322,1.36143260118678,4.43409335975041));
#5365=CARTESIAN_POINT('Ctrl Pts',(0.089851605907968,1.36306481755312,4.43572354309389));
#5366=CARTESIAN_POINT('Ctrl Pts',(0.0819291543940543,1.36356394408213,4.4362875932505));
#5367=CARTESIAN_POINT('Ctrl Pts',(0.0679306487509348,1.36432342335475,4.43727713033702));
#5368=CARTESIAN_POINT('Ctrl Pts',(0.0618568013477766,1.36461229471382,4.43770407668093));
#5369=CARTESIAN_POINT('Ctrl Pts',(0.0468862263853533,1.3652241311892,4.43875069555247));
#5370=CARTESIAN_POINT('Ctrl Pts',(0.037987948687809,1.3655007042268,4.43936788638673));
#5371=CARTESIAN_POINT('Ctrl Pts',(0.00841043820728597,1.36613066398238,
4.44140500672592));
#5372=CARTESIAN_POINT('Ctrl Pts',(-0.0122751152794063,1.36610144539997,
4.44280633752552));
#5373=CARTESIAN_POINT('Ctrl Pts',(-0.149420423080392,1.36279199421416,4.45198922257088));
#5374=CARTESIAN_POINT('Ctrl Pts',(-0.265059500413666,1.34509395819356,4.45925235748743));
#5375=CARTESIAN_POINT('Ctrl Pts',(-0.421788411532173,1.30008320556919,4.46989309372466));
#5376=CARTESIAN_POINT('Ctrl Pts',(-0.465828815595272,1.28496095307328,4.47297151842012));
#5377=CARTESIAN_POINT('Ctrl Pts',(-0.525149531164257,1.26114095259945,4.47729747267074));
#5378=CARTESIAN_POINT('Ctrl Pts',(-0.541164425535938,1.25435224364979,4.47848379093162));
#5379=CARTESIAN_POINT('Ctrl Pts',(-0.568098959237523,1.24232288146415,4.48051299900679));
#5380=CARTESIAN_POINT('Ctrl Pts',(-0.579086729531297,1.23723931099467,4.48135059150779));
#5381=CARTESIAN_POINT('Ctrl Pts',(-0.601351810287833,1.22657664785702,4.48306872622031));
#5382=CARTESIAN_POINT('Ctrl Pts',(-0.612622482326328,1.22098646521938,4.48394958083021));
#5383=CARTESIAN_POINT('Ctrl Pts',(-0.640947999549338,1.20644626604826,4.48619255147265));
#5384=CARTESIAN_POINT('Ctrl Pts',(-0.657893243334904,1.19729000011331,4.48756163151049));
#5385=CARTESIAN_POINT('Ctrl Pts',(-0.744640290155184,1.14801913340153,4.49471686268128));
#5386=CARTESIAN_POINT('Ctrl Pts',(-0.81097874001437,1.10215545805635,4.50070269730499));
#5387=CARTESIAN_POINT('Ctrl Pts',(-0.941878575716297,0.993411325213874,
4.51354366854659));
#5388=CARTESIAN_POINT('Ctrl Pts',(-1.00506352597523,0.929435721929034,4.52039034639818));
#5389=CARTESIAN_POINT('Ctrl Pts',(-1.06998902575566,0.849270525263961,4.52788787332642));
#5390=CARTESIAN_POINT('Ctrl Pts',(-1.07830052519696,0.838692406213547,4.52885742704271));
#5391=CARTESIAN_POINT('Ctrl Pts',(-1.09103634361399,0.821981038774539,4.53035645456811));
#5392=CARTESIAN_POINT('Ctrl Pts',(-1.09556805955199,0.815931225706072,4.5308925981133));
#5393=CARTESIAN_POINT('Ctrl Pts',(-1.10412681442433,0.804305462522289,4.53191001305469));
#5394=CARTESIAN_POINT('Ctrl Pts',(-1.1081622931715,0.798736272841784,4.53239179163914));
#5395=CARTESIAN_POINT('Ctrl Pts',(-1.11804235823733,0.784882205189369,4.53357704599625));
#5396=CARTESIAN_POINT('Ctrl Pts',(-1.12383723666935,0.77656208502808,4.53427732343826));
#5397=CARTESIAN_POINT('Ctrl Pts',(-1.13559197330244,0.759277761591802,4.53571023136447));
#5398=CARTESIAN_POINT('Ctrl Pts',(-1.14153919825758,0.750306666325287,4.53644209887711));
#5399=CARTESIAN_POINT('Ctrl Pts',(-1.1473796037955,0.741266514011044,4.53716884124631));
#5400=CARTESIAN_POINT('Origin',(0.,0.,-1.10921167016993));
#5401=CARTESIAN_POINT('',(-1.14737960281818,0.741266515523794,5.25438358752252));
#5402=CARTESIAN_POINT('',(-1.14737960694915,0.741266509129621,5.1349525893656));
#5403=CARTESIAN_POINT('',(-1.14737960344596,0.741266514552077,-1.10921167016993));
#5404=CARTESIAN_POINT('Ctrl Pts',(-1.14737960281818,0.741266515523794,5.25438358752252));
#5405=CARTESIAN_POINT('Ctrl Pts',(-1.11669783189643,0.788757717941165,5.25074885766899));
#5406=CARTESIAN_POINT('Ctrl Pts',(-1.08309694827719,0.834298411855299,5.24710992600634));
#5407=CARTESIAN_POINT('Ctrl Pts',(-1.02265084444286,0.906394317234178,5.24091871128984));
#5408=CARTESIAN_POINT('Ctrl Pts',(-0.99735702289175,0.93415415737226,5.2384156416747));
#5409=CARTESIAN_POINT('Ctrl Pts',(-0.959795903514824,0.972110825285475,
5.23478932399632));
#5410=CARTESIAN_POINT('Ctrl Pts',(-0.94844286229019,0.983190589251895,5.23370425550666));
#5411=CARTESIAN_POINT('Ctrl Pts',(-0.928174891064889,1.00229292962259,5.23178424832833));
#5412=CARTESIAN_POINT('Ctrl Pts',(-0.919342310852199,1.01040063575267,5.23095300820164));
#5413=CARTESIAN_POINT('Ctrl Pts',(-0.900601853912183,1.02715392355282,5.22919991589171));
#5414=CARTESIAN_POINT('Ctrl Pts',(-0.890673617213158,1.03577476709321,5.22827716916442));
#5415=CARTESIAN_POINT('Ctrl Pts',(-0.86374885996307,1.05848057411455,5.22578963248185));
#5416=CARTESIAN_POINT('Ctrl Pts',(-0.846533431717381,1.07229859069501,5.22421455223892));
#5417=CARTESIAN_POINT('Ctrl Pts',(-0.754408727016371,1.14264133572799,5.21586040770549));
#5418=CARTESIAN_POINT('Ctrl Pts',(-0.674167904635609,1.19174401540275,5.20881082342942));
#5419=CARTESIAN_POINT('Ctrl Pts',(-0.54447193355747,1.2537954204792,5.19793470667421));
#5420=CARTESIAN_POINT('Ctrl Pts',(-0.498247251526451,1.2728718637263,5.19415498689192));
#5421=CARTESIAN_POINT('Ctrl Pts',(-0.424809979657135,1.29856344533606,5.18837950056974));
#5422=CARTESIAN_POINT('Ctrl Pts',(-0.398263698719601,1.30694943024731,5.18633693708558));
#5423=CARTESIAN_POINT('Ctrl Pts',(-0.36193699230684,1.3172152097009,5.18361816673078));
#5424=CARTESIAN_POINT('Ctrl Pts',(-0.352366818568368,1.31980753712752,5.18290900356349));
#5425=CARTESIAN_POINT('Ctrl Pts',(-0.336146530968231,1.32401220260077,5.18171995093608));
#5426=CARTESIAN_POINT('Ctrl Pts',(-0.329511120636676,1.3256791591172,5.18123717041773));
#5427=CARTESIAN_POINT('Ctrl Pts',(-0.31542480450765,1.32910563703486,5.1802202561575));
#5428=CARTESIAN_POINT('Ctrl Pts',(-0.307971222037272,1.33085248442282,5.17968680206453));
#5429=CARTESIAN_POINT('Ctrl Pts',(-0.286933129785029,1.33559682856605,5.17819310633613));
#5430=CARTESIAN_POINT('Ctrl Pts',(-0.273316526152427,1.33844970895514,5.17724037381275));
#5431=CARTESIAN_POINT('Ctrl Pts',(-0.17554377492028,1.35738013418546,5.17048403636267));
#5432=CARTESIAN_POINT('Ctrl Pts',(-0.0900723148303787,1.36571860927694,
5.16501680550525));
#5433=CARTESIAN_POINT('Ctrl Pts',(0.069163873994095,1.36622844976993,5.15477838860184));
#5434=CARTESIAN_POINT('Ctrl Pts',(0.142593207758472,1.36052545096765,5.15003503863421));
#5435=CARTESIAN_POINT('Ctrl Pts',(0.2395785150999,1.3450529493333,5.14347202242919));
#5436=CARTESIAN_POINT('Ctrl Pts',(0.263843082430402,1.34050438500095,5.14180546955407));
#5437=CARTESIAN_POINT('Ctrl Pts',(0.30133136283804,1.33241969382357,5.13918480419137));
#5438=CARTESIAN_POINT('Ctrl Pts',(0.314648352973924,1.32933788844693,5.13824478290718));
#5439=CARTESIAN_POINT('Ctrl Pts',(0.339460530722377,1.3232021625791,5.13647513132173));
#5440=CARTESIAN_POINT('Ctrl Pts',(0.350966504286508,1.32019692173747,5.1356471083111));
#5441=CARTESIAN_POINT('Ctrl Pts',(0.376843871901683,1.31307583315212,5.13376737725238));
#5442=CARTESIAN_POINT('Ctrl Pts',(0.391189676763702,1.30887358163759,5.13271301264756));
#5443=CARTESIAN_POINT('Ctrl Pts',(0.428650545634914,1.29722947562982,5.12992618604247));
#5444=CARTESIAN_POINT('Ctrl Pts',(0.451640268405269,1.28940549841292,5.12818188995137));
#5445=CARTESIAN_POINT('Ctrl Pts',(0.569595189229001,1.24572093637903,5.11905053530432));
#5446=CARTESIAN_POINT('Ctrl Pts',(0.660544269572202,1.19997271917198,5.11135698716463));
#5447=CARTESIAN_POINT('Ctrl Pts',(0.778298644189569,1.12326877177145,5.10074414472386));
#5448=CARTESIAN_POINT('Ctrl Pts',(0.810098190585007,1.10055566948255,5.09780809501436));
#5449=CARTESIAN_POINT('Ctrl Pts',(0.859727018226621,1.06178965125214,5.09315374805009));
#5450=CARTESIAN_POINT('Ctrl Pts',(0.878183508706765,1.04657617963331,5.09140567685146));
#5451=CARTESIAN_POINT('Ctrl Pts',(0.903322637649673,1.02472068530454,5.08901060687207));
#5452=CARTESIAN_POINT('Ctrl Pts',(0.91034945917417,1.0184832573611,5.08833955765412));
#5453=CARTESIAN_POINT('Ctrl Pts',(0.922326078502919,1.00762909955756,5.08719388000376));
#5454=CARTESIAN_POINT('Ctrl Pts',(0.927306808247947,1.00304730129117,5.08671686696526));
#5455=CARTESIAN_POINT('Ctrl Pts',(0.938040679291453,0.993024859825739,5.08568782528002));
#5456=CARTESIAN_POINT('Ctrl Pts',(0.943780849207455,0.987570961905156,5.08513677498503));
#5457=CARTESIAN_POINT('Ctrl Pts',(0.960087580985714,0.971805434362287,5.083568036596));
#5458=CARTESIAN_POINT('Ctrl Pts',(0.97053518545871,0.961371657132912,5.08255890599368));
#5459=CARTESIAN_POINT('Ctrl Pts',(1.02902642882004,0.901032230064081,5.07687107971903));
#5460=CARTESIAN_POINT('Ctrl Pts',(1.07339349274715,0.847692837852891,5.07240343368985));
#5461=CARTESIAN_POINT('Ctrl Pts',(1.15148061778871,0.73779551892846,5.06373193442103));
#5462=CARTESIAN_POINT('Ctrl Pts',(1.18554071803918,0.68172023464191,5.05953731919391));
#5463=CARTESIAN_POINT('Ctrl Pts',(1.23362097080065,0.587980902608663,5.05261974958516));
#5464=CARTESIAN_POINT('Ctrl Pts',(1.25023760129873,0.551767821897127,5.04996934726706));
#5465=CARTESIAN_POINT('Ctrl Pts',(1.2713476964716,0.49989293685736,5.04616900024867));
#5466=CARTESIAN_POINT('Ctrl Pts',(1.27718069328018,0.484796197455747,5.04506270385184));
#5467=CARTESIAN_POINT('Ctrl Pts',(1.28688085847206,0.458299540607737,5.0431184749969));
#5468=CARTESIAN_POINT('Ctrl Pts',(1.2908681876091,0.446945319877366,5.04228454842588));
#5469=CARTESIAN_POINT('Ctrl Pts',(1.29885268887806,0.423210260469156,5.04053887449667));
#5470=CARTESIAN_POINT('Ctrl Pts',(1.30282402071905,0.410822081073346,5.03962639042171));
#5471=CARTESIAN_POINT('Ctrl Pts',(1.31285363267612,0.377926637400979,5.03719888799635));
#5472=CARTESIAN_POINT('Ctrl Pts',(1.31860814543316,0.357331319107249,5.03567444018403));
#5473=CARTESIAN_POINT('Ctrl Pts',(1.34869626424871,0.238995832071343,5.02688412657336));
#5474=CARTESIAN_POINT('Ctrl Pts',(1.36263946930033,0.138951299367281,5.01929849513842));
#5475=CARTESIAN_POINT('Ctrl Pts',(1.36675518080256,-0.00776457640466963,
5.00819742301721));
#5476=CARTESIAN_POINT('Ctrl Pts',(1.36571529958815,-0.0538717618015524,
5.00471805672353));
#5477=CARTESIAN_POINT('Ctrl Pts',(1.36040814836661,-0.12628927289488,4.99933531663233));
#5478=CARTESIAN_POINT('Ctrl Pts',(1.35769983165907,-0.152678404004389,4.99739142079486));
#5479=CARTESIAN_POINT('Ctrl Pts',(1.35294725947983,-0.188639244133493,4.99478030960976));
#5480=CARTESIAN_POINT('Ctrl Pts',(1.35156639814453,-0.198291040926888,4.99408325902257));
#5481=CARTESIAN_POINT('Ctrl Pts',(1.34904481183697,-0.214663803886214,4.99290813410803));
#5482=CARTESIAN_POINT('Ctrl Pts',(1.34795692694276,-0.221392377077281,4.99242732974284));
#5483=CARTESIAN_POINT('Ctrl Pts',(1.34552766632889,-0.235735156702116,4.9914072366854));
#5484=CARTESIAN_POINT('Ctrl Pts',(1.34417195452254,-0.24334652048537,4.99086871596583));
#5485=CARTESIAN_POINT('Ctrl Pts',(1.34020026008352,-0.264598084813544,4.98937196961392));
#5486=CARTESIAN_POINT('Ctrl Pts',(1.33744069062105,-0.278210926816376,4.98842113214607));
#5487=CARTESIAN_POINT('Ctrl Pts',(1.31648023815659,-0.374074864716769,4.98176601808539));
#5488=CARTESIAN_POINT('Ctrl Pts',(1.29091025608191,-0.45454005070677,4.97638568426065));
#5489=CARTESIAN_POINT('Ctrl Pts',(1.23604905374828,-0.584241770072027,4.96733178624128));
#5490=CARTESIAN_POINT('Ctrl Pts',(1.21079924696213,-0.634917569518465,4.96368897250628));
#5491=CARTESIAN_POINT('Ctrl Pts',(1.16418588006783,-0.715515785714465,4.95755586542614));
#5492=CARTESIAN_POINT('Ctrl Pts',(1.1446285852634,-0.746402468095068,4.95511713763425));
#5493=CARTESIAN_POINT('Ctrl Pts',(1.11492404252442,-0.789396857108036,4.95156709996658));
#5494=CARTESIAN_POINT('Ctrl Pts',(1.10576805862804,-0.802172041913922,4.95049170068267));
#5495=CARTESIAN_POINT('Ctrl Pts',(1.08925383514937,-0.824393945663081,4.94858261777873));
#5496=CARTESIAN_POINT('Ctrl Pts',(1.0819878855033,-0.833907365839652,4.94775249372462));
#5497=CARTESIAN_POINT('Ctrl Pts',(1.0664375130531,-0.853722292942234,4.94599546532073));
#5498=CARTESIAN_POINT('Ctrl Pts',(1.05812674440812,-0.864001443136632,4.94506758982232));
#5499=CARTESIAN_POINT('Ctrl Pts',(1.0353212284044,-0.891385768571927,4.94254995384899));
#5500=CARTESIAN_POINT('Ctrl Pts',(1.02055293725177,-0.908256699236898,4.94094946023481));
#5501=CARTESIAN_POINT('Ctrl Pts',(0.94747747958175,-0.987702953366598,4.93316514330796));
#5502=CARTESIAN_POINT('Ctrl Pts',(0.883803230494275,-1.04506373427434,4.92676274275056));
#5503=CARTESIAN_POINT('Ctrl Pts',(0.770698991763751,-1.12918305657435,4.91610489898208));
#5504=CARTESIAN_POINT('Ctrl Pts',(0.724225470639474,-1.15953837608525,4.9118998424951));
#5505=CARTESIAN_POINT('Ctrl Pts',(0.650361951015374,-1.20160648791937,4.90557898287706));
#5506=CARTESIAN_POINT('Ctrl Pts',(0.624220346594478,-1.21539214491306,4.90340722042469));
#5507=CARTESIAN_POINT('Ctrl Pts',(0.588552196915119,-1.23274680290621,4.90054860963409));
#5508=CARTESIAN_POINT('Ctrl Pts',(0.579404980237071,-1.23707245265791,4.89982451194704));
#5509=CARTESIAN_POINT('Ctrl Pts',(0.563962784336865,-1.24416608383566,4.89861814065666));
#5510=CARTESIAN_POINT('Ctrl Pts',(0.557693560498852,-1.24698884018793,4.89813277698527));
#5511=CARTESIAN_POINT('Ctrl Pts',(0.544476842621299,-1.25282012950273,4.89711906719937));
#5512=CARTESIAN_POINT('Ctrl Pts',(0.537525244926527,-1.25581842918948,4.89659129886739));
#5513=CARTESIAN_POINT('Ctrl Pts',(0.518107215059327,-1.26400285117295,4.8951311110009));
#5514=CARTESIAN_POINT('Ctrl Pts',(0.505587906529557,-1.26906232995245,4.89420567221588));
#5515=CARTESIAN_POINT('Ctrl Pts',(0.409738729187023,-1.3061546060285,4.88722624374629));
#5516=CARTESIAN_POINT('Ctrl Pts',(0.323512780494029,-1.33013890951881,4.88154203141087));
#5517=CARTESIAN_POINT('Ctrl Pts',(0.155955162309904,-1.35947194658716,4.87060144125238));
#5518=CARTESIAN_POINT('Ctrl Pts',(0.0752875094278573,-1.36631459279741,
4.86537568127857));
#5519=CARTESIAN_POINT('Ctrl Pts',(-0.0247768183454392,-1.36591122005228,
4.85862918802274));
#5520=CARTESIAN_POINT('Ctrl Pts',(-0.0440425062067384,-1.36542577541528,
4.85731884418325));
#5521=CARTESIAN_POINT('Ctrl Pts',(-0.0758624081861914,-1.36394988271716,
4.85513228539503));
#5522=CARTESIAN_POINT('Ctrl Pts',(-0.0884250689942695,-1.36319308115039,
4.85426325994029));
#5523=CARTESIAN_POINT('Ctrl Pts',(-0.113051290509998,-1.36136770957737,
4.85254753091446));
#5524=CARTESIAN_POINT('Ctrl Pts',(-0.125114661858915,-1.3603120743822,4.85170130233038));
#5525=CARTESIAN_POINT('Ctrl Pts',(-0.154468816105163,-1.35734960824288,
4.84962732632031));
#5526=CARTESIAN_POINT('Ctrl Pts',(-0.171739875620201,-1.35527264406935,
4.84839447613882));
#5527=CARTESIAN_POINT('Ctrl Pts',(-0.235037556964589,-1.34643134166058,
4.84382755474198));
#5528=CARTESIAN_POINT('Ctrl Pts',(-0.280745326525242,-1.33764764079029,
4.84043351978184));
#5529=CARTESIAN_POINT('Ctrl Pts',(-0.439087986855978,-1.29874544433809,
4.82834241439823));
#5530=CARTESIAN_POINT('Ctrl Pts',(-0.548229108377538,-1.25657466149148,
4.81935740125709));
#5531=CARTESIAN_POINT('Ctrl Pts',(-0.668872607647689,-1.19121499201174,
4.80925931640299));
#5532=CARTESIAN_POINT('Ctrl Pts',(-0.68683208899175,-1.18095110656499,4.80775297115189));
#5533=CARTESIAN_POINT('Ctrl Pts',(-0.712180473529222,-1.16569045844166,
4.80562934645844));
#5534=CARTESIAN_POINT('Ctrl Pts',(-0.719763462202887,-1.16102361786891,
4.80499439070001));
#5535=CARTESIAN_POINT('Ctrl Pts',(-0.732448992603572,-1.15304443405144,
4.8039334193592));
#5536=CARTESIAN_POINT('Ctrl Pts',(-0.73757582523318,-1.14977167346178,4.80350500180374));
#5537=CARTESIAN_POINT('Ctrl Pts',(-0.749345756293626,-1.14214709995494,
4.80252242096232));
#5538=CARTESIAN_POINT('Ctrl Pts',(-0.755973009903906,-1.13777145185798,
4.8019697957476));
#5539=CARTESIAN_POINT('Ctrl Pts',(-0.77490355692036,-1.12503411045038,4.80039190600163));
#5540=CARTESIAN_POINT('Ctrl Pts',(-0.787109342868636,-1.11652863797659,
4.79937535322496));
#5541=CARTESIAN_POINT('Ctrl Pts',(-0.851424215450019,-1.07013250615786,
4.79400920789582));
#5542=CARTESIAN_POINT('Ctrl Pts',(-0.90094822104981,-1.02878616432678,4.78984026274961));
#5543=CARTESIAN_POINT('Ctrl Pts',(-0.994074530355718,-0.939134799362403,
4.781518703794));
#5544=CARTESIAN_POINT('Ctrl Pts',(-1.03751477248749,-0.890910229189769,
4.77737570281461));
#5545=CARTESIAN_POINT('Ctrl Pts',(-1.1043431998229,-0.80517554617493,4.77026334189846));
#5546=CARTESIAN_POINT('Ctrl Pts',(-1.12963467533398,-0.769289595410338,
4.767352610358));
#5547=CARTESIAN_POINT('Ctrl Pts',(-1.1621089791819,-0.718148867280892,4.76324679818182));
#5548=CARTESIAN_POINT('Ctrl Pts',(-1.17080427200344,-0.703883790771883,
4.76210597745392));
#5549=CARTESIAN_POINT('Ctrl Pts',(-1.1853497715544,-0.679005646001912,4.76012176485244));
#5550=CARTESIAN_POINT('Ctrl Pts',(-1.19132451503696,-0.668467375212106,
4.75928288617851));
#5551=CARTESIAN_POINT('Ctrl Pts',(-1.20333033759404,-0.646619173637664,
4.75754622912605));
#5552=CARTESIAN_POINT('Ctrl Pts',(-1.20934395059617,-0.635301067567886,
4.75664794541302));
#5553=CARTESIAN_POINT('Ctrl Pts',(-1.22452749954289,-0.60572742380612,4.75430338493201));
#5554=CARTESIAN_POINT('Ctrl Pts',(-1.23344845118107,-0.587348403940899,
4.75284882060062));
#5555=CARTESIAN_POINT('Ctrl Pts',(-1.28685982250247,-0.470721978553352,
4.74362912820494));
#5556=CARTESIAN_POINT('Ctrl Pts',(-1.31998812292662,-0.367709640483615,
4.73548724351706));
#5557=CARTESIAN_POINT('Ctrl Pts',(-1.34880897368429,-0.22017632920495,4.72412420243323));
#5558=CARTESIAN_POINT('Ctrl Pts',(-1.35500795093921,-0.178092980712427,
4.72092134630269));
#5559=CARTESIAN_POINT('Ctrl Pts',(-1.36096412204414,-0.118471431837088,
4.71648596875408));
#5560=CARTESIAN_POINT('Ctrl Pts',(-1.36236298952932,-0.101123514533745,
4.71520763174413));
#5561=CARTESIAN_POINT('Ctrl Pts',(-1.36425807572886,-0.0702729931031215,
4.71296095144973));
#5562=CARTESIAN_POINT('Ctrl Pts',(-1.36488620198545,-0.0567809944053895,
4.71198742667749));
#5563=CARTESIAN_POINT('Ctrl Pts',(-1.36555403660669,-0.0357140512168756,
4.71048357585241));
#5564=CARTESIAN_POINT('Ctrl Pts',(-1.36573101351832,-0.0281447347595584,
4.70994651592604));
#5565=CARTESIAN_POINT('Ctrl Pts',(-1.36594741777065,-0.0137783931354472,
4.70893387845222));
#5566=CARTESIAN_POINT('Ctrl Pts',(-1.36599906528825,-0.00698199341434678,
4.70845771493244));
#5567=CARTESIAN_POINT('Ctrl Pts',(-1.36600135147124,0.00986649375045023,
4.70728393151332));
#5568=CARTESIAN_POINT('Ctrl Pts',(-1.36589176392689,0.0199184185880063,
4.7065894763613));
#5569=CARTESIAN_POINT('Ctrl Pts',(-1.36503552898715,0.0589371457037254,
4.703913262923));
#5570=CARTESIAN_POINT('Ctrl Pts',(-1.36347822159935,0.0878805814045542,
4.70196970638826));
#5571=CARTESIAN_POINT('Ctrl Pts',(-1.35642187881346,0.17013577990401,4.69650985455787));
#5572=CARTESIAN_POINT('Ctrl Pts',(-1.34870565060773,0.223204619487589,4.69306256591625));
#5573=CARTESIAN_POINT('Ctrl Pts',(-1.32008737048182,0.362087852607866,4.6839457501852));
#5574=CARTESIAN_POINT('Ctrl Pts',(-1.29395777398044,0.446552875525465,4.67828969535042));
#5575=CARTESIAN_POINT('Ctrl Pts',(-1.25122690709879,0.548532034280309,4.67087464663035));
#5576=CARTESIAN_POINT('Ctrl Pts',(-1.24207913296824,0.568942439811722,4.66936043630902));
#5577=CARTESIAN_POINT('Ctrl Pts',(-1.22673899618773,0.601033996416314,4.66692565248708));
#5578=CARTESIAN_POINT('Ctrl Pts',(-1.22087076822653,0.612866197486269,4.6660159901057));
#5579=CARTESIAN_POINT('Ctrl Pts',(-1.20935715716995,0.6352594976352,4.66427038843218));
#5580=CARTESIAN_POINT('Ctrl Pts',(-1.20374263221296,0.645835135533819,4.66343557453816));
#5581=CARTESIAN_POINT('Ctrl Pts',(-1.19042748359073,0.670138893273853,4.66149206892678));
#5582=CARTESIAN_POINT('Ctrl Pts',(-1.18262728790781,0.68381020109632,4.66037998041908));
#5583=CARTESIAN_POINT('Ctrl Pts',(-1.16579829320398,0.712156670846861,4.65803327081628));
#5584=CARTESIAN_POINT('Ctrl Pts',(-1.15672550157196,0.726800337368898,4.65679734481144));
#5585=CARTESIAN_POINT('Ctrl Pts',(-1.14737959883991,0.741266521681617,4.6555522104354));
#5586=CARTESIAN_POINT('',(-1.3659996708821,-0.000948235195896823,4.5899328338502));
#5587=CARTESIAN_POINT('Ctrl Pts',(-1.1473796037955,0.741266514011044,4.53716884124631));
#5588=CARTESIAN_POINT('Ctrl Pts',(-1.15767679492772,0.72532786460739,4.53845015724928));
#5589=CARTESIAN_POINT('Ctrl Pts',(-1.16764193692774,0.70917455145636,4.53971555061117));
#5590=CARTESIAN_POINT('Ctrl Pts',(-1.21332065966825,0.631555043677277,4.54566613716929));
#5591=CARTESIAN_POINT('Ctrl Pts',(-1.24453852880613,0.567568492559921,4.55019722722848));
#5592=CARTESIAN_POINT('Ctrl Pts',(-1.29621061788948,0.436632580775848,4.55925803753871));
#5593=CARTESIAN_POINT('Ctrl Pts',(-1.31678771034399,0.369971093617939,4.56377370522672));
#5594=CARTESIAN_POINT('Ctrl Pts',(-1.33714275305894,0.280190951277582,4.56994701280096));
#5595=CARTESIAN_POINT('Ctrl Pts',(-1.34155707699873,0.258229019814995,4.57146349227184));
#5596=CARTESIAN_POINT('Ctrl Pts',(-1.34771349509633,0.223156641365741,4.57390088528274));
#5597=CARTESIAN_POINT('Ctrl Pts',(-1.34980871957143,0.210111758630504,4.57481084092691));
#5598=CARTESIAN_POINT('Ctrl Pts',(-1.35337935489555,0.185616704484051,4.57652687584863));
#5599=CARTESIAN_POINT('Ctrl Pts',(-1.35489947434757,0.17417416366768,4.57733149092312));
#5600=CARTESIAN_POINT('Ctrl Pts',(-1.35765762039137,0.151184119954412,4.57895467316746));
#5601=CARTESIAN_POINT('Ctrl Pts',(-1.35889375766979,0.139637362233966,4.57977322779621));
#5602=CARTESIAN_POINT('Ctrl Pts',(-1.36170548673883,0.109780982559263,4.5818988621429));
#5603=CARTESIAN_POINT('Ctrl Pts',(-1.36305903328494,0.0914533261035226,
4.58321254625401));
#5604=CARTESIAN_POINT('Ctrl Pts',(-1.36536424005474,0.0484410470395323,
4.586317372959));
#5605=CARTESIAN_POINT('Ctrl Pts',(-1.36601681405356,0.0237477122534092,
4.58811669886924));
#5606=CARTESIAN_POINT('Ctrl Pts',(-1.3659996708821,-0.000948235195896823,
4.5899328338502));
#5607=CARTESIAN_POINT('Ctrl Pts',(-1.3659996719829,-0.000946648090267182,
4.5899327171348));
#5608=CARTESIAN_POINT('Ctrl Pts',(-1.36595114331841,-0.070972817751537,
4.59508242548681));
#5609=CARTESIAN_POINT('Ctrl Pts',(-1.36051799875388,-0.140887396100429,
4.60036457226783));
#5610=CARTESIAN_POINT('Ctrl Pts',(-1.3388872690427,-0.279868570277552,4.61100460506759));
#5611=CARTESIAN_POINT('Ctrl Pts',(-1.32262581051757,-0.348723951008327,
4.61634601331537));
#5612=CARTESIAN_POINT('Ctrl Pts',(-1.2971544923418,-0.42838632416305,4.62241832949855));
#5613=CARTESIAN_POINT('Ctrl Pts',(-1.2930234244454,-0.440698394500663,4.62335349172859));
#5614=CARTESIAN_POINT('Ctrl Pts',(-1.28624333581331,-0.459988851220078,
4.62481147022928));
#5615=CARTESIAN_POINT('Ctrl Pts',(-1.28371175022734,-0.467007292509119,
4.62534040285606));
#5616=CARTESIAN_POINT('Ctrl Pts',(-1.27874786051624,-0.480423509347495,
4.62634809897938));
#5617=CARTESIAN_POINT('Ctrl Pts',(-1.27632478880541,-0.486824275255625,
4.62682732176821));
#5618=CARTESIAN_POINT('Ctrl Pts',(-1.27012230492207,-0.502844043853325,
4.62802342626027));
#5619=CARTESIAN_POINT('Ctrl Pts',(-1.26628154862607,-0.512439126093901,
4.62873685730318));
#5620=CARTESIAN_POINT('Ctrl Pts',(-1.25122729122657,-0.548844939313722,
4.63143575787438));
#5621=CARTESIAN_POINT('Ctrl Pts',(-1.23926740253139,-0.575340839009211,
4.63338335620342));
#5622=CARTESIAN_POINT('Ctrl Pts',(-1.19339749134004,-0.668880283275949,
4.64026843517801));
#5623=CARTESIAN_POINT('Ctrl Pts',(-1.15481585758506,-0.733485015158952,
4.64504726983616));
#5624=CARTESIAN_POINT('Ctrl Pts',(-1.08290210021077,-0.834045263791338,
4.65301189859273));
#5625=CARTESIAN_POINT('Ctrl Pts',(-1.05260903830645,-0.871964560681386,
4.65615484802548));
#5626=CARTESIAN_POINT('Ctrl Pts',(-0.998314701884474,-0.932965036281039,
4.66155353576328));
#5627=CARTESIAN_POINT('Ctrl Pts',(-0.975370554469441,-0.95692633298336,
4.66377340766147));
#5628=CARTESIAN_POINT('Ctrl Pts',(-0.940681193381317,-0.990608704700189,
4.66706249214752));
#5629=CARTESIAN_POINT('Ctrl Pts',(-0.929608423515292,-1.00100692366398,
4.66810297767876));
#5630=CARTESIAN_POINT('Ctrl Pts',(-0.909548666636262,-1.01922473343583,
4.6699731183939));
#5631=CARTESIAN_POINT('Ctrl Pts',(-0.900628321787931,-1.02711559455379,
4.67079971005194));
#5632=CARTESIAN_POINT('Ctrl Pts',(-0.88137575759624,-1.04370260236612,4.67257384275476));
#5633=CARTESIAN_POINT('Ctrl Pts',(-0.871015536361471,-1.05236412923023,
4.67352265857536));
#5634=CARTESIAN_POINT('Ctrl Pts',(-0.842492168633863,-1.075500964574,4.67612013361844));
#5635=CARTESIAN_POINT('Ctrl Pts',(-0.824086257713378,-1.08966834519801,
4.67778046283123));
#5636=CARTESIAN_POINT('Ctrl Pts',(-0.719909877522258,-1.16570549804802,
4.68709720887509));
#5637=CARTESIAN_POINT('Ctrl Pts',(-0.627551705287686,-1.2179125719106,4.69510174683121));
#5638=CARTESIAN_POINT('Ctrl Pts',(-0.493169615378028,-1.27449878045169,
4.70611676616927));
#5639=CARTESIAN_POINT('Ctrl Pts',(-0.455550096628898,-1.28842457358354,
4.70913269548593));
#5640=CARTESIAN_POINT('Ctrl Pts',(-0.39421812463499,-1.30810523286756,4.7138955944236));
#5641=CARTESIAN_POINT('Ctrl Pts',(-0.370869704899116,-1.31491561132201,
4.71567386331182));
#5642=CARTESIAN_POINT('Ctrl Pts',(-0.33821014330455,-1.32350263183096,4.7181023534611));
#5643=CARTESIAN_POINT('Ctrl Pts',(-0.329044969029845,-1.32581097401784,
4.71877748313826));
#5644=CARTESIAN_POINT('Ctrl Pts',(-0.31327183904545,-1.32960995192767,4.71992762706408));
#5645=CARTESIAN_POINT('Ctrl Pts',(-0.306675577196369,-1.33114686183025,
4.72040508139338));
#5646=CARTESIAN_POINT('Ctrl Pts',(-0.292378482648678,-1.33436612108854,
4.72143211861859));
#5647=CARTESIAN_POINT('Ctrl Pts',(-0.284674151316659,-1.33603097179337,
4.72198076075845));
#5648=CARTESIAN_POINT('Ctrl Pts',(-0.262658774896931,-1.34058924719816,
4.72353598103835));
#5649=CARTESIAN_POINT('Ctrl Pts',(-0.248314691583184,-1.34332014734933,
4.72453422471723));
#5650=CARTESIAN_POINT('Ctrl Pts',(-0.158593510535252,-1.35891537145242,
4.73070016262247));
#5651=CARTESIAN_POINT('Ctrl Pts',(-0.0822819731337005,-1.3656630082639,
4.73560753158714));
#5652=CARTESIAN_POINT('Ctrl Pts',(0.0550589037583409,-1.36624604251924,
4.74443633102323));
#5653=CARTESIAN_POINT('Ctrl Pts',(0.115863559873802,-1.36243707277774,4.74834394047094));
#5654=CARTESIAN_POINT('Ctrl Pts',(0.214065368018784,-1.34966270060912,4.75485663279541));
#5655=CARTESIAN_POINT('Ctrl Pts',(0.251696095409365,-1.34315377305989,4.75740059341008));
#5656=CARTESIAN_POINT('Ctrl Pts',(0.304592678839958,-1.33170332414293,4.7610751249439));
#5657=CARTESIAN_POINT('Ctrl Pts',(0.320121994119462,-1.32805584093332,4.76216603399215));
#5658=CARTESIAN_POINT('Ctrl Pts',(0.347214089329831,-1.32118974371863,4.7640924812776));
#5659=CARTESIAN_POINT('Ctrl Pts',(0.358805155009196,-1.31808907419875,4.764924234507));
#5660=CARTESIAN_POINT('Ctrl Pts',(0.382965202017612,-1.31128384678621,4.76667451195091));
#5661=CARTESIAN_POINT('Ctrl Pts',(0.395524678476943,-1.30755033568398,4.76759388305945));
#5662=CARTESIAN_POINT('Ctrl Pts',(0.428886816590097,-1.29710824763192,4.77006244115314));
#5663=CARTESIAN_POINT('Ctrl Pts',(0.449584677418982,-1.29008031842112,4.77162164754501));
#5664=CARTESIAN_POINT('Ctrl Pts',(0.560555998539736,-1.24940534386587,4.78013720098553));
#5665=CARTESIAN_POINT('Ctrl Pts',(0.647232587107585,-1.20678113303573,4.78738128336765));
#5666=CARTESIAN_POINT('Ctrl Pts',(0.787111503412039,-1.1185624666084,4.79989112826457));
#5667=CARTESIAN_POINT('Ctrl Pts',(0.842659242023877,-1.07733639606051,4.80511122705955));
#5668=CARTESIAN_POINT('Ctrl Pts',(0.904886043370864,-1.02338338160022,4.81109479937021));
#5669=CARTESIAN_POINT('Ctrl Pts',(0.914791137473718,-1.01453906054054,4.81205153111534));
#5670=CARTESIAN_POINT('Ctrl Pts',(0.930103436200013,-1.00045998474769,4.81353526661675));
#5671=CARTESIAN_POINT('Ctrl Pts',(0.935598743359138,-0.995322852870971,
4.81406873164616));
#5672=CARTESIAN_POINT('Ctrl Pts',(0.945990997613875,-0.985445823188159,
4.81507898302722));
#5673=CARTESIAN_POINT('Ctrl Pts',(0.950895316948251,-0.98071429906692,4.8155563010248));
#5674=CARTESIAN_POINT('Ctrl Pts',(0.963028011288096,-0.968832502561183,
4.81673908790891));
#5675=CARTESIAN_POINT('Ctrl Pts',(0.970212533490589,-0.961637678191351,
4.81744127570779));
#5676=CARTESIAN_POINT('Ctrl Pts',(0.996698622197158,-0.934514575267737,
4.8200398234928));
#5677=CARTESIAN_POINT('Ctrl Pts',(1.01547332026404,-0.91407866905551,4.82190183511118));
#5678=CARTESIAN_POINT('Ctrl Pts',(1.08341102262867,-0.835450687671994,4.82878075736254));
#5679=CARTESIAN_POINT('Ctrl Pts',(1.12830406901466,-0.773749891877509,4.83362617620357));
#5680=CARTESIAN_POINT('Ctrl Pts',(1.19318275665264,-0.666829025529125,4.84168211776025));
#5681=CARTESIAN_POINT('Ctrl Pts',(1.21628048201297,-0.623704533628743,4.84484906425385));
#5682=CARTESIAN_POINT('Ctrl Pts',(1.2468431169362,-0.558457658420979,4.84961131698403));
#5683=CARTESIAN_POINT('Ctrl Pts',(1.25613450849916,-0.537232463251863,4.85115586697956));
#5684=CARTESIAN_POINT('Ctrl Pts',(1.2722553348868,-0.497698461355606,4.85403298315287));
#5685=CARTESIAN_POINT('Ctrl Pts',(1.27924035972624,-0.479459522795357,4.85536040943094));
#5686=CARTESIAN_POINT('Ctrl Pts',(1.29009619858651,-0.449185281741076,4.85756749914346));
#5687=CARTESIAN_POINT('Ctrl Pts',(1.2941953523752,-0.437234479901029,4.85843968159622));
#5688=CARTESIAN_POINT('Ctrl Pts',(1.30188595192241,-0.413756810702746,4.86015582246413));
#5689=CARTESIAN_POINT('Ctrl Pts',(1.30549151620741,-0.402235770216086,4.86099923421467));
#5690=CARTESIAN_POINT('Ctrl Pts',(1.31308835291425,-0.37678241166419,4.86286603220854));
#5691=CARTESIAN_POINT('Ctrl Pts',(1.31701150511735,-0.362831469171003,4.86389147901322));
#5692=CARTESIAN_POINT('Ctrl Pts',(1.32991069808374,-0.313992361839857,4.86749047562595));
#5693=CARTESIAN_POINT('Ctrl Pts',(1.33772744184804,-0.278816326032131,4.87009925536449));
#5694=CARTESIAN_POINT('Ctrl Pts',(1.36741811711657,-0.114836764744878,4.88234036029111));
#5695=CARTESIAN_POINT('Ctrl Pts',(1.37213161311019,0.0163524455795227,4.89244283506123));
#5696=CARTESIAN_POINT('Ctrl Pts',(1.35596657487202,0.166517601541037,4.9035542228749));
#5697=CARTESIAN_POINT('Ctrl Pts',(1.35332409044661,0.186781900917488,4.90504194485277));
#5698=CARTESIAN_POINT('Ctrl Pts',(1.34888506692909,0.215739660778059,4.90714431831962));
#5699=CARTESIAN_POINT('Ctrl Pts',(1.34745710748083,0.224485811057334,4.90777619224375));
#5700=CARTESIAN_POINT('Ctrl Pts',(1.34490671272466,0.239204625746198,4.90883364040639));
#5701=CARTESIAN_POINT('Ctrl Pts',(1.34382939566037,0.245184582643006,4.90926157823504));
#5702=CARTESIAN_POINT('Ctrl Pts',(1.34124759166072,0.25898715408451,4.91024533815495));
#5703=CARTESIAN_POINT('Ctrl Pts',(1.3397145368139,0.266804077906842,4.91079959505167));
#5704=CARTESIAN_POINT('Ctrl Pts',(1.33509816314236,0.289298848670706,4.9123874291092));
#5705=CARTESIAN_POINT('Ctrl Pts',(1.33184128227034,0.303940411558971,4.91341212283546));
#5706=CARTESIAN_POINT('Ctrl Pts',(1.31397432640489,0.378450661789922,4.91859545349527));
#5707=CARTESIAN_POINT('Ctrl Pts',(1.29556467300668,0.437341173733927,4.92259030502828));
#5708=CARTESIAN_POINT('Ctrl Pts',(1.25287940455285,0.547182200792347,4.93018118412665));
#5709=CARTESIAN_POINT('Ctrl Pts',(1.22930668083943,0.598264232838212,4.9337743033092));
#5710=CARTESIAN_POINT('Ctrl Pts',(1.17759852575842,0.694269191983003,4.94086231144321));
#5711=CARTESIAN_POINT('Ctrl Pts',(1.1498668453238,0.739292440570475,4.9443440068878));
#5712=CARTESIAN_POINT('Ctrl Pts',(1.10948155411394,0.797068750633401,4.94911169936519));
#5713=CARTESIAN_POINT('Ctrl Pts',(1.0990840263653,0.811345898689302,4.95031571036504));
#5714=CARTESIAN_POINT('Ctrl Pts',(1.08099510709363,0.835198347688162,4.95237429489441));
#5715=CARTESIAN_POINT('Ctrl Pts',(1.07344589569051,0.844879040797041,4.95322339480051));
#5716=CARTESIAN_POINT('Ctrl Pts',(1.05884004467203,0.863096986604661,4.95484823147545));
#5717=CARTESIAN_POINT('Ctrl Pts',(1.0518080078078,0.871652769426327,4.95562295739644));
#5718=CARTESIAN_POINT('Ctrl Pts',(1.03319712006584,0.893743221133499,4.95765453314885));
#5719=CARTESIAN_POINT('Ctrl Pts',(1.02145653679393,0.907138205876561,4.95891778600154));
#5720=CARTESIAN_POINT('Ctrl Pts',(0.975184120298329,0.957893495454662,4.96382984301967));
#5721=CARTESIAN_POINT('Ctrl Pts',(0.938841118700473,0.993539260683248,4.96755176567741));
#5722=CARTESIAN_POINT('Ctrl Pts',(0.832945069684957,1.08639533086097,4.97803011547806));
#5723=CARTESIAN_POINT('Ctrl Pts',(0.759595738793436,1.13888760918944,4.98490770271061));
#5724=CARTESIAN_POINT('Ctrl Pts',(0.649294228475388,1.20239968972569,4.99443298792593));
#5725=CARTESIAN_POINT('Ctrl Pts',(0.616209186307179,1.21968633940467,4.99719368475582));
#5726=CARTESIAN_POINT('Ctrl Pts',(0.572608233220814,1.24023961966086,5.00067522645961));
#5727=CARTESIAN_POINT('Ctrl Pts',(0.562705987928275,1.24476362948729,5.00145577680231));
#5728=CARTESIAN_POINT('Ctrl Pts',(0.546332882281975,1.25200863778534,5.00272858836615));
#5729=CARTESIAN_POINT('Ctrl Pts',(0.539893406529294,1.25479893402066,5.00322470182007));
#5730=CARTESIAN_POINT('Ctrl Pts',(0.526701757224817,1.2603946653866,5.00423150812331));
#5731=CARTESIAN_POINT('Ctrl Pts',(0.519948056032383,1.26319574056828,5.0047419550001));
#5732=CARTESIAN_POINT('Ctrl Pts',(0.501791201565178,1.27055593968199,5.00610173222198));
#5733=CARTESIAN_POINT('Ctrl Pts',(0.490348216875831,1.27501586599862,5.00694556370122));
#5734=CARTESIAN_POINT('Ctrl Pts',(0.415656170956776,1.30297288117292,5.01237833393758));
#5735=CARTESIAN_POINT('Ctrl Pts',(0.350792105499544,1.32191362271648,5.01675119553243));
#5736=CARTESIAN_POINT('Ctrl Pts',(0.216299211381655,1.35058293959469,5.02560741875803));
#5737=CARTESIAN_POINT('Ctrl Pts',(0.146793770598929,1.35989364199503,5.03007773978436));
#5738=CARTESIAN_POINT('Ctrl Pts',(0.0356485690951921,1.36615914636017,5.03737760941438));
#5739=CARTESIAN_POINT('Ctrl Pts',(-0.00566602963778863,1.36661224650933,
5.04012267363819));
#5740=CARTESIAN_POINT('Ctrl Pts',(-0.0633026394535889,1.36463071707727,
5.04403420918818));
#5741=CARTESIAN_POINT('Ctrl Pts',(-0.0796582736774609,1.36377371253939,
5.04515331245001));
#5742=CARTESIAN_POINT('Ctrl Pts',(-0.108024049438008,1.36177540205207,5.04711211071236));
#5743=CARTESIAN_POINT('Ctrl Pts',(-0.120042024082028,1.36076865674156,5.04794761069185));
#5744=CARTESIAN_POINT('Ctrl Pts',(-0.144911672283232,1.35835331415313,5.04968895994036));
#5745=CARTESIAN_POINT('Ctrl Pts',(-0.157759783042428,1.35692112864689,5.05059545423509));
#5746=CARTESIAN_POINT('Ctrl Pts',(-0.191411785425579,1.35268553044258,5.05298876195602));
#5747=CARTESIAN_POINT('Ctrl Pts',(-0.212174046011615,1.34958464115586,5.05448453181308));
#5748=CARTESIAN_POINT('Ctrl Pts',(-0.335123991915285,1.32831462317435,5.0634615162958));
#5749=CARTESIAN_POINT('Ctrl Pts',(-0.435026250830258,1.29902753213487,5.07128628303317));
#5750=CARTESIAN_POINT('Ctrl Pts',(-0.571642103511969,1.24143554984266,5.08249747965414));
#5751=CARTESIAN_POINT('Ctrl Pts',(-0.611787068824816,1.22215134840391,5.08585463934307));
#5752=CARTESIAN_POINT('Ctrl Pts',(-0.673743722892654,1.18857028046148,5.09107553852826));
#5753=CARTESIAN_POINT('Ctrl Pts',(-0.696211296417321,1.17555091423945,5.09297731184821));
#5754=CARTESIAN_POINT('Ctrl Pts',(-0.726524949418517,1.15681074477428,5.09554211102413));
#5755=CARTESIAN_POINT('Ctrl Pts',(-0.734700192448571,1.15163589836958,5.09623368356815));
#5756=CARTESIAN_POINT('Ctrl Pts',(-0.748529401938016,1.14267493948225,5.09740244493148));
#5757=CARTESIAN_POINT('Ctrl Pts',(-0.754211192439227,1.13893273219618,5.09788229219023));
#5758=CARTESIAN_POINT('Ctrl Pts',(-0.766316495362033,1.13082947372757,5.09890364714898));
#5759=CARTESIAN_POINT('Ctrl Pts',(-0.772731124447567,1.12645589638688,5.09944434732102));
#5760=CARTESIAN_POINT('Ctrl Pts',(-0.790645034106759,1.11401692044596,5.1009539391547));
#5761=CARTESIAN_POINT('Ctrl Pts',(-0.80205807828094,1.10582826259066,5.1019152372972));
#5762=CARTESIAN_POINT('Ctrl Pts',(-0.879085964851458,1.04874203299036,5.10841512788209));
#5763=CARTESIAN_POINT('Ctrl Pts',(-0.940326388376973,0.994204067604119,
5.11364974743673));
#5764=CARTESIAN_POINT('Ctrl Pts',(-1.03596822966245,0.892235609094701,5.12263682625932));
#5765=CARTESIAN_POINT('Ctrl Pts',(-1.0728831101018,0.847487938327814,5.12636530671964));
#5766=CARTESIAN_POINT('Ctrl Pts',(-1.12087425100975,0.781133882748675,5.13175664388382));
#5767=CARTESIAN_POINT('Ctrl Pts',(-1.13439091129913,0.761371241133774,5.13334610823854));
#5768=CARTESIAN_POINT('Ctrl Pts',(-1.14737960694915,0.741266509129622,5.1349525893656));
#5769=CARTESIAN_POINT('Origin',(0.,0.,-1.10921167016993));
#5770=CARTESIAN_POINT('',(-1.14737959943097,0.741266520766746,5.85369350940778));
#5771=CARTESIAN_POINT('',(-1.14737961474409,0.741266497064122,5.73596857206561));
#5772=CARTESIAN_POINT('',(-1.14737960344596,0.741266514552077,-1.10921167016993));
#5773=CARTESIAN_POINT('',(-1.36599939927838,0.00101398491177677,5.30997858642083));
#5774=CARTESIAN_POINT('Ctrl Pts',(-1.14737959943097,0.741266520766746,5.85369350940778));
#5775=CARTESIAN_POINT('Ctrl Pts',(-1.12811340835725,0.771087960124151,5.85103670934246));
#5776=CARTESIAN_POINT('Ctrl Pts',(-1.10768818488231,0.80015270559341,5.84840821513957));
#5777=CARTESIAN_POINT('Ctrl Pts',(-1.07904096174742,0.837713551471296,5.84498877000203));
#5778=CARTESIAN_POINT('Ctrl Pts',(-1.07181268446122,0.846942137620228,5.84414675067462));
#5779=CARTESIAN_POINT('Ctrl Pts',(-1.05995852614563,0.86168187722696,5.84280032055335));
#5780=CARTESIAN_POINT('Ctrl Pts',(-1.05540651333128,0.867251308693703,5.84229120035501));
#5781=CARTESIAN_POINT('Ctrl Pts',(-1.04626299955735,0.878259866956038,5.84128456402475));
#5782=CARTESIAN_POINT('Ctrl Pts',(-1.04167257144467,0.883699562818069,5.84078700820547));
#5783=CARTESIAN_POINT('Ctrl Pts',(-1.02964316162297,0.897730526525831,5.83950250054803));
#5784=CARTESIAN_POINT('Ctrl Pts',(-1.0221389317644,0.906265504193979,5.83872002301181));
#5785=CARTESIAN_POINT('Ctrl Pts',(-0.985286874755471,0.947139253643286,
5.83496156000605));
#5786=CARTESIAN_POINT('Ctrl Pts',(-0.954503372171459,0.97815494830725,5.83207469776374));
#5787=CARTESIAN_POINT('Ctrl Pts',(-0.880773689032535,1.04563869717357,5.82556086518511));
#5788=CARTESIAN_POINT('Ctrl Pts',(-0.836954522955105,1.08103195991599,5.82196567300046));
#5789=CARTESIAN_POINT('Ctrl Pts',(-0.730562427260768,1.15660895791635,5.8135622418388));
#5790=CARTESIAN_POINT('Ctrl Pts',(-0.666653002631692,1.19458679309199,5.80874250763971));
#5791=CARTESIAN_POINT('Ctrl Pts',(-0.582733046079055,1.23561594404124,5.80244364628271));
#5792=CARTESIAN_POINT('Ctrl Pts',(-0.565310879736616,1.24368328476196,5.80113808239805));
#5793=CARTESIAN_POINT('Ctrl Pts',(-0.536208454913331,1.25642132184685,5.79895726280657));
#5794=CARTESIAN_POINT('Ctrl Pts',(-0.524623029064137,1.26130278059111,5.7980891152715));
#5795=CARTESIAN_POINT('Ctrl Pts',(-0.501608207704325,1.27062801318209,5.79636365266059));
#5796=CARTESIAN_POINT('Ctrl Pts',(-0.490183068718569,1.27507916765229,5.79550667807287));
#5797=CARTESIAN_POINT('Ctrl Pts',(-0.462251404406642,1.28553026763013,5.79340979770544));
#5798=CARTESIAN_POINT('Ctrl Pts',(-0.445686485640865,1.29136669286971,5.79216472205752));
#5799=CARTESIAN_POINT('Ctrl Pts',(-0.379872986028528,1.3131380917556,5.78720956069329));
#5800=CARTESIAN_POINT('Ctrl Pts',(-0.329853423363826,1.32658610131011,5.78342296374403));
#5801=CARTESIAN_POINT('Ctrl Pts',(-0.193373360763067,1.3550828482592,5.77304821430273));
#5802=CARTESIAN_POINT('Ctrl Pts',(-0.106025444677121,1.3646977095611,5.76635160627938));
#5803=CARTESIAN_POINT('Ctrl Pts',(0.0201150312704392,1.36639400975591,5.75690010543974));
#5804=CARTESIAN_POINT('Ctrl Pts',(0.0586064109977944,1.36528496880573,5.75404822983349));
#5805=CARTESIAN_POINT('Ctrl Pts',(0.108250712098863,1.36175068911321,5.75044971052708));
#5806=CARTESIAN_POINT('Ctrl Pts',(0.11948871820148,1.36081064934967,5.74964045007355));
#5807=CARTESIAN_POINT('Ctrl Pts',(0.137083272822926,1.35911924259943,5.74838310679252));
#5808=CARTESIAN_POINT('Ctrl Pts',(0.14344808135378,1.3584622157274,5.7479302508863));
#5809=CARTESIAN_POINT('Ctrl Pts',(0.156792652316215,1.35698984541692,5.74698527775598));
#5810=CARTESIAN_POINT('Ctrl Pts',(0.163771168280475,1.35616532343295,5.74649372011592));
#5811=CARTESIAN_POINT('Ctrl Pts',(0.18158120642322,1.35392156097395,5.74524519028295));
#5812=CARTESIAN_POINT('Ctrl Pts',(0.192402929915145,1.35242613828876,5.74449222180828));
#5813=CARTESIAN_POINT('Ctrl Pts',(0.240522614915606,1.34518731647118,5.74116466539435));
#5814=CARTESIAN_POINT('Ctrl Pts',(0.277594310465031,1.33802914498583,5.73865615017316));
#5815=CARTESIAN_POINT('Ctrl Pts',(0.404466066749011,1.30803014009805,5.73011646518757));
#5816=CARTESIAN_POINT('Ctrl Pts',(0.492207106888203,1.27760288851509,5.72427505359968));
#5817=CARTESIAN_POINT('Ctrl Pts',(0.619886403456356,1.21820310367045,5.71509735254835));
#5818=CARTESIAN_POINT('Ctrl Pts',(0.662466281805737,1.19558172075626,5.71191394260033));
#5819=CARTESIAN_POINT('Ctrl Pts',(0.718848196878404,1.16168981017179,5.70746409455181));
#5820=CARTESIAN_POINT('Ctrl Pts',(0.733759802198443,1.15232914156233,5.70626376684042));
#5821=CARTESIAN_POINT('Ctrl Pts',(0.758646355095302,1.13602783400398,5.70421779487226));
#5822=CARTESIAN_POINT('Ctrl Pts',(0.768717406244891,1.12923738186927,5.70337766227386));
#5823=CARTESIAN_POINT('Ctrl Pts',(0.788993560471834,1.11516915312739,5.70166046108495));
#5824=CARTESIAN_POINT('Ctrl Pts',(0.799191698782948,1.10788342737899,5.70078315249443));
#5825=CARTESIAN_POINT('Ctrl Pts',(0.824598801950516,1.08919879938662,5.6985620235798));
#5826=CARTESIAN_POINT('Ctrl Pts',(0.839672373258382,1.07762119965418,5.69721151907929));
#5827=CARTESIAN_POINT('Ctrl Pts',(0.911450161597383,1.02007018549913,5.69061618078121));
#5828=CARTESIAN_POINT('Ctrl Pts',(0.964640752949628,0.96992256760908,5.68520996884125));
#5829=CARTESIAN_POINT('Ctrl Pts',(1.06442425962048,0.859483760170551,5.67400587012014));
#5830=CARTESIAN_POINT('Ctrl Pts',(1.11050640986662,0.799053935867799,5.6682202998947));
#5831=CARTESIAN_POINT('Ctrl Pts',(1.16647052175749,0.711402622186961,5.66049443552602));
#5832=CARTESIAN_POINT('Ctrl Pts',(1.18087277856443,0.687231329839464,5.65842816478654));
#5833=CARTESIAN_POINT('Ctrl Pts',(1.19947620653614,0.653695071007281,5.65566351393403));
#5834=CARTESIAN_POINT('Ctrl Pts',(1.20433281079463,0.644703740383673,5.65493202002744));
#5835=CARTESIAN_POINT('Ctrl Pts',(1.21226395527527,0.629617880907142,5.65372185512977));
#5836=CARTESIAN_POINT('Ctrl Pts',(1.21539447739533,0.623553402611398,5.65323994074028));
#5837=CARTESIAN_POINT('Ctrl Pts',(1.221872440534,0.61077006971569,5.65223399826883));
#5838=CARTESIAN_POINT('Ctrl Pts',(1.22521016544028,0.604046683897153,5.65171053597974));
#5839=CARTESIAN_POINT('Ctrl Pts',(1.23426188914298,0.585429490421958,5.650275532307));
#5840=CARTESIAN_POINT('Ctrl Pts',(1.23985941064889,0.573479531817133,5.64937058595956));
#5841=CARTESIAN_POINT('Ctrl Pts',(1.25221819251087,0.54606802855242,5.64732710258067));
#5842=CARTESIAN_POINT('Ctrl Pts',(1.25886797606314,0.530558353341643,5.6461939233601));
#5843=CARTESIAN_POINT('Ctrl Pts',(1.28044360758679,0.477544969917856,5.64238518879082));
#5844=CARTESIAN_POINT('Ctrl Pts',(1.29399491468335,0.439502695973512,5.63975976881507));
#5845=CARTESIAN_POINT('Ctrl Pts',(1.33721109196928,0.298740506565782,5.6302509688775));
#5846=CARTESIAN_POINT('Ctrl Pts',(1.35647811827134,0.1932479909177,5.62348217538948));
#5847=CARTESIAN_POINT('Ctrl Pts',(1.36468783518042,0.0639971828951293,5.61480067335884));
#5848=CARTESIAN_POINT('Ctrl Pts',(1.36556096056847,0.0413726154390076,5.61326840234323));
#5849=CARTESIAN_POINT('Ctrl Pts',(1.36605340070809,0.00547676935262888,
5.61081157977231));
#5850=CARTESIAN_POINT('Ctrl Pts',(1.36604218403481,-0.00778581354329597,
5.6098982983631));
#5851=CARTESIAN_POINT('Ctrl Pts',(1.3656536071336,-0.0330038856479323,5.60815012901416));
#5852=CARTESIAN_POINT('Ctrl Pts',(1.36531231819664,-0.0449587471834363,
5.60731642664285));
#5853=CARTESIAN_POINT('Ctrl Pts',(1.36416303783,-0.0725220855555203,5.60538202811318));
#5854=CARTESIAN_POINT('Ctrl Pts',(1.36324406248576,-0.0881239853978485,
5.60427803944421));
#5855=CARTESIAN_POINT('Ctrl Pts',(1.35932782890157,-0.139559094175983,5.60060697649554));
#5856=CARTESIAN_POINT('Ctrl Pts',(1.35518371153783,-0.175287134731346,5.59800587615646));
#5857=CARTESIAN_POINT('Ctrl Pts',(1.34113443382196,-0.265233713003493,5.59132512831303));
#5858=CARTESIAN_POINT('Ctrl Pts',(1.32934959755508,-0.319091086169834,5.5871996621979));
#5859=CARTESIAN_POINT('Ctrl Pts',(1.29063415975088,-0.455848726721799,5.57646944920219));
#5860=CARTESIAN_POINT('Ctrl Pts',(1.25896676498579,-0.537158615925589,5.56983106015817));
#5861=CARTESIAN_POINT('Ctrl Pts',(1.21357863623652,-0.627193969891007,5.56249802814622));
#5862=CARTESIAN_POINT('Ctrl Pts',(1.20719818571257,-0.639388738890343,5.56150556857924));
#5863=CARTESIAN_POINT('Ctrl Pts',(1.19699799102136,-0.658186857115488,5.5599791744674));
#5864=CARTESIAN_POINT('Ctrl Pts',(1.19330560205386,-0.66485778679711,5.55943819222689));
#5865=CARTESIAN_POINT('Ctrl Pts',(1.18618858797609,-0.677465570299977,5.55841756943209));
#5866=CARTESIAN_POINT('Ctrl Pts',(1.18277487450405,-0.683408050539663,5.55793734762481));
#5867=CARTESIAN_POINT('Ctrl Pts',(1.17427735270562,-0.69794585458701,5.55676405847408));
#5868=CARTESIAN_POINT('Ctrl Pts',(1.16914362488872,-0.706511794908748,5.5560740356382));
#5869=CARTESIAN_POINT('Ctrl Pts',(1.14904038219926,-0.739235995949547,5.55343990553807));
#5870=CARTESIAN_POINT('Ctrl Pts',(1.13341124766477,-0.762982871582658,5.55153248002844));
#5871=CARTESIAN_POINT('Ctrl Pts',(1.08723990934802,-0.828581966910275,5.54622354522196));
#5872=CARTESIAN_POINT('Ctrl Pts',(1.05504162121242,-0.869210313240072,5.5428866022548));
#5873=CARTESIAN_POINT('Ctrl Pts',(0.960193589929525,-0.975831662356207,
5.53370959418636));
#5874=CARTESIAN_POINT('Ctrl Pts',(0.893153656820455,-1.03754208210594,5.52789037941165));
#5875=CARTESIAN_POINT('Ctrl Pts',(0.802689002983414,-1.10550524574623,5.52030103713272));
#5876=CARTESIAN_POINT('Ctrl Pts',(0.784569004379448,-1.11843769123451,5.51879372696432));
#5877=CARTESIAN_POINT('Ctrl Pts',(0.755225044619035,-1.13831674253875,5.5163673597787));
#5878=CARTESIAN_POINT('Ctrl Pts',(0.744201969236459,-1.14555370129841,5.51545907792456));
#5879=CARTESIAN_POINT('Ctrl Pts',(0.722968187949847,-1.15905845366703,5.51371442503807));
#5880=CARTESIAN_POINT('Ctrl Pts',(0.712776364461891,-1.16535373943174,5.51287915614465));
#5881=CARTESIAN_POINT('Ctrl Pts',(0.688967071333869,-1.17963108315959,5.51093202598312));
#5882=CARTESIAN_POINT('Ctrl Pts',(0.675291659330994,-1.18751263384023,5.5098167265655));
#5883=CARTESIAN_POINT('Ctrl Pts',(0.629113799296732,-1.21307072154672,5.50605918041482));
#5884=CARTESIAN_POINT('Ctrl Pts',(0.59603281852178,-1.22966222034964,5.50338062668796));
#5885=CARTESIAN_POINT('Ctrl Pts',(0.50971590974709,-1.26865193555939,5.49642247401979));
#5886=CARTESIAN_POINT('Ctrl Pts',(0.455661276352021,-1.28905380745921,5.49209169331816));
#5887=CARTESIAN_POINT('Ctrl Pts',(0.321881874064552,-1.33007789978373,5.48151917735493));
#5888=CARTESIAN_POINT('Ctrl Pts',(0.241259433426665,-1.34703788201261,5.4752620821045));
#5889=CARTESIAN_POINT('Ctrl Pts',(0.145664043116108,-1.35828376228655,5.4682554512615));
#5890=CARTESIAN_POINT('Ctrl Pts',(0.13170673047209,-1.35970811873738,5.46724290876802));
#5891=CARTESIAN_POINT('Ctrl Pts',(0.109997125192415,-1.36158615818662,5.4656865992969));
#5892=CARTESIAN_POINT('Ctrl Pts',(0.102259161179741,-1.36218915911001,5.46513554955022));
#5893=CARTESIAN_POINT('Ctrl Pts',(0.0877257108335951,-1.36319717310451,
5.46410795574094));
#5894=CARTESIAN_POINT('Ctrl Pts',(0.0809320141986718,-1.36361737462213,
5.46363069247365));
#5895=CARTESIAN_POINT('Ctrl Pts',(0.0644618052833058,-1.36451255897796,
5.462480680883));
#5896=CARTESIAN_POINT('Ctrl Pts',(0.0547828935567366,-1.36493541835123,
5.46181069777981));
#5897=CARTESIAN_POINT('Ctrl Pts',(0.0190694938133556,-1.36611517761471,
5.45935738793531));
#5898=CARTESIAN_POINT('Ctrl Pts',(-0.00698225003111828,-1.36623049999388,
5.45760458150581));
#5899=CARTESIAN_POINT('Ctrl Pts',(-0.0777504449832397,-1.36451916767586,
5.45290486302397));
#5900=CARTESIAN_POINT('Ctrl Pts',(-0.122400546815885,-1.36124072985494,
5.450006118593));
#5901=CARTESIAN_POINT('Ctrl Pts',(-0.26934852992166,-1.34316056719411,5.44046590734403));
#5902=CARTESIAN_POINT('Ctrl Pts',(-0.370112591271138,-1.31895540498923,
5.43389606617279));
#5903=CARTESIAN_POINT('Ctrl Pts',(-0.486966884504906,-1.27642568474055,
5.42553864069193));
#5904=CARTESIAN_POINT('Ctrl Pts',(-0.506581308770287,-1.26876892071136,
5.42411067722837));
#5905=CARTESIAN_POINT('Ctrl Pts',(-0.537954635311713,-1.2556784303353,5.42178113253919));
#5906=CARTESIAN_POINT('Ctrl Pts',(-0.54982734971787,-1.25052523998784,5.42088881570568));
#5907=CARTESIAN_POINT('Ctrl Pts',(-0.572617020700198,-1.24024641057731,
5.41915416238086));
#5908=CARTESIAN_POINT('Ctrl Pts',(-0.583542879392435,-1.23514335315846,
5.41831264998797));
#5909=CARTESIAN_POINT('Ctrl Pts',(-0.609122052391537,-1.22278113668598,
5.41631835679555));
#5910=CARTESIAN_POINT('Ctrl Pts',(-0.623715115103117,-1.21540231897139,
5.41516159701297));
#5911=CARTESIAN_POINT('Ctrl Pts',(-0.674497387262082,-1.18856941308465,
5.41106695761327));
#5912=CARTESIAN_POINT('Ctrl Pts',(-0.709935049411847,-1.1677480858733,5.40808310346114));
#5913=CARTESIAN_POINT('Ctrl Pts',(-0.802522777739353,-1.10757483865519,
5.39993823675457));
#5914=CARTESIAN_POINT('Ctrl Pts',(-0.857701131903669,-1.06541635086511,
5.39469869524285));
#5915=CARTESIAN_POINT('Ctrl Pts',(-0.960434113196507,-0.973752402194657,
5.38428458147063));
#5916=CARTESIAN_POINT('Ctrl Pts',(-1.00795079010317,-0.924480667589373,
5.3791255862122));
#5917=CARTESIAN_POINT('Ctrl Pts',(-1.05945319542635,-0.862361284379285,
5.37327578903984));
#5918=CARTESIAN_POINT('Ctrl Pts',(-1.06719507006544,-0.852761846993567,
5.37238885976758));
#5919=CARTESIAN_POINT('Ctrl Pts',(-1.07932595386523,-0.83729631295194,5.37098852001014));
#5920=CARTESIAN_POINT('Ctrl Pts',(-1.08379940883366,-0.831497731931924,
5.37046973924917));
#5921=CARTESIAN_POINT('Ctrl Pts',(-1.09246490760222,-0.820076584204894,
5.36946054683667));
#5922=CARTESIAN_POINT('Ctrl Pts',(-1.09666065197684,-0.814457240238254,
5.36896991996012));
#5923=CARTESIAN_POINT('Ctrl Pts',(-1.10723959764355,-0.800058923374119,
5.36772707626161));
#5924=CARTESIAN_POINT('Ctrl Pts',(-1.11356195672795,-0.791235486326229,
5.36697879007257));
#5925=CARTESIAN_POINT('Ctrl Pts',(-1.14092055316001,-0.752076449634641,
5.36371151721501));
#5926=CARTESIAN_POINT('Ctrl Pts',(-1.16082911439143,-0.720968085848893,
5.36125567827709));
#5927=CARTESIAN_POINT('Ctrl Pts',(-1.20607386929054,-0.643526464700441,
5.35537606041516));
#5928=CARTESIAN_POINT('Ctrl Pts',(-1.23003197699511,-0.5964581567411,5.3519933548579));
#5929=CARTESIAN_POINT('Ctrl Pts',(-1.28275353915265,-0.476109263892447,
5.34354642634669));
#5930=CARTESIAN_POINT('Ctrl Pts',(-1.30802089038347,-0.4015173995275,5.33847916256507));
#5931=CARTESIAN_POINT('Ctrl Pts',(-1.33215155124514,-0.303061769322372,
5.33168540456953));
#5932=CARTESIAN_POINT('Ctrl Pts',(-1.33701660729152,-0.280821447301688,
5.33014492999682));
#5933=CARTESIAN_POINT('Ctrl Pts',(-1.34383773284858,-0.245423521469275,
5.32767808412711));
#5934=CARTESIAN_POINT('Ctrl Pts',(-1.34616136843354,-0.232340495840752,
5.32676314723762));
#5935=CARTESIAN_POINT('Ctrl Pts',(-1.35015251861225,-0.207793946913368,
5.32503951435536));
#5936=CARTESIAN_POINT('Ctrl Pts',(-1.35186579661275,-0.196338995950011,
5.32423232006003));
#5937=CARTESIAN_POINT('Ctrl Pts',(-1.35500114798998,-0.173384338772403,
5.32260852186823));
#5938=CARTESIAN_POINT('Ctrl Pts',(-1.35642297505521,-0.161885570886295,
5.32179198182166));
#5939=CARTESIAN_POINT('Ctrl Pts',(-1.35998783228077,-0.12969838390021,5.3194970049368));
#5940=CARTESIAN_POINT('Ctrl Pts',(-1.36180480488839,-0.108977817475672,
5.31800882229745));
#5941=CARTESIAN_POINT('Ctrl Pts',(-1.36507084082304,-0.0585147998587496,
5.31435673505237));
#5942=CARTESIAN_POINT('Ctrl Pts',(-1.36602175362683,-0.0287522005951587,
5.31217927100926));
#5943=CARTESIAN_POINT('Ctrl Pts',(-1.3659996224837,0.00101556604943034,
5.30997885891414));
#5944=CARTESIAN_POINT('Ctrl Pts',(-1.36599962363692,0.00101401369812244,
5.30997897366282));
#5945=CARTESIAN_POINT('Ctrl Pts',(-1.36591453674133,0.115636397574861,5.30150617172131));
#5946=CARTESIAN_POINT('Ctrl Pts',(-1.35140392567906,0.229783323934746,5.29268365016902));
#5947=CARTESIAN_POINT('Ctrl Pts',(-1.31641703436901,0.365594045425327,5.28229751583335));
#5948=CARTESIAN_POINT('Ctrl Pts',(-1.30932584318178,0.390229226810623,5.280420654698));
#5949=CARTESIAN_POINT('Ctrl Pts',(-1.29862120705221,0.423829850540205,5.27788313415047));
#5950=CARTESIAN_POINT('Ctrl Pts',(-1.29560019362518,0.432976827982795,5.27719468143049));
#5951=CARTESIAN_POINT('Ctrl Pts',(-1.29028227490084,0.448524103978794,5.27602936762576));
#5952=CARTESIAN_POINT('Ctrl Pts',(-1.28803393185139,0.454940457090177,5.27554989070704));
#5953=CARTESIAN_POINT('Ctrl Pts',(-1.28310718714189,0.468671109057133,5.27452718288019));
#5954=CARTESIAN_POINT('Ctrl Pts',(-1.2804140078954,0.47597966142664,5.2739847861442));
#5955=CARTESIAN_POINT('Ctrl Pts',(-1.27264996126539,0.49650628584666,5.27246591749855));
#5956=CARTESIAN_POINT('Ctrl Pts',(-1.26743575630958,0.509669558193727,5.27149718474744));
#5957=CARTESIAN_POINT('Ctrl Pts',(-1.23147895875168,0.596476080521171,5.26512890149727));
#5958=CARTESIAN_POINT('Ctrl Pts',(-1.19453447072306,0.667394026218049,5.26001719739372));
#5959=CARTESIAN_POINT('Ctrl Pts',(-1.15020188489181,0.736884263153701,5.25471866229315));
#5960=CARTESIAN_POINT('Ctrl Pts',(-1.14879384500244,0.739077461247534,5.2545511263618));
#5961=CARTESIAN_POINT('Ctrl Pts',(-1.14737960281818,0.741266515523794,5.25438358752252));
#5962=CARTESIAN_POINT('Ctrl Pts',(-1.14737960694915,0.741266509129622,5.1349525893656));
#5963=CARTESIAN_POINT('Ctrl Pts',(-1.15450894696792,0.730231261687857,5.13583436768247));
#5964=CARTESIAN_POINT('Ctrl Pts',(-1.16147922321502,0.719092948402125,5.13672125066156));
#5965=CARTESIAN_POINT('Ctrl Pts',(-1.17647240150357,0.694347267289952,5.13868640863433));
#5966=CARTESIAN_POINT('Ctrl Pts',(-1.1844214162519,0.680699135474698,5.13976688572985));
#5967=CARTESIAN_POINT('Ctrl Pts',(-1.19797950498453,0.656463683518967,5.14168150157374));
#5968=CARTESIAN_POINT('Ctrl Pts',(-1.20368936084057,0.645934492702167,5.1425120056133));
#5969=CARTESIAN_POINT('Ctrl Pts',(-1.21538765439165,0.62366852794634,5.14426629621625));
#5970=CARTESIAN_POINT('Ctrl Pts',(-1.22134618530777,0.611917524922512,5.14519101030784));
#5971=CARTESIAN_POINT('Ctrl Pts',(-1.2368934577186,0.580124263251856,5.1476908755887));
#5972=CARTESIAN_POINT('Ctrl Pts',(-1.24616438612236,0.559931966528528,5.14927650203044));
#5973=CARTESIAN_POINT('Ctrl Pts',(-1.29893217937928,0.437193445085112,5.15890798489505));
#5974=CARTESIAN_POINT('Ctrl Pts',(-1.33023776296448,0.329881369553427,5.16735092085455));
#5975=CARTESIAN_POINT('Ctrl Pts',(-1.35647845897519,0.169068066811006,5.17965084744787));
#5976=CARTESIAN_POINT('Ctrl Pts',(-1.36189655802888,0.117713919453158,5.18351917466306));
#5977=CARTESIAN_POINT('Ctrl Pts',(-1.36508952614646,0.0518784708489853,
5.18831831453016));
#5978=CARTESIAN_POINT('Ctrl Pts',(-1.36555813590157,0.0375740417395821,
5.18935133300515));
#5979=CARTESIAN_POINT('Ctrl Pts',(-1.36593363012036,0.0155294052801895,
5.19092581799107));
#5980=CARTESIAN_POINT('Ctrl Pts',(-1.36599967616427,0.00779338323103472,
5.19147502449439));
#5981=CARTESIAN_POINT('Ctrl Pts',(-1.36600028311803,-0.00675474728496466,
5.19250109548764));
#5982=CARTESIAN_POINT('Ctrl Pts',(-1.36594961932748,-0.0135660898302727,
5.19297865092577));
#5983=CARTESIAN_POINT('Ctrl Pts',(-1.36570284638087,-0.0301068606673808,
5.19413190119696));
#5984=CARTESIAN_POINT('Ctrl Pts',(-1.36545372279224,-0.0398350662353058,
5.1948047868326));
#5985=CARTESIAN_POINT('Ctrl Pts',(-1.36414327017427,-0.0759306051827434,
5.19728424352104));
#5986=CARTESIAN_POINT('Ctrl Pts',(-1.36242189053262,-0.102269862442182,
5.19905943513985));
#5987=CARTESIAN_POINT('Ctrl Pts',(-1.35563665462605,-0.174054276210706,
5.20384422909637));
#5988=CARTESIAN_POINT('Ctrl Pts',(-1.34905295166681,-0.21932239868494,5.20680351483517));
#5989=CARTESIAN_POINT('Ctrl Pts',(-1.32059528484207,-0.36369216799689,5.21628158880166));
#5990=CARTESIAN_POINT('Ctrl Pts',(-1.28995942306744,-0.460702006339788,
5.22273812161931));
#5991=CARTESIAN_POINT('Ctrl Pts',(-1.24024427337802,-0.572890479318851,
5.23098181524686));
#5992=CARTESIAN_POINT('Ctrl Pts',(-1.23116434737239,-0.592151692939552,
5.23242546088701));
#5993=CARTESIAN_POINT('Ctrl Pts',(-1.21582697051859,-0.622807735452572,
5.23477396790487));
#5994=CARTESIAN_POINT('Ctrl Pts',(-1.20985036748271,-0.634339629824502,
5.2356692715818));
#5995=CARTESIAN_POINT('Ctrl Pts',(-1.19802007244958,-0.65639072506628,5.23740527464382));
#5996=CARTESIAN_POINT('Ctrl Pts',(-1.19218996286681,-0.666921250279914,
5.23824509218044));
#5997=CARTESIAN_POINT('Ctrl Pts',(-1.17817805405076,-0.691459027069183,
5.24022825661707));
#5998=CARTESIAN_POINT('Ctrl Pts',(-1.16988455275361,-0.70540003274223,5.24137545907456));
#5999=CARTESIAN_POINT('Ctrl Pts',(-1.14022195309742,-0.753299108715682,
5.24539077706077));
#6000=CARTESIAN_POINT('Ctrl Pts',(-1.11760842305144,-0.786458195591769,
5.2483024893283));
#6001=CARTESIAN_POINT('Ctrl Pts',(-1.05378026584285,-0.871729423492695,
5.25615182126945));
#6002=CARTESIAN_POINT('Ctrl Pts',(-1.01017024646971,-0.921910856948246,
5.26116046551499));
#6003=CARTESIAN_POINT('Ctrl Pts',(-0.914880073155494,-1.01664731801719,
5.27132508363935));
#6004=CARTESIAN_POINT('Ctrl Pts',(-0.8631561031155,-1.06091490904156,5.27646737636355));
#6005=CARTESIAN_POINT('Ctrl Pts',(-0.796430891736597,-1.10989744827673,
5.28250192610961));
#6006=CARTESIAN_POINT('Ctrl Pts',(-0.784373012541011,-1.11845139941638,
5.28357023595833));
#6007=CARTESIAN_POINT('Ctrl Pts',(-0.765644706481638,-1.13128551349674,
5.285193060773));
#6008=CARTESIAN_POINT('Ctrl Pts',(-0.759072336608693,-1.13570591499868,
5.2857558207428));
#6009=CARTESIAN_POINT('Ctrl Pts',(-0.746815869255001,-1.14379535674293,
5.28679231903699));
#6010=CARTESIAN_POINT('Ctrl Pts',(-0.741142663988383,-1.14747954877711,
5.28726695350393));
#6011=CARTESIAN_POINT('Ctrl Pts',(-0.727534349771829,-1.15617378617581,
5.28839362033158));
#6012=CARTESIAN_POINT('Ctrl Pts',(-0.719574614510532,-1.16114445297622,
5.28904318559633));
#6013=CARTESIAN_POINT('Ctrl Pts',(-0.691211850959365,-1.17845264563038,
5.2913269143071));
#6014=CARTESIAN_POINT('Ctrl Pts',(-0.67053653688783,-1.19033834549166,5.29293578638724));
#6015=CARTESIAN_POINT('Ctrl Pts',(-0.615354038592541,-1.2201668983377,5.29711361778615));
#6016=CARTESIAN_POINT('Ctrl Pts',(-0.580372681738932,-1.23718866756822,
5.29964649054921));
#6017=CARTESIAN_POINT('Ctrl Pts',(-0.452290400755728,-1.29288278544482,
5.30867415504866));
#6018=CARTESIAN_POINT('Ctrl Pts',(-0.355713277352951,-1.32271671026837,
5.31505421068723));
#6019=CARTESIAN_POINT('Ctrl Pts',(-0.230017874135355,-1.34676936383823,
5.32357250719713));
#6020=CARTESIAN_POINT('Ctrl Pts',(-0.203155593040073,-1.35108237578636,
5.32540302832876));
#6021=CARTESIAN_POINT('Ctrl Pts',(-0.161990942479023,-1.35643642718762,
5.32823381365224));
#6022=CARTESIAN_POINT('Ctrl Pts',(-0.147770369659149,-1.35805918061005,
5.32921632115055));
#6023=CARTESIAN_POINT('Ctrl Pts',(-0.121724195876615,-1.36061746241729,
5.33102561009702));
#6024=CARTESIAN_POINT('Ctrl Pts',(-0.109906763257582,-1.3616229826134,5.33185015462506));
#6025=CARTESIAN_POINT('Ctrl Pts',(-0.0839330299346769,-1.36349270808605,
5.33367117010073));
#6026=CARTESIAN_POINT('Ctrl Pts',(-0.069773499646246,-1.36429056669935,
5.33466958069469));
#6027=CARTESIAN_POINT('Ctrl Pts',(-0.0282458582375009,-1.36598239856109,
5.33761562348487));
#6028=CARTESIAN_POINT('Ctrl Pts',(-0.000861671889294049,-1.36627406128866,
5.33958115885716));
#6029=CARTESIAN_POINT('Ctrl Pts',(0.0631276116285825,-1.36503193223893,
5.34423021943495));
#6030=CARTESIAN_POINT('Ctrl Pts',(0.0996978597546384,-1.36284893754478,
5.34693045470113));
#6031=CARTESIAN_POINT('Ctrl Pts',(0.190805737046929,-1.35372382115644,5.35375654223748));
#6032=CARTESIAN_POINT('Ctrl Pts',(0.245095090711306,-1.34495458559843,5.35791508980577));
#6033=CARTESIAN_POINT('Ctrl Pts',(0.358292675106155,-1.31958753500389,5.36668807334671));
#6034=CARTESIAN_POINT('Ctrl Pts',(0.416922557012886,-1.30225258848866,5.37129244626548));
#6035=CARTESIAN_POINT('Ctrl Pts',(0.488221750774554,-1.27586013114751,5.37683696645621));
#6036=CARTESIAN_POINT('Ctrl Pts',(0.502158164396142,-1.27043959958545,5.37791782775316));
#6037=CARTESIAN_POINT('Ctrl Pts',(0.523369815070111,-1.26178577087957,5.37955559857019));
#6038=CARTESIAN_POINT('Ctrl Pts',(0.530710008758775,-1.25871608775739,5.38012097599131));
#6039=CARTESIAN_POINT('Ctrl Pts',(0.543609729075416,-1.25318849435541,5.38111164132233));
#6040=CARTESIAN_POINT('Ctrl Pts',(0.549180054904535,-1.25075745429931,5.38153840741199));
#6041=CARTESIAN_POINT('Ctrl Pts',(0.562844952468293,-1.24468483289101,5.38258303300933));
#6042=CARTESIAN_POINT('Ctrl Pts',(0.570920552161064,-1.24100141323936,5.38319843589929));
#6043=CARTESIAN_POINT('Ctrl Pts',(0.597543686662399,-1.22854325160766,5.38522266207002));
#6044=CARTESIAN_POINT('Ctrl Pts',(0.6159303474781,-1.21942892136342,5.38661320724766));
#6045=CARTESIAN_POINT('Ctrl Pts',(0.750144277404238,-1.14908789390465,5.3967590978939));
#6046=CARTESIAN_POINT('Ctrl Pts',(0.856839600941048,-1.07189221334997,5.40486173155934));
#6047=CARTESIAN_POINT('Ctrl Pts',(0.976508263362306,-0.955854902042567,
5.41584235714626));
#6048=CARTESIAN_POINT('Ctrl Pts',(1.00111929850485,-0.93004666468943,5.41822073983362));
#6049=CARTESIAN_POINT('Ctrl Pts',(1.03423753057966,-0.892478081839303,5.42162035765726));
#6050=CARTESIAN_POINT('Ctrl Pts',(1.04361113327111,-0.881498821501704,5.42260676229364));
#6051=CARTESIAN_POINT('Ctrl Pts',(1.06049228539495,-0.861079282695392,5.424429926698));
#6052=CARTESIAN_POINT('Ctrl Pts',(1.06805225483812,-0.851684086545846,5.42526450665598));
#6053=CARTESIAN_POINT('Ctrl Pts',(1.0832891177097,-0.832226438155453,5.42698506388635));
#6054=CARTESIAN_POINT('Ctrl Pts',(1.09095250973728,-0.822154948513786,5.42787145531561));
#6055=CARTESIAN_POINT('Ctrl Pts',(1.11014688234491,-0.796188096474105,5.43014709425882));
#6056=CARTESIAN_POINT('Ctrl Pts',(1.12147671116343,-0.78014838378125,5.43154372455901));
#6057=CARTESIAN_POINT('Ctrl Pts',(1.18274654006279,-0.689314419547003,5.439407566593));
#6058=CARTESIAN_POINT('Ctrl Pts',(1.22554263320739,-0.609986676872524,5.4461286100276));
#6059=CARTESIAN_POINT('Ctrl Pts',(1.29008659352131,-0.455654134637411,5.45877579098599));
#6060=CARTESIAN_POINT('Ctrl Pts',(1.31382524117489,-0.381849726491105,5.46465400960749));
#6061=CARTESIAN_POINT('Ctrl Pts',(1.33444165695525,-0.292287511987954,5.4713505685251));
#6062=CARTESIAN_POINT('Ctrl Pts',(1.33747116650936,-0.2780961104876,5.47239870322061));
#6063=CARTESIAN_POINT('Ctrl Pts',(1.34179286840774,-0.256143940649222,5.47399746886107));
#6064=CARTESIAN_POINT('Ctrl Pts',(1.34324502771044,-0.24841623008786,5.47455599157326));
#6065=CARTESIAN_POINT('Ctrl Pts',(1.3458245366006,-0.234004806969269,5.47558909379036));
#6066=CARTESIAN_POINT('Ctrl Pts',(1.34696893962538,-0.227324902049264,5.47606450673496));
#6067=CARTESIAN_POINT('Ctrl Pts',(1.34959571309199,-0.211275605672952,5.47719887739154));
#6068=CARTESIAN_POINT('Ctrl Pts',(1.35103028880671,-0.20189884111409,5.47785526807297));
#6069=CARTESIAN_POINT('Ctrl Pts',(1.35582855022567,-0.168191016632206,5.48019454771902));
#6070=CARTESIAN_POINT('Ctrl Pts',(1.35863375904979,-0.143783730602052,5.48185048809029));
#6071=CARTESIAN_POINT('Ctrl Pts',(1.36433716832411,-0.0787352919552279,
5.4861948317873));
#6072=CARTESIAN_POINT('Ctrl Pts',(1.36607844843105,-0.0380166348105744,
5.48884348979549));
#6073=CARTESIAN_POINT('Ctrl Pts',(1.36578123411808,0.11117059056373,5.49847555341945));
#6074=CARTESIAN_POINT('Ctrl Pts',(1.35265206358475,0.219197996974596,5.50534478210836));
#6075=CARTESIAN_POINT('Ctrl Pts',(1.32178242462068,0.345411612577719,5.51407081230514));
#6076=CARTESIAN_POINT('Ctrl Pts',(1.31618427225149,0.366165042277167,5.51552769550149));
#6077=CARTESIAN_POINT('Ctrl Pts',(1.30641000050486,0.399272670101188,5.51789234947613));
#6078=CARTESIAN_POINT('Ctrl Pts',(1.30254242451737,0.411714666666021,5.5187903138062));
#6079=CARTESIAN_POINT('Ctrl Pts',(1.29476509769958,0.435527121282318,5.52052790072583));
#6080=CARTESIAN_POINT('Ctrl Pts',(1.29088201792773,0.446905058302476,5.52136659431758));
#6081=CARTESIAN_POINT('Ctrl Pts',(1.28144141310626,0.473417154370428,5.52334147662694));
#6082=CARTESIAN_POINT('Ctrl Pts',(1.27576523518989,0.488506829522304,5.52448142605063));
#6083=CARTESIAN_POINT('Ctrl Pts',(1.25530444153453,0.540109634754774,5.52843674867076));
#6084=CARTESIAN_POINT('Ctrl Pts',(1.23920963753097,0.57607863434675,5.5312939596283));
#6085=CARTESIAN_POINT('Ctrl Pts',(1.19282653851386,0.668767933763115,5.53892664413396));
#6086=CARTESIAN_POINT('Ctrl Pts',(1.16005123739714,0.724130811923968,5.54376793987982));
#6087=CARTESIAN_POINT('Ctrl Pts',(1.0828975709452,0.835694697594957,5.55402808007369));
#6088=CARTESIAN_POINT('Ctrl Pts',(1.03774605386802,0.891143992435052,5.55943647808425));
#6089=CARTESIAN_POINT('Ctrl Pts',(0.978379082116922,0.953385461254074,5.56570511368386));
#6090=CARTESIAN_POINT('Ctrl Pts',(0.968125439883169,0.963795954522817,5.56676072056508));
#6091=CARTESIAN_POINT('Ctrl Pts',(0.952084494709027,0.979567900517138,5.56836840087211));
#6092=CARTESIAN_POINT('Ctrl Pts',(0.946414830089232,0.985046767434491,5.56892849619608));
#6093=CARTESIAN_POINT('Ctrl Pts',(0.935787226642523,0.995140257627,5.56996284312835));
#6094=CARTESIAN_POINT('Ctrl Pts',(0.930842154921886,0.999767348427093,5.57043795154724));
#6095=CARTESIAN_POINT('Ctrl Pts',(0.918916759775011,1.01076071869798,5.57156939394643));
#6096=CARTESIAN_POINT('Ctrl Pts',(0.91190447952565,1.01709167477767,5.57222319874144));
#6097=CARTESIAN_POINT('Ctrl Pts',(0.886632082052517,1.0394370623333,5.57454128184999));
#6098=CARTESIAN_POINT('Ctrl Pts',(0.868010180181264,1.05503760788256,5.57617925030358));
#6099=CARTESIAN_POINT('Ctrl Pts',(0.817629650011505,1.0950065196732,5.58045955421784));
#6100=CARTESIAN_POINT('Ctrl Pts',(0.785198449424994,1.11849065204015,5.58306357320232));
#6101=CARTESIAN_POINT('Ctrl Pts',(0.663750928290365,1.1985436753139,5.59245878758647));
#6102=CARTESIAN_POINT('Ctrl Pts',(0.569306889965283,1.24617829552289,5.59913517343118));
#6103=CARTESIAN_POINT('Ctrl Pts',(0.448303040506616,1.2905544036315,5.60776001354228));
#6104=CARTESIAN_POINT('Ctrl Pts',(0.42607595765485,1.29806219295615,5.6093453932261));
#6105=CARTESIAN_POINT('Ctrl Pts',(0.39072035355457,1.30899857776846,5.61187537921978));
#6106=CARTESIAN_POINT('Ctrl Pts',(0.37771460871665,1.31281046734407,5.61280774555333));
#6107=CARTESIAN_POINT('Ctrl Pts',(0.354331873442698,1.31928755790913,5.61448813871794));
#6108=CARTESIAN_POINT('Ctrl Pts',(0.343976047294522,1.32202541746576,5.61523378354662));
#6109=CARTESIAN_POINT('Ctrl Pts',(0.319519434279017,1.32818441806638,5.61699862891258));
#6110=CARTESIAN_POINT('Ctrl Pts',(0.305394463595379,1.3315031768989,5.61802096386402));
#6111=CARTESIAN_POINT('Ctrl Pts',(0.262713128041464,1.34081659251518,5.62112057963922));
#6112=CARTESIAN_POINT('Ctrl Pts',(0.234016556084462,1.34612159437641,5.62321874550225));
#6113=CARTESIAN_POINT('Ctrl Pts',(0.165533348248381,1.35652584155136,5.62826225691103));
#6114=CARTESIAN_POINT('Ctrl Pts',(0.125650014033341,1.36079948602555,5.63122867071618));
#6115=CARTESIAN_POINT('Ctrl Pts',(0.0345545374194687,1.36652184158529,5.63805614746475));
#6116=CARTESIAN_POINT('Ctrl Pts',(-0.0166685924520419,1.36685688322614,
5.64193316556925));
#6117=CARTESIAN_POINT('Ctrl Pts',(-0.126444224446211,1.36140257736312,5.65024299845795));
#6118=CARTESIAN_POINT('Ctrl Pts',(-0.184857527009722,1.35470810540855,5.65466560896516));
#6119=CARTESIAN_POINT('Ctrl Pts',(-0.257245702894402,1.34164087358332,5.66002866586836));
#6120=CARTESIAN_POINT('Ctrl Pts',(-0.271785382853547,1.33877120373766,5.66109966220259));
#6121=CARTESIAN_POINT('Ctrl Pts',(-0.294028003511482,1.33400389203126,5.66272568811305));
#6122=CARTESIAN_POINT('Ctrl Pts',(-0.301765437545236,1.33227492638884,5.66328901017658));
#6123=CARTESIAN_POINT('Ctrl Pts',(-0.315412074212977,1.32910053109462,5.66427793783087));
#6124=CARTESIAN_POINT('Ctrl Pts',(-0.321327069112466,1.32768291212253,5.66470499245999));
#6125=CARTESIAN_POINT('Ctrl Pts',(-0.335890166129764,1.32408961557647,5.66575274189337));
#6126=CARTESIAN_POINT('Ctrl Pts',(-0.344526749376954,1.32186869381107,5.66637094094005));
#6127=CARTESIAN_POINT('Ctrl Pts',(-0.373208878357486,1.31419278822845,5.66841532619139));
#6128=CARTESIAN_POINT('Ctrl Pts',(-0.393152697705361,1.30836486508455,5.66982273237149));
#6129=CARTESIAN_POINT('Ctrl Pts',(-0.524356055665068,1.26675360255849,5.67903488684609));
#6130=CARTESIAN_POINT('Ctrl Pts',(-0.630770161749997,1.21727104312232,5.68631932571444));
#6131=CARTESIAN_POINT('Ctrl Pts',(-0.768598042118655,1.13019543368379,5.69696101541999));
#6132=CARTESIAN_POINT('Ctrl Pts',(-0.806326397234676,1.10359492348215,5.70001382961969));
#6133=CARTESIAN_POINT('Ctrl Pts',(-0.856291253176667,1.0644352346191,5.70431022711215));
#6134=CARTESIAN_POINT('Ctrl Pts',(-0.869742486589888,1.05347284754225,5.70549377981104));
#6135=CARTESIAN_POINT('Ctrl Pts',(-0.892212626495895,1.03443657372131,5.70751972656323));
#6136=CARTESIAN_POINT('Ctrl Pts',(-0.901339892813703,1.02649343752124,5.70835686590052));
#6137=CARTESIAN_POINT('Ctrl Pts',(-0.919747968330122,1.01003872400555,5.71007534708974));
#6138=CARTESIAN_POINT('Ctrl Pts',(-0.929018977764569,1.00151798258327,5.710957016416));
#6139=CARTESIAN_POINT('Ctrl Pts',(-0.952209409305448,0.979605174984993,
5.71320477249114));
#6140=CARTESIAN_POINT('Ctrl Pts',(-0.965964612166757,0.966044180412237,
5.71457788387072));
#6141=CARTESIAN_POINT('Ctrl Pts',(-1.03714106876451,0.892832260762352,5.72190206385362));
#6142=CARTESIAN_POINT('Ctrl Pts',(-1.08932881502182,0.828353515204724,5.72806542448722));
#6143=CARTESIAN_POINT('Ctrl Pts',(-1.13941107388268,0.753492984586296,5.73486557418252));
#6144=CARTESIAN_POINT('Ctrl Pts',(-1.14342019818566,0.747395134825857,5.73541698282043));
#6145=CARTESIAN_POINT('Ctrl Pts',(-1.14737961474409,0.741266497064122,5.73596857206561));
#6146=CARTESIAN_POINT('Origin',(0.,0.,-1.10921167016993));
#6147=CARTESIAN_POINT('',(-1.14737960337948,0.741266514654979,6.45569480720057));
#6148=CARTESIAN_POINT('',(-1.14737960347042,0.741266514514221,6.33682691740051));
#6149=CARTESIAN_POINT('',(-1.14737960344596,0.741266514552077,-1.10921167016993));
#6150=CARTESIAN_POINT('Ctrl Pts',(-1.14737960337948,0.741266514654979,6.45569480720057));
#6151=CARTESIAN_POINT('Ctrl Pts',(-1.14440445020754,0.745871646546051,6.45530983005762));
#6152=CARTESIAN_POINT('Ctrl Pts',(-1.14140160089578,0.750458822460515,6.45492383550652));
#6153=CARTESIAN_POINT('Ctrl Pts',(-1.12652618635747,0.772886796456123,6.45302407185668));
#6154=CARTESIAN_POINT('Ctrl Pts',(-1.1142631691645,0.790463627220123,6.45149600304674));
#6155=CARTESIAN_POINT('Ctrl Pts',(-1.0331256952661,0.901118037528676,6.4416153273618));
#6156=CARTESIAN_POINT('Ctrl Pts',(-0.953074742876551,0.98539384339097,6.4328220089232));
#6157=CARTESIAN_POINT('Ctrl Pts',(-0.835074385669332,1.08163819922126,6.42132631641499));
#6158=CARTESIAN_POINT('Ctrl Pts',(-0.805849997455173,1.1035834900728,6.41858373599471));
#6159=CARTESIAN_POINT('Ctrl Pts',(-0.75695234810557,1.13732244969378,6.41419692716241));
#6160=CARTESIAN_POINT('Ctrl Pts',(-0.737800584619165,1.14983897029597,6.41252619215766));
#6161=CARTESIAN_POINT('Ctrl Pts',(-0.710516083765737,1.16670799891075,6.41022063931965));
#6162=CARTESIAN_POINT('Ctrl Pts',(-0.702641005517084,1.17146757936909,6.40956367510072));
#6163=CARTESIAN_POINT('Ctrl Pts',(-0.688983873355262,1.17953447453376,6.40843966839099));
#6164=CARTESIAN_POINT('Ctrl Pts',(-0.683224854159839,1.18287960491944,6.40797035453718));
#6165=CARTESIAN_POINT('Ctrl Pts',(-0.670531960670527,1.19012864759636,6.40694626238539));
#6166=CARTESIAN_POINT('Ctrl Pts',(-0.663588153550101,1.19401427067333,6.40639258875045));
#6167=CARTESIAN_POINT('Ctrl Pts',(-0.643512574817295,1.20501895154721,6.40480947527345));
#6168=CARTESIAN_POINT('Ctrl Pts',(-0.630297024991605,1.21198383370177,6.40378882476267));
#6169=CARTESIAN_POINT('Ctrl Pts',(-0.562731053724689,1.24618837029166,6.39866509343204));
#6170=CARTESIAN_POINT('Ctrl Pts',(-0.506714121456532,1.26999768900327,6.3947213613623));
#6171=CARTESIAN_POINT('Ctrl Pts',(-0.383234688998911,1.31300419079069,6.38629660361829));
#6172=CARTESIAN_POINT('Ctrl Pts',(-0.315510738722809,1.33090246850612,6.38183374219945));
#6173=CARTESIAN_POINT('Ctrl Pts',(-0.204589781098267,1.35127103821574,6.3744478966227));
#6174=CARTESIAN_POINT('Ctrl Pts',(-0.162127400519548,1.3570204703536,6.37160435668986));
#6175=CARTESIAN_POINT('Ctrl Pts',(-0.102927092378867,1.36221794305548,6.3675752874553));
#6176=CARTESIAN_POINT('Ctrl Pts',(-0.0863617076294256,1.36336837506538,
6.36644104216258));
#6177=CARTESIAN_POINT('Ctrl Pts',(-0.057670769968438,1.36483592444291,6.36446258564259));
#6178=CARTESIAN_POINT('Ctrl Pts',(-0.0455541280466855,1.36529404283025,
6.36362275807181));
#6179=CARTESIAN_POINT('Ctrl Pts',(-0.0205305648774539,1.36590668673522,
6.36187868208877));
#6180=CARTESIAN_POINT('Ctrl Pts',(-0.00762438340186637,1.36603968814276,
6.36097386201327));
#6181=CARTESIAN_POINT('Ctrl Pts',(0.0260383138641941,1.36590953713018,6.35859914428232));
#6182=CARTESIAN_POINT('Ctrl Pts',(0.0467896724752679,1.36535618087983,6.3571206211887));
#6183=CARTESIAN_POINT('Ctrl Pts',(0.172310182162419,1.35914429087719,6.34808380490484));
#6184=CARTESIAN_POINT('Ctrl Pts',(0.276137723201556,1.34190324070143,6.34017403794649));
#6185=CARTESIAN_POINT('Ctrl Pts',(0.418778274807004,1.3009514838768,6.3289602822008));
#6186=CARTESIAN_POINT('Ctrl Pts',(0.460013119199794,1.28694923642598,6.32568102972326));
#6187=CARTESIAN_POINT('Ctrl Pts',(0.524337441251927,1.26161879470272,6.32056312438273));
#6188=CARTESIAN_POINT('Ctrl Pts',(0.547897212024778,1.25156724842174,6.31868830675984));
#6189=CARTESIAN_POINT('Ctrl Pts',(0.57993169930762,1.2368219047728,6.31615113337325));
#6190=CARTESIAN_POINT('Ctrl Pts',(0.588658580463402,1.2326922930434,6.31546122077102));
#6191=CARTESIAN_POINT('Ctrl Pts',(0.603476008832462,1.2254873480536,6.31429286983384));
#6192=CARTESIAN_POINT('Ctrl Pts',(0.609588510114468,1.22245833886558,6.31381181996603));
#6193=CARTESIAN_POINT('Ctrl Pts',(0.622657850208297,1.21585950349539,6.31278550451638));
#6194=CARTESIAN_POINT('Ctrl Pts',(0.629607100958736,1.21227556137372,6.31224108079112));
#6195=CARTESIAN_POINT('Ctrl Pts',(0.649149352704366,1.20198364502491,6.31071265810335));
#6196=CARTESIAN_POINT('Ctrl Pts',(0.661668979811253,1.19513755111781,6.30973652712519));
#6197=CARTESIAN_POINT('Ctrl Pts',(0.742687226976892,1.14917094478586,6.30342448182142));
#6198=CARTESIAN_POINT('Ctrl Pts',(0.807803204980027,1.10437099698966,6.29836831671898));
#6199=CARTESIAN_POINT('Ctrl Pts',(0.937508247894822,0.997489452536332,6.28756297667497));
#6200=CARTESIAN_POINT('Ctrl Pts',(1.00059698491479,0.934189540578288,6.28182713684428));
#6201=CARTESIAN_POINT('Ctrl Pts',(1.06936175443099,0.850175472799675,6.27450893565179));
#6202=CARTESIAN_POINT('Ctrl Pts',(1.08133589564082,0.83489251682933,6.27318906818643));
#6203=CARTESIAN_POINT('Ctrl Pts',(1.10054750895023,0.809265319325732,6.27099075328883));
#6204=CARTESIAN_POINT('Ctrl Pts',(1.10797475919416,0.799066387210834,6.27011964889677));
#6205=CARTESIAN_POINT('Ctrl Pts',(1.12224387337831,0.77889087501064,6.2684028283803));
#6206=CARTESIAN_POINT('Ctrl Pts',(1.1290965978954,0.768923378854817,6.26755762471015));
#6207=CARTESIAN_POINT('Ctrl Pts',(1.14391003359632,0.746751711100486,6.2656833531759));
#6208=CARTESIAN_POINT('Ctrl Pts',(1.15180956849467,0.734508660117627,6.2646521693244));
#6209=CARTESIAN_POINT('Ctrl Pts',(1.17881781509049,0.691142712383491,6.26101139636744));
#6210=CARTESIAN_POINT('Ctrl Pts',(1.19687151723236,0.659384431595825,6.25836549542448));
#6211=CARTESIAN_POINT('Ctrl Pts',(1.27339882629084,0.511243761276505,6.24611053992899));
#6212=CARTESIAN_POINT('Ctrl Pts',(1.31630705305452,0.387612538287398,6.23603828958759));
#6213=CARTESIAN_POINT('Ctrl Pts',(1.34494681228947,0.23977049999888,6.22495936165501));
#6214=CARTESIAN_POINT('Ctrl Pts',(1.34837645728437,0.219665331900744,6.22347456644959));
#6215=CARTESIAN_POINT('Ctrl Pts',(1.35264792892096,0.190730128241583,6.22137554938291));
#6216=CARTESIAN_POINT('Ctrl Pts',(1.35385587282002,0.181957928923353,6.22074416382356));
#6217=CARTESIAN_POINT('Ctrl Pts',(1.35574842334905,0.167149928308582,6.21968738627107));
#6218=CARTESIAN_POINT('Ctrl Pts',(1.35647819818583,0.161120418052551,6.21925963351081));
#6219=CARTESIAN_POINT('Ctrl Pts',(1.35807178484605,0.14717482494711,6.21827625673913));
#6220=CARTESIAN_POINT('Ctrl Pts',(1.358906633699,0.139255774759589,6.21772219879438));
#6221=CARTESIAN_POINT('Ctrl Pts',(1.36111422127253,0.116400341995082,6.21613448632429));
#6222=CARTESIAN_POINT('Ctrl Pts',(1.36231031820514,0.101447552015138,6.21510972949913));
#6223=CARTESIAN_POINT('Ctrl Pts',(1.36716353701563,0.0249396662897132,6.20992388297698));
#6224=CARTESIAN_POINT('Ctrl Pts',(1.3668963603584,-0.0367988979956117,6.20592696799781));
#6225=CARTESIAN_POINT('Ctrl Pts',(1.35737839888966,-0.168700863544685,6.19740924188006));
#6226=CARTESIAN_POINT('Ctrl Pts',(1.34685286961724,-0.238585335064236,6.19290607094659));
#6227=CARTESIAN_POINT('Ctrl Pts',(1.32164607377661,-0.347745789026422,6.18556117799279));
#6228=CARTESIAN_POINT('Ctrl Pts',(1.31048223161538,-0.387700007231746,6.18280552681886));
#6229=CARTESIAN_POINT('Ctrl Pts',(1.2923943968099,-0.442652727132081,6.17888197866998));
#6230=CARTESIAN_POINT('Ctrl Pts',(1.28698958831601,-0.458129320828903,6.17776192967536));
#6231=CARTESIAN_POINT('Ctrl Pts',(1.27712896707764,-0.48481226516603,6.17580252845228));
#6232=CARTESIAN_POINT('Ctrl Pts',(1.27280076988883,-0.496064023090694,6.17496739486579));
#6233=CARTESIAN_POINT('Ctrl Pts',(1.26353118474063,-0.519241321798936,6.17322784884794));
#6234=CARTESIAN_POINT('Ctrl Pts',(1.25856855822918,-0.531157009807242,6.1723228040802));
#6235=CARTESIAN_POINT('Ctrl Pts',(1.24512112689277,-0.562198471790177,6.16993588974925));
#6236=CARTESIAN_POINT('Ctrl Pts',(1.23636474060115,-0.581202103264453,6.16844513204998));
#6237=CARTESIAN_POINT('Ctrl Pts',(1.18135137566068,-0.693721256429585,6.1594351305149));
#6238=CARTESIAN_POINT('Ctrl Pts',(1.12494786305416,-0.78187273542734,6.15156768497056));
#6239=CARTESIAN_POINT('Ctrl Pts',(1.03111454543118,-0.897061554814988,6.14033238585897));
#6240=CARTESIAN_POINT('Ctrl Pts',(1.00149475503274,-0.930013607369452,6.13699264760518));
#6241=CARTESIAN_POINT('Ctrl Pts',(0.952112153077906,-0.979851019272929,
6.13179510033943));
#6242=CARTESIAN_POINT('Ctrl Pts',(0.933379017009408,-0.997712076012414,
6.12989955628111));
#6243=CARTESIAN_POINT('Ctrl Pts',(0.906970681146503,-1.02149571236173,6.12734193330027));
#6244=CARTESIAN_POINT('Ctrl Pts',(0.899724343702005,-1.02788395550298,6.12665146230513));
#6245=CARTESIAN_POINT('Ctrl Pts',(0.887263110893025,-1.03863679787903,6.12548409710729));
#6246=CARTESIAN_POINT('Ctrl Pts',(0.882082403951631,-1.04304020383841,6.12500455656652));
#6247=CARTESIAN_POINT('Ctrl Pts',(0.870910816259394,-1.05239285686619,6.12398303847046));
#6248=CARTESIAN_POINT('Ctrl Pts',(0.864910288107302,-1.05732992773473,6.12344187774078));
#6249=CARTESIAN_POINT('Ctrl Pts',(0.847928940834887,-1.07106040846325,6.12193033182987));
#6250=CARTESIAN_POINT('Ctrl Pts',(0.836853601307326,-1.07973606761225,6.12096756579873));
#6251=CARTESIAN_POINT('Ctrl Pts',(0.760817502329282,-1.13742454254391,6.11449728121188));
#6252=CARTESIAN_POINT('Ctrl Pts',(0.691715274520605,-1.18072488413482,6.10929006046853));
#6253=CARTESIAN_POINT('Ctrl Pts',(0.567250484647958,-1.24401542546841,6.10031400487418));
#6254=CARTESIAN_POINT('Ctrl Pts',(0.51370719297801,-1.26706425570585,6.0965679762011));
#6255=CARTESIAN_POINT('Ctrl Pts',(0.423821986447855,-1.29912073507177,6.09028582856094));
#6256=CARTESIAN_POINT('Ctrl Pts',(0.388291503652538,-1.31017903012344,6.0878048761877));
#6257=CARTESIAN_POINT('Ctrl Pts',(0.337074086496683,-1.32385318457558,6.0842044664804));
#6258=CARTESIAN_POINT('Ctrl Pts',(0.3217226887629,-1.32766737954676,6.0831223836814));
#6259=CARTESIAN_POINT('Ctrl Pts',(0.294626135083744,-1.33390222928798,6.08120542220118));
#6260=CARTESIAN_POINT('Ctrl Pts',(0.282908681953205,-1.33643644762305,6.08037419378321));
#6261=CARTESIAN_POINT('Ctrl Pts',(0.258242016487869,-1.34143235863214,6.07861884304774));
#6262=CARTESIAN_POINT('Ctrl Pts',(0.245287551443216,-1.34386149116407,6.07769379805122));
#6263=CARTESIAN_POINT('Ctrl Pts',(0.210414047757166,-1.34987970005337,6.07519411535882));
#6264=CARTESIAN_POINT('Ctrl Pts',(0.188440085098363,-1.35312213359127,6.07360902260546));
#6265=CARTESIAN_POINT('Ctrl Pts',(0.0753841768797939,-1.3669972563527,6.06539775923293));
#6266=CARTESIAN_POINT('Ctrl Pts',(-0.0165087501760205,-1.36897278954647,
6.05851537358678));
#6267=CARTESIAN_POINT('Ctrl Pts',(-0.158953219622941,-1.35768687377814,
6.04770758090593));
#6268=CARTESIAN_POINT('Ctrl Pts',(-0.209750261559177,-1.35077202641308,
6.04383083264569));
#6269=CARTESIAN_POINT('Ctrl Pts',(-0.287761429526375,-1.33564467113485,
6.0379297681569));
#6270=CARTESIAN_POINT('Ctrl Pts',(-0.315311021690413,-1.32941059993486,
6.0358566520489));
#6271=CARTESIAN_POINT('Ctrl Pts',(-0.352298666655904,-1.31982612694721,
6.03310439248042));
#6272=CARTESIAN_POINT('Ctrl Pts',(-0.361920435123491,-1.31722016746267,
6.03239133086418));
#6273=CARTESIAN_POINT('Ctrl Pts',(-0.378107732938875,-1.31264523167021,
6.03119756511241));
#6274=CARTESIAN_POINT('Ctrl Pts',(-0.384688406119156,-1.31073178064364,
6.03071392181081));
#6275=CARTESIAN_POINT('Ctrl Pts',(-0.398572135039674,-1.30658125738923,
6.02969736262084));
#6276=CARTESIAN_POINT('Ctrl Pts',(-0.405871245646881,-1.30433234572426,
6.02916510129971));
#6277=CARTESIAN_POINT('Ctrl Pts',(-0.426324834242277,-1.29784211309081,
6.02767871498929));
#6278=CARTESIAN_POINT('Ctrl Pts',(-0.439434773335473,-1.29346207193785,
6.02673197952802));
#6279=CARTESIAN_POINT('Ctrl Pts',(-0.534104287670281,-1.26022730997512,
6.01992359983421));
#6280=CARTESIAN_POINT('Ctrl Pts',(-0.612836336047709,-1.22387739829746,
6.01440581546567));
#6281=CARTESIAN_POINT('Ctrl Pts',(-0.759231301078887,-1.13859327465452,
6.00351144808931));
#6282=CARTESIAN_POINT('Ctrl Pts',(-0.826899319098853,-1.09044121198202,
5.99815820758992));
#6283=CARTESIAN_POINT('Ctrl Pts',(-0.904440483505733,-1.02387334794342,
5.9912686712639));
#6284=CARTESIAN_POINT('Ctrl Pts',(-0.918829536599898,-1.01098043591348,
5.98995512418428));
#6285=CARTESIAN_POINT('Ctrl Pts',(-0.942139537993689,-0.989185381330332,
5.987764686366));
#6286=CARTESIAN_POINT('Ctrl Pts',(-0.951219622387305,-0.980456954393349,
5.98689503877151));
#6287=CARTESIAN_POINT('Ctrl Pts',(-0.968785917618262,-0.96309725571591,
5.98517916100943));
#6288=CARTESIAN_POINT('Ctrl Pts',(-0.977280678003605,-0.954476263679363,
5.98433341916004));
#6289=CARTESIAN_POINT('Ctrl Pts',(-0.99767685882617,-0.933219248255586,
5.98226260526604));
#6290=CARTESIAN_POINT('Ctrl Pts',(-1.00945386027575,-0.920467345826625,
5.98103246779922));
#6291=CARTESIAN_POINT('Ctrl Pts',(-1.05159886445962,-0.873051785552421,
5.97649973291954));
#6292=CARTESIAN_POINT('Ctrl Pts',(-1.08044761741099,-0.8370852399255,5.97313842627058));
#6293=CARTESIAN_POINT('Ctrl Pts',(-1.17589104567685,-0.704921059882282,
5.96105327948384));
#6294=CARTESIAN_POINT('Ctrl Pts',(-1.23189474927965,-0.601718948704819,
5.95203582672786));
#6295=CARTESIAN_POINT('Ctrl Pts',(-1.28156798426731,-0.473256692169054,
5.94189766057578));
#6296=CARTESIAN_POINT('Ctrl Pts',(-1.28862410383586,-0.453691996609041,
5.94038288996042));
#6297=CARTESIAN_POINT('Ctrl Pts',(-1.29806536655051,-0.425513677613729,
5.93824975337007));
#6298=CARTESIAN_POINT('Ctrl Pts',(-1.30081672326878,-0.417026916630356,
5.93761349974809));
#6299=CARTESIAN_POINT('Ctrl Pts',(-1.30530417774433,-0.402708348064585,
5.93655112927669));
#6300=CARTESIAN_POINT('Ctrl Pts',(-1.30708474808069,-0.396891013779978,
5.9361225930048));
#6301=CARTESIAN_POINT('Ctrl Pts',(-1.31109587051744,-0.383466369127569,
5.9351408493504));
#6302=CARTESIAN_POINT('Ctrl Pts',(-1.31329915579811,-0.375851264781785,
5.93458916630575));
#6303=CARTESIAN_POINT('Ctrl Pts',(-1.31942870003773,-0.353953796880181,
5.93301653595154));
#6304=CARTESIAN_POINT('Ctrl Pts',(-1.32318925783754,-0.339625701442354,
5.93200421434232));
#6305=CARTESIAN_POINT('Ctrl Pts',(-1.34065302965984,-0.268387318971649,
5.92704036557674));
#6306=CARTESIAN_POINT('Ctrl Pts',(-1.35092281608484,-0.21069252994807,5.92323653002666));
#6307=CARTESIAN_POINT('Ctrl Pts',(-1.36310831423466,-0.102232810880837,
5.91619935983331));
#6308=CARTESIAN_POINT('Ctrl Pts',(-1.36595936467849,-0.0516798434778776,
5.91296421690439));
#6309=CARTESIAN_POINT('Ctrl Pts',(-1.366047001476,0.0586057802240502,5.90582635074415));
#6310=CARTESIAN_POINT('Ctrl Pts',(-1.362181923725,0.118229610721552,5.90191469227535));
#6311=CARTESIAN_POINT('Ctrl Pts',(-1.35201016131709,0.19588768243336,5.89662787991302));
#6312=CARTESIAN_POINT('Ctrl Pts',(-1.34921135206583,0.214317829707607,5.89535915937795));
#6313=CARTESIAN_POINT('Ctrl Pts',(-1.34412573925723,0.24373718572544,5.89330841556674));
#6314=CARTESIAN_POINT('Ctrl Pts',(-1.34207903734226,0.25476589893796,5.8925338501391));
#6315=CARTESIAN_POINT('Ctrl Pts',(-1.33753296025065,0.277685426158528,5.89091142799491));
#6316=CARTESIAN_POINT('Ctrl Pts',(-1.33501029714375,0.289570553369898,5.89006290951559));
#6317=CARTESIAN_POINT('Ctrl Pts',(-1.32859364054022,0.317933294837616,5.8880199565238));
#6318=CARTESIAN_POINT('Ctrl Pts',(-1.32455125394838,0.334374896836102,5.8868209794133));
#6319=CARTESIAN_POINT('Ctrl Pts',(-1.30844645651988,0.394994840010479,5.88234354358863));
#6320=CARTESIAN_POINT('Ctrl Pts',(-1.29447161457298,0.438629073356744,5.87900658410948));
#6321=CARTESIAN_POINT('Ctrl Pts',(-1.24785192896617,0.562405982736412,5.86920991196423));
#6322=CARTESIAN_POINT('Ctrl Pts',(-1.2097545625888,0.640255153364024,5.86261965587765));
#6323=CARTESIAN_POINT('Ctrl Pts',(-1.15894021175953,0.723138427875389,5.85530498938922));
#6324=CARTESIAN_POINT('Ctrl Pts',(-1.15321303393221,0.73223715878447,5.85449793769901));
#6325=CARTESIAN_POINT('Ctrl Pts',(-1.14737959943097,0.741266520766746,5.85369350940778));
#6326=CARTESIAN_POINT('',(-1.36599948656567,0.000864816812998655,5.78997189030577));
#6327=CARTESIAN_POINT('Ctrl Pts',(-1.14737961474409,0.741266497064122,5.73596857206561));
#6328=CARTESIAN_POINT('Ctrl Pts',(-1.1904390391621,0.674616370563709,5.74196721228499));
#6329=CARTESIAN_POINT('Ctrl Pts',(-1.22761917360703,0.604325674625206,5.74799784971009));
#6330=CARTESIAN_POINT('Ctrl Pts',(-1.26385745663935,0.518469722964953,5.75477595797064));
#6331=CARTESIAN_POINT('Ctrl Pts',(-1.26903215898028,0.50567177192747,5.75577147868141));
#6332=CARTESIAN_POINT('Ctrl Pts',(-1.27676541420663,0.485679235051532,5.75730143114503));
#6333=CARTESIAN_POINT('Ctrl Pts',(-1.27945899464218,0.478538327087086,5.75784296259488));
#6334=CARTESIAN_POINT('Ctrl Pts',(-1.28445557466837,0.464948131192376,5.75886375145181));
#6335=CARTESIAN_POINT('Ctrl Pts',(-1.28677004381773,0.458503810711634,5.75934358414366));
#6336=CARTESIAN_POINT('Ctrl Pts',(-1.29233212524565,0.442643063548985,5.76051474460296));
#6337=CARTESIAN_POINT('Ctrl Pts',(-1.29552538832794,0.433208017806375,5.76120303571006));
#6338=CARTESIAN_POINT('Ctrl Pts',(-1.30736921686815,0.396910689697875,5.76382194096085));
#6339=CARTESIAN_POINT('Ctrl Pts',(-1.31529041836771,0.369815814102299,5.76571640831512));
#6340=CARTESIAN_POINT('Ctrl Pts',(-1.35126590273527,0.230914257858472,5.77521477579502));
#6341=CARTESIAN_POINT('Ctrl Pts',(-1.36592675483423,0.116128576340583,5.78240718741147));
#6342=CARTESIAN_POINT('Ctrl Pts',(-1.36599972625862,0.000864789789742776,
5.78997147629599));
#6343=CARTESIAN_POINT('Ctrl Pts',(-1.14737960347042,0.741266514514221,6.33682691740051));
#6344=CARTESIAN_POINT('Ctrl Pts',(-1.14723096453265,0.741496587345168,6.33680902383529));
#6345=CARTESIAN_POINT('Ctrl Pts',(-1.14708225500945,0.741726617610742,6.33679112826742));
#6346=CARTESIAN_POINT('Ctrl Pts',(-1.12525165515805,0.77547285771292,6.33416500414653));
#6347=CARTESIAN_POINT('Ctrl Pts',(-1.10211318795007,0.808019388345351,6.33151930391138));
#6348=CARTESIAN_POINT('Ctrl Pts',(-1.07059991158523,0.848469820141379,6.32801762349369));
#6349=CARTESIAN_POINT('Ctrl Pts',(-1.06350279087134,0.857348819772749,6.32723504209464));
#6350=CARTESIAN_POINT('Ctrl Pts',(-1.05223168284591,0.871094468075964,6.32599963840549));
#6351=CARTESIAN_POINT('Ctrl Pts',(-1.04813264084159,0.876022288293213,6.32555183897138));
#6352=CARTESIAN_POINT('Ctrl Pts',(-1.03948157824367,0.88627485665296,6.32460939732392));
#6353=CARTESIAN_POINT('Ctrl Pts',(-1.03492304926233,0.891593712006638,6.32411425894315));
#6354=CARTESIAN_POINT('Ctrl Pts',(-1.02321928075941,0.905038891851274,6.32284720487594));
#6355=CARTESIAN_POINT('Ctrl Pts',(-1.01601812235669,0.9131156818452,6.32207150324614));
#6356=CARTESIAN_POINT('Ctrl Pts',(-0.984084033010925,0.948087367889869,
6.31865159366154));
#6357=CARTESIAN_POINT('Ctrl Pts',(-0.958375517571697,0.974067203004257,
6.31595015759383));
#6358=CARTESIAN_POINT('Ctrl Pts',(-0.869195900675413,1.05723681358068,6.30682937812303));
#6359=CARTESIAN_POINT('Ctrl Pts',(-0.801405968763932,1.10950471419032,6.30030422555004));
#6360=CARTESIAN_POINT('Ctrl Pts',(-0.682668169963466,1.18445981664098,6.28982482379678));
#6361=CARTESIAN_POINT('Ctrl Pts',(-0.634425256535374,1.21098590210553,6.28578812494159));
#6362=CARTESIAN_POINT('Ctrl Pts',(-0.568053821610563,1.24242120255726,6.28052933440924));
#6363=CARTESIAN_POINT('Ctrl Pts',(-0.551240836551429,1.24997167475445,6.27922092291943));
#6364=CARTESIAN_POINT('Ctrl Pts',(-0.523987835425009,1.26155372288526,6.2771367374175));
#6365=CARTESIAN_POINT('Ctrl Pts',(-0.513642627249782,1.26580105545935,6.27635390555899));
#6366=CARTESIAN_POINT('Ctrl Pts',(-0.491919902409015,1.27440936873442,6.27472693046606));
#6367=CARTESIAN_POINT('Ctrl Pts',(-0.480533807818921,1.2787461459087,6.27388364134074));
#6368=CARTESIAN_POINT('Ctrl Pts',(-0.45301878601578,1.28880674524566,6.27186756907271));
#6369=CARTESIAN_POINT('Ctrl Pts',(-0.436837103257292,1.29438102427092,6.27069969966985));
#6370=CARTESIAN_POINT('Ctrl Pts',(-0.375459820246054,1.31424212702984,6.26633131726732));
#6371=CARTESIAN_POINT('Ctrl Pts',(-0.329633485626932,1.32647838928624,6.26319520891731));
#6372=CARTESIAN_POINT('Ctrl Pts',(-0.191334400224435,1.35579390127283,6.25397054412427));
#6373=CARTESIAN_POINT('Ctrl Pts',(-0.0976491674684298,1.36574129866363,
6.24804701724237));
#6374=CARTESIAN_POINT('Ctrl Pts',(0.033993280002979,1.36609677200363,6.23942680174019));
#6375=CARTESIAN_POINT('Ctrl Pts',(0.0716597263597227,1.36463924751874,6.23692372875893));
#6376=CARTESIAN_POINT('Ctrl Pts',(0.120374236612702,1.36073193415394,6.23358444143237));
#6377=CARTESIAN_POINT('Ctrl Pts',(0.131522648630233,1.35969964545806,6.23281325655067));
#6378=CARTESIAN_POINT('Ctrl Pts',(0.149006497069655,1.35786370043844,6.23159107075647));
#6379=CARTESIAN_POINT('Ctrl Pts',(0.155351423310136,1.35715242185572,6.23114489233996));
#6380=CARTESIAN_POINT('Ctrl Pts',(0.168684834346834,1.35556299594173,6.23020127260897));
#6381=CARTESIAN_POINT('Ctrl Pts',(0.175671872813295,1.35467523587653,6.22970328607124));
#6382=CARTESIAN_POINT('Ctrl Pts',(0.193559226041958,1.35226179829853,6.22841991884293));
#6383=CARTESIAN_POINT('Ctrl Pts',(0.20444835674903,1.35065835603961,6.22763056677145));
#6384=CARTESIAN_POINT('Ctrl Pts',(0.253589639516747,1.34281437758426,6.22403513984802));
#6385=CARTESIAN_POINT('Ctrl Pts',(0.291581993739851,1.33507959679299,6.22116467483921));
#6386=CARTESIAN_POINT('Ctrl Pts',(0.425778015598182,1.30175783987426,6.2108068676161));
#6387=CARTESIAN_POINT('Ctrl Pts',(0.519467878813218,1.26728718328051,6.20319381413474));
#6388=CARTESIAN_POINT('Ctrl Pts',(0.646023166964252,1.20430858652762,6.19275250421038));
#6389=CARTESIAN_POINT('Ctrl Pts',(0.682593097560144,1.18396469732931,6.18971022100872));
#6390=CARTESIAN_POINT('Ctrl Pts',(0.732521085941029,1.15310592738439,6.18552090943373));
#6391=CARTESIAN_POINT('Ctrl Pts',(0.746702037525502,1.14397400907077,6.18432662354723));
#6392=CARTESIAN_POINT('Ctrl Pts',(0.770691846055378,1.12788939300134,6.1822976436892));
#6393=CARTESIAN_POINT('Ctrl Pts',(0.780584403000371,1.12106574761171,6.18145837105975));
#6394=CARTESIAN_POINT('Ctrl Pts',(0.800767046223592,1.10674755226151,6.17974006956903));
#6395=CARTESIAN_POINT('Ctrl Pts',(0.81104502831989,1.09923791219301,6.1788617122077));
#6396=CARTESIAN_POINT('Ctrl Pts',(0.837201690498609,1.07955984577203,6.17661652434054));
#6397=CARTESIAN_POINT('Ctrl Pts',(0.852921088848621,1.06718405886742,6.1752577173778));
#6398=CARTESIAN_POINT('Ctrl Pts',(0.933020639030918,1.00122130650264,6.1682712458327));
#6399=CARTESIAN_POINT('Ctrl Pts',(0.992646369926603,0.9421396147417,6.16286934869321));
#6400=CARTESIAN_POINT('Ctrl Pts',(1.10038364310237,0.813721818013225,6.15209304523007));
#6401=CARTESIAN_POINT('Ctrl Pts',(1.14824159036326,0.744664307084841,6.14673745338958));
#6402=CARTESIAN_POINT('Ctrl Pts',(1.19630848763014,0.659542186703067,6.14010820120531));
#6403=CARTESIAN_POINT('Ctrl Pts',(1.20296912258001,0.647313792807427,6.13915503519501));
#6404=CARTESIAN_POINT('Ctrl Pts',(1.21303789253717,0.628136077809906,6.13765553426122));
#6405=CARTESIAN_POINT('Ctrl Pts',(1.21657606252696,0.621255613780105,6.13711663523172));
#6406=CARTESIAN_POINT('Ctrl Pts',(1.22311842145835,0.608262862044143,6.13609658311447));
#6407=CARTESIAN_POINT('Ctrl Pts',(1.22613563931947,0.602157593822545,6.1356162079459));
#6408=CARTESIAN_POINT('Ctrl Pts',(1.23335085452847,0.587278697820586,6.13444324049325));
#6409=CARTESIAN_POINT('Ctrl Pts',(1.23750097292051,0.578482434696092,6.13374793939764));
#6410=CARTESIAN_POINT('Ctrl Pts',(1.25254815887428,0.545686568089057,6.13115070926833));
#6411=CARTESIAN_POINT('Ctrl Pts',(1.26284316913252,0.521418869291389,6.12921932471899));
#6412=CARTESIAN_POINT('Ctrl Pts',(1.28902359909137,0.454373766959362,6.12388468202372));
#6413=CARTESIAN_POINT('Ctrl Pts',(1.30347793977487,0.411074434611565,6.12044163577528));
#6414=CARTESIAN_POINT('Ctrl Pts',(1.34304350979749,0.269279620973568,6.10930789038274));
#6415=CARTESIAN_POINT('Ctrl Pts',(1.3593515329279,0.168664785083447,6.1016514097853));
#6416=CARTESIAN_POINT('Ctrl Pts',(1.36539363505839,0.0459182219369729,6.09280556149921));
#6417=CARTESIAN_POINT('Ctrl Pts',(1.36594307473127,0.0246549835607194,6.09128944628695));
#6418=CARTESIAN_POINT('Ctrl Pts',(1.36602798545492,-0.00959514265164508,
6.08887207555029));
#6419=CARTESIAN_POINT('Ctrl Pts',(1.36587511343861,-0.0225769547362636,
6.08796152522914));
#6420=CARTESIAN_POINT('Ctrl Pts',(1.36522392435435,-0.0475867251530467,
6.08621764183283));
#6421=CARTESIAN_POINT('Ctrl Pts',(1.36475163931352,-0.0596140849356033,
6.08538359696397));
#6422=CARTESIAN_POINT('Ctrl Pts',(1.36326944676234,-0.0878393676983431,
6.08343622962519));
#6423=CARTESIAN_POINT('Ctrl Pts',(1.36212971955882,-0.104028859829275,6.08232696011955));
#6424=CARTESIAN_POINT('Ctrl Pts',(1.35716597624842,-0.160222425983841,6.07849947578572));
#6425=CARTESIAN_POINT('Ctrl Pts',(1.35186551179989,-0.200077020791389,6.07582581843807));
#6426=CARTESIAN_POINT('Ctrl Pts',(1.33313060226053,-0.30521252492663,6.06881603736694));
#6427=CARTESIAN_POINT('Ctrl Pts',(1.3166663428574,-0.369840757963558,6.06455525745848));
#6428=CARTESIAN_POINT('Ctrl Pts',(1.2741352518087,-0.497091773021355,6.05592326830799));
#6429=CARTESIAN_POINT('Ctrl Pts',(1.24799574870182,-0.559486689925425,6.05156198322036));
#6430=CARTESIAN_POINT('Ctrl Pts',(1.21061009477214,-0.632929778636938,6.04598541681214));
#6431=CARTESIAN_POINT('Ctrl Pts',(1.20365216067483,-0.646063725657715,6.04496978901454));
#6432=CARTESIAN_POINT('Ctrl Pts',(1.19265225892561,-0.66603271850596,6.04339316741588));
#6433=CARTESIAN_POINT('Ctrl Pts',(1.18876243903611,-0.672950851425942,6.04284086889513));
#6434=CARTESIAN_POINT('Ctrl Pts',(1.1817862463817,-0.685108930773588,6.04185873120822));
#6435=CARTESIAN_POINT('Ctrl Pts',(1.17872481232108,-0.690362796339865,6.04143042701915));
#6436=CARTESIAN_POINT('Ctrl Pts',(1.17109456295627,-0.70325869912298,6.04036960701642));
#6437=CARTESIAN_POINT('Ctrl Pts',(1.16648603138621,-0.710876642511075,6.03973468844069));
#6438=CARTESIAN_POINT('Ctrl Pts',(1.15092238847172,-0.736044611485236,6.03761078878561));
#6439=CARTESIAN_POINT('Ctrl Pts',(1.13964360669512,-0.753389906973071,6.03610412269872));
#6440=CARTESIAN_POINT('Ctrl Pts',(1.06225131740906,-0.866692843627718,6.02600589851431));
#6441=CARTESIAN_POINT('Ctrl Pts',(0.984484890517809,-0.954110476343341,
6.01702115446776));
#6442=CARTESIAN_POINT('Ctrl Pts',(0.861468540129706,-1.0611273908183,6.00493010243138));
#6443=CARTESIAN_POINT('Ctrl Pts',(0.824837296202431,-1.08984571466828,6.00153588986857));
#6444=CARTESIAN_POINT('Ctrl Pts',(0.772591504234391,-1.1266591443182,5.99696893006937));
#6445=CARTESIAN_POINT('Ctrl Pts',(0.758184301068697,-1.13640445044443,5.99573621283639));
#6446=CARTESIAN_POINT('Ctrl Pts',(0.73343877328153,-1.15246263817196,5.9936625166208));
#6447=CARTESIAN_POINT('Ctrl Pts',(0.723195794720574,-1.15891778209984,5.99281643566034));
#6448=CARTESIAN_POINT('Ctrl Pts',(0.702135726468353,-1.17180190925377,5.99110105987824));
#6449=CARTESIAN_POINT('Ctrl Pts',(0.691312902544989,-1.17821932673476,5.99023223913466));
#6450=CARTESIAN_POINT('Ctrl Pts',(0.663699862792933,-1.19408104011411,5.98804632150419));
#6451=CARTESIAN_POINT('Ctrl Pts',(0.646795362803002,-1.20332159379481,5.98673640757605));
#6452=CARTESIAN_POINT('Ctrl Pts',(0.558138420305705,-1.24937605664431,5.98000058958578));
#6453=CARTESIAN_POINT('Ctrl Pts',(0.483421757123601,-1.28014242796536,5.97478416574482));
#6454=CARTESIAN_POINT('Ctrl Pts',(0.320980846549595,-1.33076517826726,5.96384058841696));
#6455=CARTESIAN_POINT('Ctrl Pts',(0.233144320857145,-1.34892698356517,5.95814464289484));
#6456=CARTESIAN_POINT('Ctrl Pts',(0.130774740134236,-1.35979249242472,5.95115331696106));
#6457=CARTESIAN_POINT('Ctrl Pts',(0.117352384735143,-1.36101654605131,5.95022954192214));
#6458=CARTESIAN_POINT('Ctrl Pts',(0.0963719359629294,-1.36261721525101,
5.94877145333579));
#6459=CARTESIAN_POINT('Ctrl Pts',(0.0888246926803422,-1.36312999832691,
5.94824408864919));
#6460=CARTESIAN_POINT('Ctrl Pts',(0.0744100192719718,-1.3639891597929,5.94723075704724));
#6461=CARTESIAN_POINT('Ctrl Pts',(0.0675436133213621,-1.36434641151483,
5.94674536234453));
#6462=CARTESIAN_POINT('Ctrl Pts',(0.0505577907766123,-1.36510163403285,
5.9455383247655));
#6463=CARTESIAN_POINT('Ctrl Pts',(0.0404362169862525,-1.36543892506649,
5.94481358244947));
#6464=CARTESIAN_POINT('Ctrl Pts',(0.000681321907970434,-1.36632132337396,
5.9419477857565));
#6465=CARTESIAN_POINT('Ctrl Pts',(-0.0289607774440487,-1.36601442383707,
5.93976924873405));
#6466=CARTESIAN_POINT('Ctrl Pts',(-0.114282003861064,-1.36235293538809,
5.93341836936025));
#6467=CARTESIAN_POINT('Ctrl Pts',(-0.169796274916512,-1.35655248938338,
5.92918954302956));
#6468=CARTESIAN_POINT('Ctrl Pts',(-0.308709648445458,-1.3333759661935,5.91854150290063));
#6469=CARTESIAN_POINT('Ctrl Pts',(-0.391141898439683,-1.31156601464212,
5.91217251747732));
#6470=CARTESIAN_POINT('Ctrl Pts',(-0.49206495959233,-1.27449235482162,5.90441887640844));
#6471=CARTESIAN_POINT('Ctrl Pts',(-0.512918083284765,-1.26624398588903,
5.90281812290129));
#6472=CARTESIAN_POINT('Ctrl Pts',(-0.545725724285701,-1.2523234765058,5.90030034868819));
#6473=CARTESIAN_POINT('Ctrl Pts',(-0.557816427376738,-1.2469849682473,5.89937258813855));
#6474=CARTESIAN_POINT('Ctrl Pts',(-0.58070321766845,-1.23648006713151,5.89761594750999));
#6475=CARTESIAN_POINT('Ctrl Pts',(-0.591512530231947,-1.23134565652511,
5.89678609450838));
#6476=CARTESIAN_POINT('Ctrl Pts',(-0.616350975457051,-1.21914485348429,
5.89487789614863));
#6477=CARTESIAN_POINT('Ctrl Pts',(-0.630328644966801,-1.21197711707044,
5.89380310398349));
#6478=CARTESIAN_POINT('Ctrl Pts',(-0.676364210674887,-1.18735820471018,
5.89025659022246));
#6479=CARTESIAN_POINT('Ctrl Pts',(-0.707847527346664,-1.16886281874683,
5.88782068480353));
#6480=CARTESIAN_POINT('Ctrl Pts',(-0.786044769648155,-1.11860474209448,
5.88169728982519));
#6481=CARTESIAN_POINT('Ctrl Pts',(-0.831599416638986,-1.08516631497758,
5.87806114292099));
#6482=CARTESIAN_POINT('Ctrl Pts',(-0.939825610390796,-0.994896710889066,
5.86900051111617));
#6483=CARTESIAN_POINT('Ctrl Pts',(-0.999528290433561,-0.934896299024387,
5.86360740352212));
#6484=CARTESIAN_POINT('Ctrl Pts',(-1.06213219289128,-0.859082987100705,
5.85693898454604));
#6485=CARTESIAN_POINT('Ctrl Pts',(-1.07079979400966,-0.848254760128754,
5.85598946138802));
#6486=CARTESIAN_POINT('Ctrl Pts',(-1.08403605887532,-0.831192822520132,
5.85449443661436));
#6487=CARTESIAN_POINT('Ctrl Pts',(-1.08871950066444,-0.825048802582859,
5.85395629900024));
#6488=CARTESIAN_POINT('Ctrl Pts',(-1.09743583884147,-0.81341073603355,5.85293666768306));
#6489=CARTESIAN_POINT('Ctrl Pts',(-1.10148012134357,-0.807925726583716,
5.85245593781119));
#6490=CARTESIAN_POINT('Ctrl Pts',(-1.11121229182865,-0.794517695498988,
5.85128066071818));
#6491=CARTESIAN_POINT('Ctrl Pts',(-1.11685660277803,-0.786563691411526,
5.85058337908918));
#6492=CARTESIAN_POINT('Ctrl Pts',(-1.13755359943611,-0.756725384917957,
5.84796933254502));
#6493=CARTESIAN_POINT('Ctrl Pts',(-1.15205123712983,-0.734465267145847,
5.84602264320846));
#6494=CARTESIAN_POINT('Ctrl Pts',(-1.20296072227006,-0.651078132416014,
5.83877983945842));
#6495=CARTESIAN_POINT('Ctrl Pts',(-1.23523019366588,-0.587556792199495,
5.83336380620333));
#6496=CARTESIAN_POINT('Ctrl Pts',(-1.2904223139448,-0.454032510265899,5.82246364282492));
#6497=CARTESIAN_POINT('Ctrl Pts',(-1.31293869255956,-0.38409650211287,5.81700142079563));
#6498=CARTESIAN_POINT('Ctrl Pts',(-1.33489839526453,-0.29070904672298,5.81008138536126));
#6499=CARTESIAN_POINT('Ctrl Pts',(-1.33951995424586,-0.268611010201654,
5.80846955967288));
#6500=CARTESIAN_POINT('Ctrl Pts',(-1.34598137816927,-0.233378634483755,
5.80593868475107));
#6501=CARTESIAN_POINT('Ctrl Pts',(-1.34818121501188,-0.220315434738023,
5.80500870020211));
#6502=CARTESIAN_POINT('Ctrl Pts',(-1.35194437230554,-0.195795919405125,
5.80327812258695));
#6503=CARTESIAN_POINT('Ctrl Pts',(-1.35355292069266,-0.184347858791772,
5.80247620477624));
#6504=CARTESIAN_POINT('Ctrl Pts',(-1.35648370817036,-0.161376701461312,
5.8008786273071));
#6505=CARTESIAN_POINT('Ctrl Pts',(-1.35780490106219,-0.149854445707179,
5.8000830625301));
#6506=CARTESIAN_POINT('Ctrl Pts',(-1.36095380321471,-0.118916025686271,
5.79796127990866));
#6507=CARTESIAN_POINT('Ctrl Pts',(-1.36251278902884,-0.0994748039951829,
5.7966431664332));
#6508=CARTESIAN_POINT('Ctrl Pts',(-1.36523487203515,-0.0530785383892744,
5.79352797295233));
#6509=CARTESIAN_POINT('Ctrl Pts',(-1.36601683429475,-0.0261093149545231,
5.79174167536384));
#6510=CARTESIAN_POINT('Ctrl Pts',(-1.36599972525692,0.00086637060349483,
5.78997137255369));
#6511=CARTESIAN_POINT('Origin',(0.,0.,3.44061240069463));
#6512=CARTESIAN_POINT('',(-1.70824949798349,0.00130963321928915,0.193190200199919));
#6513=CARTESIAN_POINT('',(0.747616516620363,1.53872147257634,4.34771760247897E-5));
#6514=CARTESIAN_POINT('Ctrl Pts',(-1.70971129366951,0.00131075390815409,
0.193190200199919));
#6515=CARTESIAN_POINT('Ctrl Pts',(-1.7103415218327,0.0801238654015101,0.188773164585797));
#6516=CARTESIAN_POINT('Ctrl Pts',(-1.66983493919842,0.719618324757823,0.152894693722701));
#6517=CARTESIAN_POINT('Ctrl Pts',(-0.899480193612338,1.76907630764895,0.0885124527147331));
#6518=CARTESIAN_POINT('Ctrl Pts',(0.28909851215658,1.75784256997736,0.0285472473208922));
#6519=CARTESIAN_POINT('Ctrl Pts',(0.747616516620363,1.53872147257634,4.34771760247897E-5));
#6520=CARTESIAN_POINT('',(-0.746545333137425,1.53648564199954,0.));
#6521=CARTESIAN_POINT('Origin',(0.,0.,0.));
#6522=CARTESIAN_POINT('',(-1.70829001772743,0.00184159784217005,0.106809799800075));
#6523=CARTESIAN_POINT('Ctrl Pts',(-0.746545333137426,1.53648564199954,6.93889390390723E-16));
#6524=CARTESIAN_POINT('Ctrl Pts',(-1.25276108530162,1.2905262935952,0.0314614352489755));
#6525=CARTESIAN_POINT('Ctrl Pts',(-1.67270494886694,0.709596610538724,0.0670647018490002));
#6526=CARTESIAN_POINT('Ctrl Pts',(-1.71019420630271,0.0756867134818199,
0.102667968449025));
#6527=CARTESIAN_POINT('Ctrl Pts',(-1.70960986444288,0.00184302068421545,
0.106809799800075));
#6528=CARTESIAN_POINT('',(-1.70824999635299,0.000111624363083944,0.70680979975714));
#6529=CARTESIAN_POINT('Ctrl Pts',(-1.70824900736989,0.00184155363153534,
0.106809799800075));
#6530=CARTESIAN_POINT('Ctrl Pts',(-1.70831458995836,-0.0589937051053382,
0.110224750287315));
#6531=CARTESIAN_POINT('Ctrl Pts',(-1.70512614389993,-0.119972079441817,
0.113639700774556));
#6532=CARTESIAN_POINT('Ctrl Pts',(-1.69866513901472,-0.180706413821171,
0.117054651261796));
#6533=CARTESIAN_POINT('Ctrl Pts',(-1.69225479648065,-0.240964515133158,
0.120442824270333));
#6534=CARTESIAN_POINT('Ctrl Pts',(-1.68262305022738,-0.300981850843056,
0.123830997278869));
#6535=CARTESIAN_POINT('Ctrl Pts',(-1.66980391133269,-0.360378911977436,
0.127219170287406));
#6536=CARTESIAN_POINT('Ctrl Pts',(-1.65699495703225,-0.419728783127227,
0.130604651448416));
#6537=CARTESIAN_POINT('Ctrl Pts',(-1.64100373423955,-0.478458836454786,
0.133990132609428));
#6538=CARTESIAN_POINT('Ctrl Pts',(-1.621915776411,-0.536197050280131,0.137375613770439));
#6539=CARTESIAN_POINT('Ctrl Pts',(-1.60283531726547,-0.593912581712318,
0.140759764948937));
#6540=CARTESIAN_POINT('Ctrl Pts',(-1.58066070057341,-0.650636540481587,
0.144143916127434));
#6541=CARTESIAN_POINT('Ctrl Pts',(-1.55552739778889,-0.706011740148935,
0.147528067305932));
#6542=CARTESIAN_POINT('Ctrl Pts',(-1.53000373790585,-0.762246997981248,
0.150964779321592));
#6543=CARTESIAN_POINT('Ctrl Pts',(-1.50142888312398,-0.81709070658417,0.154401491337252));
#6544=CARTESIAN_POINT('Ctrl Pts',(-1.46999459697372,-0.870191902610033,
0.157838203352912));
#6545=CARTESIAN_POINT('Ctrl Pts',(-1.43900897726615,-0.922535177027307,
0.161225862644827));
#6546=CARTESIAN_POINT('Ctrl Pts',(-1.40524538544557,-0.973184946985413,
0.164613521936742));
#6547=CARTESIAN_POINT('Ctrl Pts',(-1.36893126062472,-1.02183426551687,0.168001181228657));
#6548=CARTESIAN_POINT('Ctrl Pts',(-1.33182840238382,-1.07154023469262,0.171462419606189));
#6549=CARTESIAN_POINT('Ctrl Pts',(-1.29206326804371,-1.11915736418746,0.174923657983722));
#6550=CARTESIAN_POINT('Ctrl Pts',(-1.24991976686571,-1.16439625510321,0.178384896361254));
#6551=CARTESIAN_POINT('Ctrl Pts',(-1.2077762656877,-1.20963514601895,0.181846134738786));
#6552=CARTESIAN_POINT('Ctrl Pts',(-1.1632548734801,-1.25249545114912,0.185307373116318));
#6553=CARTESIAN_POINT('Ctrl Pts',(-1.11667462808752,-1.29273192792845,0.18876861149385));
#6554=CARTESIAN_POINT('Ctrl Pts',(-1.06980461621609,-1.33321870785881,0.192251381549643));
#6555=CARTESIAN_POINT('Ctrl Pts',(-1.02063842807767,-1.37123223284083,0.195734151605436));
#6556=CARTESIAN_POINT('Ctrl Pts',(-0.969466967790923,-1.40650341658393,
0.199216921661229));
#6557=CARTESIAN_POINT('Ctrl Pts',(-0.918081535653809,-1.44192208567155,
0.202714254810377));
#6558=CARTESIAN_POINT('Ctrl Pts',(-0.864674369909386,-1.47457504324174,
0.206211587959525));
#6559=CARTESIAN_POINT('Ctrl Pts',(-0.809575461633486,-1.50422924929046,
0.209708921108673));
#6560=CARTESIAN_POINT('Ctrl Pts',(-0.754852679879619,-1.53368102422513,
0.213182380105048));
#6561=CARTESIAN_POINT('Ctrl Pts',(-0.698461622166891,-1.56017460403329,
0.216655839101424));
#6562=CARTESIAN_POINT('Ctrl Pts',(-0.640754405190757,-1.58352513549,0.220129298097799));
#6563=CARTESIAN_POINT('Ctrl Pts',(-0.583081702786774,-1.60686170104011,
0.22360067962523));
#6564=CARTESIAN_POINT('Ctrl Pts',(-0.524094870000844,-1.6270587575761,0.227072061152661));
#6565=CARTESIAN_POINT('Ctrl Pts',(-0.464167575172626,-1.64397886989413,
0.230543442680092));
#6566=CARTESIAN_POINT('Ctrl Pts',(-0.404254501418413,-1.66089496697719,
0.234014000429747));
#6567=CARTESIAN_POINT('Ctrl Pts',(-0.343401894943893,-1.67453552683196,
0.237484558179402));
#6568=CARTESIAN_POINT('Ctrl Pts',(-0.281998295476573,-1.6848130530858,0.240955115929057));
#6569=CARTESIAN_POINT('Ctrl Pts',(-0.219782145675592,-1.69522658125907,
0.244471599371701));
#6570=CARTESIAN_POINT('Ctrl Pts',(-0.157000829752451,-1.70218728839646,
0.247988082814344));
#6571=CARTESIAN_POINT('Ctrl Pts',(-0.0940666075405792,-1.70565809465022,
0.251504566256987));
#6572=CARTESIAN_POINT('Ctrl Pts',(-0.0318790834905831,-1.70908772069138,
0.254979327539086));
#6573=CARTESIAN_POINT('Ctrl Pts',(0.0304572233450804,-1.7091098811712,0.258454088821184));
#6574=CARTESIAN_POINT('Ctrl Pts',(0.0925444116386326,-1.70574136209874,
0.261928850103282));
#6575=CARTESIAN_POINT('Ctrl Pts',(0.155749840047458,-1.70231217329296,0.265466194626198));
#6576=CARTESIAN_POINT('Ctrl Pts',(0.218696542192045,-1.69536899906895,0.269003539149113));
#6577=CARTESIAN_POINT('Ctrl Pts',(0.280972685895826,-1.6849843952632,0.272540883672029));
#6578=CARTESIAN_POINT('Ctrl Pts',(0.343248829599607,-1.67459979145744,0.276078228194944));
#6579=CARTESIAN_POINT('Ctrl Pts',(0.404853895881334,-1.6607739382837,0.27961557271786));
#6580=CARTESIAN_POINT('Ctrl Pts',(0.465392026083252,-1.64363266107672,0.283152917240776));
#6581=CARTESIAN_POINT('Ctrl Pts',(0.524997251490571,-1.62675553440822,0.286635750571249));
#6582=CARTESIAN_POINT('Ctrl Pts',(0.583797434628291,-1.6065996069445,0.290118583901722));
#6583=CARTESIAN_POINT('Ctrl Pts',(0.641407914169682,-1.58326054398526,0.293601417232194));
#6584=CARTESIAN_POINT('Ctrl Pts',(0.699258108267395,-1.55982436825822,0.297098742472007));
#6585=CARTESIAN_POINT('Ctrl Pts',(0.755908164860664,-1.53317858765772,0.30059606771182));
#6586=CARTESIAN_POINT('Ctrl Pts',(0.810982201756074,-1.50347129368501,0.304093392951633));
#6587=CARTESIAN_POINT('Ctrl Pts',(0.865685923739254,-1.47396374998629,0.307567202361443));
#6588=CARTESIAN_POINT('Ctrl Pts',(0.918834298152729,-1.44143596599254,0.311041011771252));
#6589=CARTESIAN_POINT('Ctrl Pts',(0.970079538891547,-1.4060809901012,0.314514821181061));
#6590=CARTESIAN_POINT('Ctrl Pts',(1.02129571686976,-1.37074606510992,0.317986660486139));
#6591=CARTESIAN_POINT('Ctrl Pts',(1.07061048676336,-1.33258741489734,0.321458499791217));
#6592=CARTESIAN_POINT('Ctrl Pts',(1.11770390797386,-1.29184210977966,0.324930339096295));
#6593=CARTESIAN_POINT('Ctrl Pts',(1.16478760702395,-1.25110521629108,0.328401461660524));
#6594=CARTESIAN_POINT('Ctrl Pts',(1.20965048620019,-1.20778305899605,0.331872584224754));
#6595=CARTESIAN_POINT('Ctrl Pts',(1.25200621942742,-1.16215252398946,0.335343706788983));
#6596=CARTESIAN_POINT('Ctrl Pts',(1.29491110305326,-1.11593038013611,0.338859833138876));
#6597=CARTESIAN_POINT('Ctrl Pts',(1.33524297221629,-1.06733993260901,0.34237595948877));
#6598=CARTESIAN_POINT('Ctrl Pts',(1.37274487765719,-1.01670524901072,0.345892085838663));
#6599=CARTESIAN_POINT('Ctrl Pts',(1.40981438688767,-0.966654382289095,0.349367671322935));
#6600=CARTESIAN_POINT('Ctrl Pts',(1.44411862471989,-0.914606640349092,0.352843256807207));
#6601=CARTESIAN_POINT('Ctrl Pts',(1.47545332507607,-0.860903913350356,0.356318842291478));
#6602=CARTESIAN_POINT('Ctrl Pts',(1.50733627948133,-0.806261565509918,0.359855239074182));
#6603=CARTESIAN_POINT('Ctrl Pts',(1.5361445182402,-0.749906239244957,0.363391635856886));
#6604=CARTESIAN_POINT('Ctrl Pts',(1.56171302119027,-0.692221425516987,0.36692803263959));
#6605=CARTESIAN_POINT('Ctrl Pts',(1.58728152414033,-0.634536611789017,0.370464429422294));
#6606=CARTESIAN_POINT('Ctrl Pts',(1.60961015864768,-0.575522842169992,0.374000826204998));
#6607=CARTESIAN_POINT('Ctrl Pts',(1.6285871045859,-0.515579387947677,0.377537222987702));
#6608=CARTESIAN_POINT('Ctrl Pts',(1.64722044712831,-0.45672129142701,0.381009588500704));
#6609=CARTESIAN_POINT('Ctrl Pts',(1.6626970729652,-0.39673127692693,0.384481954013706));
#6610=CARTESIAN_POINT('Ctrl Pts',(1.6748836768792,-0.335980254514478,0.387954319526707));
#6611=CARTESIAN_POINT('Ctrl Pts',(1.68716247160561,-0.274769654835853,0.391452953243704));
#6612=CARTESIAN_POINT('Ctrl Pts',(1.69610102240621,-0.212786956690893,0.394951586960701));
#6613=CARTESIAN_POINT('Ctrl Pts',(1.70161369856505,-0.150428997722399,0.398450220677697));
#6614=CARTESIAN_POINT('Ctrl Pts',(1.70707003818485,-0.088708303031531,0.401913100269235));
#6615=CARTESIAN_POINT('Ctrl Pts',(1.70917014433344,-0.026620498361166,0.405375979860772));
#6616=CARTESIAN_POINT('Ctrl Pts',(1.70788233348107,0.0354400547864655,0.408838859452309));
#6617=CARTESIAN_POINT('Ctrl Pts',(1.70659530809443,0.0974627557620102,0.412299626953194));
#6618=CARTESIAN_POINT('Ctrl Pts',(1.70192447367992,0.15945773039416,0.415760394454078));
#6619=CARTESIAN_POINT('Ctrl Pts',(1.6938902172817,0.221029396907651,0.419221161954963));
#6620=CARTESIAN_POINT('Ctrl Pts',(1.68585791093812,0.282586118900111,0.422681089467008));
#6621=CARTESIAN_POINT('Ctrl Pts',(1.67446386916949,0.343719232323013,0.426141016979053));
#6622=CARTESIAN_POINT('Ctrl Pts',(1.6597802429042,0.404039116627186,0.429600944491098));
#6623=CARTESIAN_POINT('Ctrl Pts',(1.64481317494788,0.465523370665447,0.433127659844726));
#6624=CARTESIAN_POINT('Ctrl Pts',(1.62642826834427,0.52616212671388,0.436654375198354));
#6625=CARTESIAN_POINT('Ctrl Pts',(1.60475580541016,0.58555688664927,0.440181090551981));
#6626=CARTESIAN_POINT('Ctrl Pts',(1.58346741409825,0.643899073932092,0.443645306719844));
#6627=CARTESIAN_POINT('Ctrl Pts',(1.55900731654214,0.701040549287598,0.447109522887707));
#6628=CARTESIAN_POINT('Ctrl Pts',(1.53154746996109,0.756624351812561,0.45057373905557));
#6629=CARTESIAN_POINT('Ctrl Pts',(1.50334450373795,0.813712365780093,0.45413170400208));
#6630=CARTESIAN_POINT('Ctrl Pts',(1.47197732711775,0.869156660332305,0.457689668948589));
#6631=CARTESIAN_POINT('Ctrl Pts',(1.43768090094917,0.922600503764211,0.461247633895098));
#6632=CARTESIAN_POINT('Ctrl Pts',(1.4033844747806,0.976044347196117,0.464805598841607));
#6633=CARTESIAN_POINT('Ctrl Pts',(1.36615919110336,1.02748731456081,0.468363563788117));
#6634=CARTESIAN_POINT('Ctrl Pts',(1.32628400933715,1.07660985926964,0.471921528734626));
#6635=CARTESIAN_POINT('Ctrl Pts',(1.2873024587237,1.12463153285235,0.475399757158923));
#6636=CARTESIAN_POINT('Ctrl Pts',(1.24563210246975,1.17062859785337,0.47887798558322));
#6637=CARTESIAN_POINT('Ctrl Pts',(1.20151108135262,1.21428546227271,0.482356214007517));
#6638=CARTESIAN_POINT('Ctrl Pts',(1.15714051720953,1.25818924450528,0.485854114860602));
#6639=CARTESIAN_POINT('Ctrl Pts',(1.1102917499648,1.2997258249965,0.489352015713686));
#6640=CARTESIAN_POINT('Ctrl Pts',(1.06124904461688,1.3386069355116,0.492849916566771));
#6641=CARTESIAN_POINT('Ctrl Pts',(1.01261269947674,1.3771658832089,0.496318834358923));
#6642=CARTESIAN_POINT('Ctrl Pts',(0.961819031833934,1.41311287122005,0.499787752151075));
#6643=CARTESIAN_POINT('Ctrl Pts',(0.909181379826556,1.44620443958545,0.503256669943226));
#6644=CARTESIAN_POINT('Ctrl Pts',(0.856575039118757,1.47927632356201,0.506723524263318));
#6645=CARTESIAN_POINT('Ctrl Pts',(0.802127317729894,1.50949588715465,0.510190378583409));
#6646=CARTESIAN_POINT('Ctrl Pts',(0.746181120237089,1.53666255186418,0.513657232903501));
#6647=CARTESIAN_POINT('Ctrl Pts',(0.690247857302824,1.56382293573907,0.517123285699412));
#6648=CARTESIAN_POINT('Ctrl Pts',(0.632817262007056,1.58793160091938,0.520589338495322));
#6649=CARTESIAN_POINT('Ctrl Pts',(0.57425565462772,1.6088345177886,0.524055391291232));
#6650=CARTESIAN_POINT('Ctrl Pts',(0.514767864255296,1.63006802541475,0.527576261557092));
#6651=CARTESIAN_POINT('Ctrl Pts',(0.454113466530574,1.64799327853745,0.531097131822953));
#6652=CARTESIAN_POINT('Ctrl Pts',(0.392693999809817,1.66250097293607,0.534618002088813));
#6653=CARTESIAN_POINT('Ctrl Pts',(0.332155549922089,1.67680056518636,0.538088368074243));
#6654=CARTESIAN_POINT('Ctrl Pts',(0.270874358340689,1.68777998316324,0.541558734059672));
#6655=CARTESIAN_POINT('Ctrl Pts',(0.209244251076581,1.69538635888443,0.545029100045102));
#6656=CARTESIAN_POINT('Ctrl Pts',(0.146268788207356,1.70315877812988,0.548575222451177));
#6657=CARTESIAN_POINT('Ctrl Pts',(0.0829295507635524,1.70740908443476,0.552121344857253));
#6658=CARTESIAN_POINT('Ctrl Pts',(0.0196484347567886,1.70813699729021,0.555667467263328));
#6659=CARTESIAN_POINT('Ctrl Pts',(-0.0436326812499752,1.70886491014566,
0.559213589669403));
#6660=CARTESIAN_POINT('Ctrl Pts',(-0.106855121658145,1.70607051955128,0.562759712075477));
#6661=CARTESIAN_POINT('Ctrl Pts',(-0.169603612446375,1.69980960026267,0.566305834481553));
#6662=CARTESIAN_POINT('Ctrl Pts',(-0.231141829633215,1.69366943966069,0.56978356036874));
#6663=CARTESIAN_POINT('Ctrl Pts',(-0.292468277930089,1.68417100072598,0.573261286255928));
#6664=CARTESIAN_POINT('Ctrl Pts',(-0.353188497672923,1.67133956681805,0.576739012143115));
#6665=CARTESIAN_POINT('Ctrl Pts',(-0.414262064020097,1.65843346348995,0.580236975813338));
#6666=CARTESIAN_POINT('Ctrl Pts',(-0.474721801697741,1.64215542820075,0.583734939483562));
#6667=CARTESIAN_POINT('Ctrl Pts',(-0.534170512454316,1.62258433559686,0.587232903153786));
#6668=CARTESIAN_POINT('Ctrl Pts',(-0.59311744304232,1.60317843389485,0.590701342065982));
#6669=CARTESIAN_POINT('Ctrl Pts',(-0.651069855630353,1.580535001617,0.594169780978179));
#6670=CARTESIAN_POINT('Ctrl Pts',(-0.707652173206536,1.55478180599596,0.597638219890375));
#6671=CARTESIAN_POINT('Ctrl Pts',(-0.76420099665976,1.52904385507923,0.601104605646668));
#6672=CARTESIAN_POINT('Ctrl Pts',(-0.819380872878149,1.50020000119686,0.60457099140296));
#6673=CARTESIAN_POINT('Ctrl Pts',(-0.872835779942873,1.46842628815733,0.608037377159252));
#6674=CARTESIAN_POINT('Ctrl Pts',(-0.926278498929028,1.43665981973822,0.611502972556263));
#6675=CARTESIAN_POINT('Ctrl Pts',(-0.977996594013848,1.40196507765051,0.614968567953273));
#6676=CARTESIAN_POINT('Ctrl Pts',(-1.02766004585383,1.36456326077456,0.618434163350284));
#6677=CARTESIAN_POINT('Ctrl Pts',(-1.07812221834835,1.32655992301053,0.6219554947568));
#6678=CARTESIAN_POINT('Ctrl Pts',(-1.1264626182537,1.28576195469007,0.625476826163317));
#6679=CARTESIAN_POINT('Ctrl Pts',(-1.17236898279256,1.24244477973306,0.628998157569833));
#6680=CARTESIAN_POINT('Ctrl Pts',(-1.21760539790529,1.1997597680239,0.632468099283903));
#6681=CARTESIAN_POINT('Ctrl Pts',(-1.26047804564556,1.15462901610646,0.635938040997972));
#6682=CARTESIAN_POINT('Ctrl Pts',(-1.3007262878688,1.10735233171157,0.639407982712041));
#6683=CARTESIAN_POINT('Ctrl Pts',(-1.34186864228173,1.05902539872268,0.642955008964781));
#6684=CARTESIAN_POINT('Ctrl Pts',(-1.38026822661701,1.00845647137167,0.64650203521752));
#6685=CARTESIAN_POINT('Ctrl Pts',(-1.4156926497375,0.955998108773865,0.65004906147026));
#6686=CARTESIAN_POINT('Ctrl Pts',(-1.451117072858,0.903539746176061,0.653596087722999));
#6687=CARTESIAN_POINT('Ctrl Pts',(-1.48356610494929,0.849192461909207,0.657143113975739));
#6688=CARTESIAN_POINT('Ctrl Pts',(-1.51285789915611,0.793334128511411,0.660690140228478));
#6689=CARTESIAN_POINT('Ctrl Pts',(-1.54459640063931,0.73281001773563,0.6645334451892));
#6690=CARTESIAN_POINT('Ctrl Pts',(-1.5727487797283,0.670282551675062,0.668376750149923));
#6691=CARTESIAN_POINT('Ctrl Pts',(-1.59707520162033,0.606192100632624,0.672220055110644));
#6692=CARTESIAN_POINT('Ctrl Pts',(-1.62023120184969,0.545185245385863,0.675878446424705));
#6693=CARTESIAN_POINT('Ctrl Pts',(-1.63992068276636,0.482762784725111,0.679536837738766));
#6694=CARTESIAN_POINT('Ctrl Pts',(-1.65598315357621,0.419330248815646,0.683195229052827));
#6695=CARTESIAN_POINT('Ctrl Pts',(-1.67201517077544,0.356017977700565,0.686846684246917));
#6696=CARTESIAN_POINT('Ctrl Pts',(-1.68443374424877,0.291699846434291,0.690498139441006));
#6697=CARTESIAN_POINT('Ctrl Pts',(-1.69312744441239,0.226798411541141,0.694149594635095));
#6698=CARTESIAN_POINT('Ctrl Pts',(-1.70180113708534,0.162046339385127,0.697792646450381));
#6699=CARTESIAN_POINT('Ctrl Pts',(-1.70676696174966,0.0967140536837641,
0.701435698265668));
#6700=CARTESIAN_POINT('Ctrl Pts',(-1.70796442270991,0.0312344882654268,
0.705078750080954));
#6701=CARTESIAN_POINT('Ctrl Pts',(-1.70815408644173,0.0208632952600976,
0.705655766639683));
#6702=CARTESIAN_POINT('Ctrl Pts',(-1.7082493182883,0.0104884272114703,0.706232783198412));
#6703=CARTESIAN_POINT('Ctrl Pts',(-1.70824999635299,0.000111624363083394,
0.70680979975714));
#6704=CARTESIAN_POINT('',(-1.70824952897253,-0.00126856813606742,1.30680979980007));
#6705=CARTESIAN_POINT('Ctrl Pts',(-1.70824999635304,0.000111623590999127,
0.706809799800073));
#6706=CARTESIAN_POINT('Ctrl Pts',(-1.70825423774439,-0.0647972069556505,
0.710419145624602));
#6707=CARTESIAN_POINT('Ctrl Pts',(-1.70455463276262,-0.129644182097538,
0.714028491449132));
#6708=CARTESIAN_POINT('Ctrl Pts',(-1.69719806951645,-0.194001998261928,
0.717637837273661));
#6709=CARTESIAN_POINT('Ctrl Pts',(-1.68982284212325,-0.258523094983278,
0.721256340276473));
#6710=CARTESIAN_POINT('Ctrl Pts',(-1.67877217615949,-0.3225521131443,0.724874843279286));
#6711=CARTESIAN_POINT('Ctrl Pts',(-1.66414446627173,-0.385669881993904,
0.728493346282097));
#6712=CARTESIAN_POINT('Ctrl Pts',(-1.64949678221494,-0.448873838291371,
0.73211679035847));
#6713=CARTESIAN_POINT('Ctrl Pts',(-1.63126244491383,-0.511163641249322,
0.735740234434843));
#6714=CARTESIAN_POINT('Ctrl Pts',(-1.60958946394413,-0.572136190133131,
0.739363678511216));
#6715=CARTESIAN_POINT('Ctrl Pts',(-1.5878610510406,-0.63326468555238,0.742996390095023));
#6716=CARTESIAN_POINT('Ctrl Pts',(-1.56267659384783,-0.693068787128632,
0.746629101678831));
#6717=CARTESIAN_POINT('Ctrl Pts',(-1.53423184058334,-0.751166241147904,
0.750261813262638));
#6718=CARTESIAN_POINT('Ctrl Pts',(-1.52167059471973,-0.776822164305316,
0.751866024166894));
#6719=CARTESIAN_POINT('Ctrl Pts',(-1.50847414164659,-0.802145619181886,
0.753470235071149));
#6720=CARTESIAN_POINT('Ctrl Pts',(-1.49466204101235,-0.827105462233683,
0.755074445975405));
#6721=CARTESIAN_POINT('Ctrl Pts',(-1.4647228023275,-0.881208651781241,0.758551748554876));
#6722=CARTESIAN_POINT('Ctrl Pts',(-1.43178256343332,-0.933791892404183,
0.762029051134347));
#6723=CARTESIAN_POINT('Ctrl Pts',(-1.39602016698291,-0.98450279627688,0.765506353713818));
#6724=CARTESIAN_POINT('Ctrl Pts',(-1.36004473689107,-1.03551578081488,0.769004370297506));
#6725=CARTESIAN_POINT('Ctrl Pts',(-1.32121360177983,-1.08463355996619,0.772502386881194));
#6726=CARTESIAN_POINT('Ctrl Pts',(-1.27975602779576,-1.13152223655588,0.776000403464882));
#6727=CARTESIAN_POINT('Ctrl Pts',(-1.23865440931033,-1.17800832609929,0.779468386013347));
#6728=CARTESIAN_POINT('Ctrl Pts',(-1.19497160965764,-1.22230304805398,0.782936368561813));
#6729=CARTESIAN_POINT('Ctrl Pts',(-1.14897319366195,-1.26411180785018,0.786404351110279));
#6730=CARTESIAN_POINT('Ctrl Pts',(-1.10300215759204,-1.30589568155596,0.789870269389731));
#6731=CARTESIAN_POINT('Ctrl Pts',(-1.05471861327783,-1.34519618714438,0.793336187669184));
#6732=CARTESIAN_POINT('Ctrl Pts',(-1.0044247665779,-1.38175574932219,0.796802105948637));
#6733=CARTESIAN_POINT('Ctrl Pts',(-0.954142538812777,-1.41830686547335,
0.800267223528179));
#6734=CARTESIAN_POINT('Ctrl Pts',(-0.901851340961412,-1.45211799742215,
0.803732341107722));
#6735=CARTESIAN_POINT('Ctrl Pts',(-0.84788460589561,-1.48297328282921,0.807197458687265));
#6736=CARTESIAN_POINT('Ctrl Pts',(-0.79303548095234,-1.51433307145434,0.810719233106853));
#6737=CARTESIAN_POINT('Ctrl Pts',(-0.736455979813227,-1.54263917879348,
0.814241007526442));
#6738=CARTESIAN_POINT('Ctrl Pts',(-0.678522649743967,-1.56771332720125,
0.817762781946031));
#6739=CARTESIAN_POINT('Ctrl Pts',(-0.621450160103226,-1.59241489490921,
0.821232225767726));
#6740=CARTESIAN_POINT('Ctrl Pts',(-0.563064313702586,-1.61397979088082,
0.82470166958942));
#6741=CARTESIAN_POINT('Ctrl Pts',(-0.503743386284735,-1.63228694268942,
0.828171113411115));
#6742=CARTESIAN_POINT('Ctrl Pts',(-0.443080327494135,-1.65100829238497,
0.831719053129651));
#6743=CARTESIAN_POINT('Ctrl Pts',(-0.381439894359464,-1.66632251886815,
0.835266992848186));
#6744=CARTESIAN_POINT('Ctrl Pts',(-0.319238175549031,-1.67815525198717,
0.838814932566722));
#6745=CARTESIAN_POINT('Ctrl Pts',(-0.257036456738598,-1.6899879851062,0.842362872285257));
#6746=CARTESIAN_POINT('Ctrl Pts',(-0.194274016137331,-1.69833921645597,
0.845910812003793));
#6747=CARTESIAN_POINT('Ctrl Pts',(-0.131370246528373,-1.70319109932711,
0.849458751722329));
#6748=CARTESIAN_POINT('Ctrl Pts',(-0.0697216369706872,-1.7079461694064,
0.852935897079466));
#6749=CARTESIAN_POINT('Ctrl Pts',(-0.00769170042111965,-1.70935926745733,
0.856413042436603));
#6750=CARTESIAN_POINT('Ctrl Pts',(0.0543269327415997,-1.70738591035503,
0.85989018779374));
#6751=CARTESIAN_POINT('Ctrl Pts',(0.116718177241874,-1.70540069721542,0.86338822403022));
#6752=CARTESIAN_POINT('Ctrl Pts',(0.179097471754126,-1.69998808811252,0.8668862602667));
#6753=CARTESIAN_POINT('Ctrl Pts',(0.241059829430328,-1.69115588315655,0.87038429650318));
#6754=CARTESIAN_POINT('Ctrl Pts',(0.302487049652064,-1.68239995747489,0.873852121974972));
#6755=CARTESIAN_POINT('Ctrl Pts',(0.363503994625234,-1.67028333183075,0.877319947446765));
#6756=CARTESIAN_POINT('Ctrl Pts',(0.423718594525157,-1.6548657393135,0.880787772918557));
#6757=CARTESIAN_POINT('Ctrl Pts',(0.483897359799761,-1.63945732204033,0.884253534634605));
#6758=CARTESIAN_POINT('Ctrl Pts',(0.543274236444688,-1.62075195929602,0.887719296350653));
#6759=CARTESIAN_POINT('Ctrl Pts',(0.601467916059901,-1.59886034676283,0.891185058066701));
#6760=CARTESIAN_POINT('Ctrl Pts',(0.65964816428865,-1.5769737869211,0.894650019867959));
#6761=CARTESIAN_POINT('Ctrl Pts',(0.716645283123954,-1.55190261607231,0.898114981669217));
#6762=CARTESIAN_POINT('Ctrl Pts',(0.772095624091946,-1.52380655260373,0.901579943470475));
#6763=CARTESIAN_POINT('Ctrl Pts',(0.8284575749594,-1.49524858666266,0.90510186963704));
#6764=CARTESIAN_POINT('Ctrl Pts',(0.883220929047204,-1.46356557419215,0.908623795803605));
#6765=CARTESIAN_POINT('Ctrl Pts',(0.93602962127879,-1.42897397127753,0.91214572197017));
#6766=CARTESIAN_POINT('Ctrl Pts',(0.988049100236263,-1.39489933159452,0.915615013792584));
#6767=CARTESIAN_POINT('Ctrl Pts',(1.03817156964567,-1.35800281172865,0.919084305614998));
#6768=CARTESIAN_POINT('Ctrl Pts',(1.08608788274937,-1.31853372101171,0.922553597437411));
#6769=CARTESIAN_POINT('Ctrl Pts',(1.1350946390228,-1.27816642261559,0.926101840776052));
#6770=CARTESIAN_POINT('Ctrl Pts',(1.18179315984421,-1.23510838225422,0.929650084114692));
#6771=CARTESIAN_POINT('Ctrl Pts',(1.22589239731985,-1.18966629467821,0.933198327453333));
#6772=CARTESIAN_POINT('Ctrl Pts',(1.2699916347955,-1.1442242071022,0.936746570791974));
#6773=CARTESIAN_POINT('Ctrl Pts',(1.31149127156381,-1.09639853899546,0.940294814130615));
#6774=CARTESIAN_POINT('Ctrl Pts',(1.35014567385118,-1.04652984758245,0.943843057469255));
#6775=CARTESIAN_POINT('Ctrl Pts',(1.38802379743077,-0.997662646324197,0.9473200430574));
#6776=CARTESIAN_POINT('Ctrl Pts',(1.42332100809394,-0.946638894748168,0.950797028645544));
#6777=CARTESIAN_POINT('Ctrl Pts',(1.45578418587916,-0.893761974266163,0.954274014233688));
#6778=CARTESIAN_POINT('Ctrl Pts',(1.48844409133214,-0.840564618326074,0.957772070441292));
#6779=CARTESIAN_POINT('Ctrl Pts',(1.51823512427273,-0.785491921303965,0.961270126648896));
#6780=CARTESIAN_POINT('Ctrl Pts',(1.54494099487746,-0.728886400509045,0.9647681828565));
#6781=CARTESIAN_POINT('Ctrl Pts',(1.57141478631477,-0.672772792609696,0.968235840280845));
#6782=CARTESIAN_POINT('Ctrl Pts',(1.59485659445252,-0.615153358056696,0.971703497705189));
#6783=CARTESIAN_POINT('Ctrl Pts',(1.61510063895128,-0.556388343299131,0.975171155129534));
#6784=CARTESIAN_POINT('Ctrl Pts',(1.6353326199887,-0.497658346716116,0.978636746170785));
#6785=CARTESIAN_POINT('Ctrl Pts',(1.65237045144827,-0.437784602479932,0.982102337212036));
#6786=CARTESIAN_POINT('Ctrl Pts',(1.66609683140508,-0.377146405102794,0.985567928253287));
#6787=CARTESIAN_POINT('Ctrl Pts',(1.6798200338144,-0.316522244984715,0.989032717037852));
#6788=CARTESIAN_POINT('Ctrl Pts',(1.6902331948799,-0.255134477737986,0.992497505822418));
#6789=CARTESIAN_POINT('Ctrl Pts',(1.69726966623695,-0.193374617186187,0.995962294606983));
#6790=CARTESIAN_POINT('Ctrl Pts',(1.7044225059232,-0.130593379381629,0.99948438365775));
#6791=CARTESIAN_POINT('Ctrl Pts',(1.70808584899727,-0.0674281599390935,
1.00300647270852));
#6792=CARTESIAN_POINT('Ctrl Pts',(1.70824459941817,-0.00429546954982385,
1.00652856175928));
#6793=CARTESIAN_POINT('Ctrl Pts',(1.70840096215087,0.0578876726139587,1.00999767677413));
#6794=CARTESIAN_POINT('Ctrl Pts',(1.70515753144939,0.120038744033914,1.01346679178899));
#6795=CARTESIAN_POINT('Ctrl Pts',(1.69855246280966,0.181762464725931,1.01693590680384));
#6796=CARTESIAN_POINT('Ctrl Pts',(1.6917961032174,0.244899984578319,1.02048448287256));
#6797=CARTESIAN_POINT('Ctrl Pts',(1.68152226277215,0.307589775897309,1.02403305894129));
#6798=CARTESIAN_POINT('Ctrl Pts',(1.66782702210342,0.36941993292409,1.02758163501001));
#6799=CARTESIAN_POINT('Ctrl Pts',(1.65413178143469,0.43125008995087,1.03113021107874));
#6800=CARTESIAN_POINT('Ctrl Pts',(1.6370153559103,0.492220090517584,1.03467878714746));
#6801=CARTESIAN_POINT('Ctrl Pts',(1.61662711611434,0.551937342407481,1.03822736321618));
#6802=CARTESIAN_POINT('Ctrl Pts',(1.59664941728707,0.610452117836267,1.04170448457027));
#6803=CARTESIAN_POINT('Ctrl Pts',(1.57345085609657,0.667997458907379,1.04518160592435));
#6804=CARTESIAN_POINT('Ctrl Pts',(1.54714561072322,0.724195085401638,1.04865872727843));
#6805=CARTESIAN_POINT('Ctrl Pts',(1.52068211661961,0.780730789070622,1.05215676651529));
#6806=CARTESIAN_POINT('Ctrl Pts',(1.49107453233224,0.835901995143896,1.05565480575215));
#6807=CARTESIAN_POINT('Ctrl Pts',(1.45848995386028,0.889339708429038,1.05915284498901));
#6808=CARTESIAN_POINT('Ctrl Pts',(1.42618707608989,0.942315441169128,1.06262064292298));
#6809=CARTESIAN_POINT('Ctrl Pts',(1.39095873370873,0.993587090027181,1.06608844085695));
#6810=CARTESIAN_POINT('Ctrl Pts',(1.35301463007387,1.04281804419854,1.06955623879092));
#6811=CARTESIAN_POINT('Ctrl Pts',(1.31509312141691,1.09201968229138,1.07302197171847));
#6812=CARTESIAN_POINT('Ctrl Pts',(1.27445936771176,1.13918263458369,1.07648770464602));
#6813=CARTESIAN_POINT('Ctrl Pts',(1.23136564333278,1.18400030190859,1.07995343757357));
#6814=CARTESIAN_POINT('Ctrl Pts',(1.18828188026439,1.22880760942565,1.08341836938118));
#6815=CARTESIAN_POINT('Ctrl Pts',(1.14273962708848,1.27127034289864,1.08688330118878));
#6816=CARTESIAN_POINT('Ctrl Pts',(1.09502922272576,1.31111748667944,1.09034823299639));
#6817=CARTESIAN_POINT('Ctrl Pts',(1.04653366466733,1.35162038118424,1.09387018599361));
#6818=CARTESIAN_POINT('Ctrl Pts',(0.99579833416888,1.38942043990573,1.09739213899084));
#6819=CARTESIAN_POINT('Ctrl Pts',(0.94316271883561,1.42427600846838,1.10091409198807));
#6820=CARTESIAN_POINT('Ctrl Pts',(0.8913146129287,1.45861008433772,1.10438335117394));
#6821=CARTESIAN_POINT('Ctrl Pts',(0.837623180639486,1.49008697865002,1.10785261035982));
#6822=CARTESIAN_POINT('Ctrl Pts',(0.782439547816649,1.51852112810869,1.1113218695457));
#6823=CARTESIAN_POINT('Ctrl Pts',(0.725998656982107,1.54760309758905,1.1148701694486));
#6824=CARTESIAN_POINT('Ctrl Pts',(0.667997234118838,1.57350171281687,1.1184184693515));
#6825=CARTESIAN_POINT('Ctrl Pts',(0.608832009473348,1.5960706897693,1.1219667692544));
#6826=CARTESIAN_POINT('Ctrl Pts',(0.549666784827857,1.61863966672173,1.12551506915731));
#6827=CARTESIAN_POINT('Ctrl Pts',(0.48933831255979,1.63787889810672,1.1290633690602));
#6828=CARTESIAN_POINT('Ctrl Pts',(0.428256500237485,1.65369720097252,1.13261166896311));
#6829=CARTESIAN_POINT('Ctrl Pts',(0.368400574695673,1.66919803702397,1.13608875595043));
#6830=CARTESIAN_POINT('Ctrl Pts',(0.307582676479223,1.68147584657023,1.13956584293775));
#6831=CARTESIAN_POINT('Ctrl Pts',(0.246181516856185,1.69041791378889,1.14304292992508));
#6832=CARTESIAN_POINT('Ctrl Pts',(0.184410289934603,1.69941387521215,1.14654097345778));
#6833=CARTESIAN_POINT('Ctrl Pts',(0.122049229967692,1.70503354944297,1.15003901699049));
#6834=CARTESIAN_POINT('Ctrl Pts',(0.0594984146863207,1.70721351949597,1.1535370605232));
#6835=CARTESIAN_POINT('Ctrl Pts',(-0.0025109364627393,1.70937461888217,
1.15700482363353));
#6836=CARTESIAN_POINT('Ctrl Pts',(-0.0647062559420003,1.70815530097898,
1.16047258674387));
#6837=CARTESIAN_POINT('Ctrl Pts',(-0.126691088671181,1.70354554695532,1.16394034985421));
#6838=CARTESIAN_POINT('Ctrl Pts',(-0.188639009003621,1.69893853807208,1.16740604788762));
#6839=CARTESIAN_POINT('Ctrl Pts',(-0.250376186231586,1.69094513465487,1.17087174592104));
#6840=CARTESIAN_POINT('Ctrl Pts',(-0.311507813255484,1.67960737816336,1.17433744395445));
#6841=CARTESIAN_POINT('Ctrl Pts',(-0.372625309096618,1.66827224250687,1.17780234085734));
#6842=CARTESIAN_POINT('Ctrl Pts',(-0.433137034075065,1.65359438129887,1.18126723776023));
#6843=CARTESIAN_POINT('Ctrl Pts',(-0.492656961259791,1.63566719751368,1.18473213466312));
#6844=CARTESIAN_POINT('Ctrl Pts',(-0.553157575290576,1.61744463444703,1.1882541213337));
#6845=CARTESIAN_POINT('Ctrl Pts',(-0.612632883565026,1.59586481638843,1.19177610800428));
#6846=CARTESIAN_POINT('Ctrl Pts',(-0.670694323999386,1.57107835140549,1.19529809467485));
#6847=CARTESIAN_POINT('Ctrl Pts',(-0.72788596043462,1.54666320629002,1.19876731933904));
#6848=CARTESIAN_POINT('Ctrl Pts',(-0.783705369257537,1.519137128998,1.20223654400323));
#6849=CARTESIAN_POINT('Ctrl Pts',(-0.837804453796072,1.4886912909329,1.20570576866742));
#6850=CARTESIAN_POINT('Ctrl Pts',(-0.893137694314755,1.45755089558574,1.20925413634119));
#6851=CARTESIAN_POINT('Ctrl Pts',(-0.946670663385841,1.42335615774327,1.21280250401496));
#6852=CARTESIAN_POINT('Ctrl Pts',(-0.998062955749583,1.3863579620215,1.21635087168873));
#6853=CARTESIAN_POINT('Ctrl Pts',(-1.04945524811332,1.34935976629973,1.2198992393625));
#6854=CARTESIAN_POINT('Ctrl Pts',(-1.09870646929954,1.30955851656066,1.22344760703627));
#6855=CARTESIAN_POINT('Ctrl Pts',(-1.14551498837387,1.26724641404536,1.22699597471004));
#6856=CARTESIAN_POINT('Ctrl Pts',(-1.1906986357399,1.22640309840167,1.23042116732171));
#6857=CARTESIAN_POINT('Ctrl Pts',(-1.23379799134156,1.18304695768846,1.23384635993338));
#6858=CARTESIAN_POINT('Ctrl Pts',(-1.27451524177969,1.13742206808698,1.23727155254505));
#6859=CARTESIAN_POINT('Ctrl Pts',(-1.31517768667276,1.09185858972806,1.24069213483686));
#6860=CARTESIAN_POINT('Ctrl Pts',(-1.35346402917097,1.04403279531404,1.24411271712868));
#6861=CARTESIAN_POINT('Ctrl Pts',(-1.38911118072363,0.994227433783946,1.2475332994205));
#6862=CARTESIAN_POINT('Ctrl Pts',(-1.42472427191129,0.944469660594528,1.25095061339279));
#6863=CARTESIAN_POINT('Ctrl Pts',(-1.45770286383511,0.892736490591282,1.25436792736509));
#6864=CARTESIAN_POINT('Ctrl Pts',(-1.4878237713354,0.839344081976698,1.25778524133739));
#6865=CARTESIAN_POINT('Ctrl Pts',(-1.51792765527182,0.785981849381159,1.26120062393153));
#6866=CARTESIAN_POINT('Ctrl Pts',(-1.54517679975331,0.730962692487708,1.26461600652567));
#6867=CARTESIAN_POINT('Ctrl Pts',(-1.56939228284869,0.67463021355034,1.26803138911981));
#6868=CARTESIAN_POINT('Ctrl Pts',(-1.59361608259122,0.618278387596485,1.27144794470447));
#6869=CARTESIAN_POINT('Ctrl Pts',(-1.61480392019255,0.560612814904588,1.27486450028913));
#6870=CARTESIAN_POINT('Ctrl Pts',(-1.63282439117922,0.501998575765123,1.27828105587378));
#6871=CARTESIAN_POINT('Ctrl Pts',(-1.65084729114232,0.443376436021646,1.28169807197542));
#6872=CARTESIAN_POINT('Ctrl Pts',(-1.66570183633137,0.383805881212224,1.28511508807706));
#6873=CARTESIAN_POINT('Ctrl Pts',(-1.67730691034948,0.323665863188982,1.28853210417871));
#6874=CARTESIAN_POINT('Ctrl Pts',(-1.68892792247905,0.263443250405129,1.29195381312275));
#6875=CARTESIAN_POINT('Ctrl Pts',(-1.69729047117641,0.202650131359429,1.2953755220668));
#6876=CARTESIAN_POINT('Ctrl Pts',(-1.70236506406829,0.141673043094835,1.29879723101085));
#6877=CARTESIAN_POINT('Ctrl Pts',(-1.70632609886975,0.09407664002299,1.30146808727392));
#6878=CARTESIAN_POINT('Ctrl Pts',(-1.70828490476063,0.0463683475638418,
1.304138943537));
#6879=CARTESIAN_POINT('Ctrl Pts',(-1.70824952897253,-0.00126856813606742,
1.30680979980007));
#6880=CARTESIAN_POINT('',(-1.70874899700092,0.00144479297225062,1.90680979980007));
#6881=CARTESIAN_POINT('Ctrl Pts',(-1.70952177679497,-0.00126951292371165,
1.30680979980007));
#6882=CARTESIAN_POINT('Ctrl Pts',(-1.71024375601734,-0.0879601103335736,
1.3116666266857));
#6883=CARTESIAN_POINT('Ctrl Pts',(-1.66510645419673,-0.73545936100502,1.34798488882031));
#6884=CARTESIAN_POINT('Ctrl Pts',(-0.83877314664564,-1.82974998182628,1.41576458620388));
#6885=CARTESIAN_POINT('Ctrl Pts',(1.0667458112657,-1.70692133093719,1.5101488919508));
#6886=CARTESIAN_POINT('Ctrl Pts',(2.01226847719202,-0.0479825385523114,
1.60453319769774));
#6887=CARTESIAN_POINT('Ctrl Pts',(1.14689041295175,1.65413688855294,1.69891750344466));
#6888=CARTESIAN_POINT('Ctrl Pts',(-0.750608607457775,1.86764917269852,1.79330180919158));
#6889=CARTESIAN_POINT('Ctrl Pts',(-1.64781001616314,0.790393313501198,1.86259924131006));
#6890=CARTESIAN_POINT('Ctrl Pts',(-1.70976669927472,0.115359128516567,1.90043523817955));
#6891=CARTESIAN_POINT('Ctrl Pts',(-1.70874899700092,0.00144479297225062,
1.90680979980007));
#6892=CARTESIAN_POINT('',(-1.705717720998,-0.000520512975719864,2.50680979980007));
#6893=CARTESIAN_POINT('Ctrl Pts',(-1.70874899700092,0.00144479297225062,
1.90680979980007));
#6894=CARTESIAN_POINT('Ctrl Pts',(-1.7047438638084,-0.446861256979479,1.93189667342853));
#6895=CARTESIAN_POINT('Ctrl Pts',(-1.29576946753668,-1.46386083145327,1.98844498230595));
#6896=CARTESIAN_POINT('Ctrl Pts',(0.411169349837819,-1.97039752822379,2.07645472643237));
#6897=CARTESIAN_POINT('Ctrl Pts',(1.87171845306621,-0.740403048133278,2.17083903217928));
#6898=CARTESIAN_POINT('Ctrl Pts',(1.6478520978538,1.15590228912575,2.26522333792622));
#6899=CARTESIAN_POINT('Ctrl Pts',(-0.0589656792105725,2.01197656350589,
2.35960764367313));
#6900=CARTESIAN_POINT('Ctrl Pts',(-1.46994986117608,1.19754152846963,2.44013646429776));
#6901=CARTESIAN_POINT('Ctrl Pts',(-1.7048382529488,0.315522270522238,2.4892038496734));
#6902=CARTESIAN_POINT('Ctrl Pts',(-1.705717720998,-0.000520512975719864,
2.50680979980007));
#6903=CARTESIAN_POINT('',(-1.71045989027119,-0.000789597318511919,3.10680979980007));
#6904=CARTESIAN_POINT('Ctrl Pts',(-1.705717720998,-0.000520512975719864,
2.50680979980007));
#6905=CARTESIAN_POINT('Ctrl Pts',(-1.70640984249009,-0.249239045816198,
2.52066528492238));
#6906=CARTESIAN_POINT('Ctrl Pts',(-1.53973233319606,-1.0618356879368,2.56598220529367));
#6907=CARTESIAN_POINT('Ctrl Pts',(-0.295068532255919,-1.99109547814598,
2.64276056091391));
#6908=CARTESIAN_POINT('Ctrl Pts',(1.50054859493888,-1.34159627149913,2.73714486666085));
#6909=CARTESIAN_POINT('Ctrl Pts',(1.94577713018251,0.515245573630572,2.83152917240776));
#6910=CARTESIAN_POINT('Ctrl Pts',(0.639942589016321,1.908402505851,2.9259134781547));
#6911=CARTESIAN_POINT('Ctrl Pts',(-1.18947887930053,1.59314638667863,3.01767368728545));
#6912=CARTESIAN_POINT('Ctrl Pts',(-1.70747901217689,0.513193512138237,3.07797246116726));
#6913=CARTESIAN_POINT('Ctrl Pts',(-1.71045989027119,-0.000789597318511919,
3.10680979980007));
#6914=CARTESIAN_POINT('',(-1.70758981783261,0.0014582535397993,3.70680979980007));
#6915=CARTESIAN_POINT('Ctrl Pts',(-1.71045989027119,-0.000789597318511919,
3.10680979980007));
#6916=CARTESIAN_POINT('Ctrl Pts',(-1.71073113971692,-0.0475602565482115,
3.10943389641623));
#6917=CARTESIAN_POINT('Ctrl Pts',(-1.68793010806937,-0.654816382704861,
3.1435194282814));
#6918=CARTESIAN_POINT('Ctrl Pts',(-0.964950165450157,-1.76646478021415,
3.20906639539542));
#6919=CARTESIAN_POINT('Ctrl Pts',(0.944491791186656,-1.77748752398191,3.30345070114242));
#6920=CARTESIAN_POINT('Ctrl Pts',(2.00395731635616,-0.188896044836109,3.3978350068893));
#6921=CARTESIAN_POINT('Ctrl Pts',(1.26000167422617,1.56968863870526,3.49221931263626));
#6922=CARTESIAN_POINT('Ctrl Pts',(-0.617867186307812,1.91566353559733,3.58660361838318));
#6923=CARTESIAN_POINT('Ctrl Pts',(-1.61963156293518,0.871340451104524,3.65813378077111));
#6924=CARTESIAN_POINT('Ctrl Pts',(-1.70888992723901,0.155539500215835,3.69820250791008));
#6925=CARTESIAN_POINT('Ctrl Pts',(-1.70758981783261,0.0014582535397993,
3.70680979980007));
#6926=CARTESIAN_POINT('',(-1.70629192088898,-0.00105167077536168,4.30680979980007));
#6927=CARTESIAN_POINT('Ctrl Pts',(-1.70758981783261,0.0014582535397993,
3.70680979980007));
#6928=CARTESIAN_POINT('Ctrl Pts',(-1.70413775798199,-0.407659381306412,
3.72966394315906));
#6929=CARTESIAN_POINT('Ctrl Pts',(-1.35288253689885,-1.38529989117204,3.78397952176701));
#6930=CARTESIAN_POINT('Ctrl Pts',(0.272061413425965,-1.99436938124897,3.86975653562395));
#6931=CARTESIAN_POINT('Ctrl Pts',(1.81522410712393,-0.869763233554926,3.96414084137088));
#6932=CARTESIAN_POINT('Ctrl Pts',(1.72481229728226,1.03756887996144,4.05852514711779));
#6933=CARTESIAN_POINT('Ctrl Pts',(0.0821902775978209,2.01116170405157,4.15290945286473));
#6934=CARTESIAN_POINT('Ctrl Pts',(-1.42301171001672,1.27783575536462,4.23567100375882));
#6935=CARTESIAN_POINT('Ctrl Pts',(-1.70424737531169,0.354769758201447,4.28697111940393));
#6936=CARTESIAN_POINT('Ctrl Pts',(-1.70629192088898,-0.00105167077536168,
4.30680979980007));
#6937=CARTESIAN_POINT('',(-1.71092577309385,-0.00012504919473697,4.90680979980007));
#6938=CARTESIAN_POINT('Ctrl Pts',(-1.70629192088898,-0.00105167077536168,
4.30680979980007));
#6939=CARTESIAN_POINT('Ctrl Pts',(-1.70748974511699,-0.209514388950238,
4.31843255465291));
#6940=CARTESIAN_POINT('Ctrl Pts',(-1.57615353051455,-0.980804623883353,
4.3615167447547));
#6941=CARTESIAN_POINT('Ctrl Pts',(-0.43389044046669,-1.96551920048943,4.4360623701055));
#6942=CARTESIAN_POINT('Ctrl Pts',(1.40283186881175,-1.44346437052995,4.53044667585243));
#6943=CARTESIAN_POINT('Ctrl Pts',(1.97710379266664,0.377607248774025,4.62483098159934));
#6944=CARTESIAN_POINT('Ctrl Pts',(0.7721208389405,1.85885880407731,4.71921528734628));
#6945=CARTESIAN_POINT('Ctrl Pts',(-1.11983905399775,1.66806212057561,4.81320822674652));
#6946=CARTESIAN_POINT('Ctrl Pts',(-1.71033251354333,0.553250797363694,4.87573973089778));
#6947=CARTESIAN_POINT('Ctrl Pts',(-1.71092577309385,-0.00012504919473697,
4.90680979980007));
#6948=CARTESIAN_POINT('',(-1.70658039029172,0.00119792360719225,5.50680979980008));
#6949=CARTESIAN_POINT('Ctrl Pts',(-1.71092577309385,-0.00012504919473697,
4.90680979980007));
#6950=CARTESIAN_POINT('Ctrl Pts',(-1.7109332459393,-0.0070955095465335,
4.90720116614676));
#6951=CARTESIAN_POINT('Ctrl Pts',(-1.71089426063458,-0.0140658840322902,
4.90759253249344));
#6952=CARTESIAN_POINT('Ctrl Pts',(-1.70391933284558,-0.581328914761308,
4.9394453340891));
#6953=CARTESIAN_POINT('Ctrl Pts',(-1.08638139435793,-1.69449169943945,5.00236820458706));
#6954=CARTESIAN_POINT('Ctrl Pts',(0.817592645828785,-1.8393120678936,5.09675251033397));
#6955=CARTESIAN_POINT('Ctrl Pts',(1.98579059287652,-0.328880479199768,5.19113681608091));
#6956=CARTESIAN_POINT('Ctrl Pts',(1.3669161520747,1.47752054032031,5.28552112182784));
#6957=CARTESIAN_POINT('Ctrl Pts',(-0.482087048092087,1.95425651935824,5.37990542757475));
#6958=CARTESIAN_POINT('Ctrl Pts',(-1.58805687488604,0.95238534644948,5.45366832023218));
#6959=CARTESIAN_POINT('Ctrl Pts',(-1.70786729365446,0.195538944080348,5.49596977764062));
#6960=CARTESIAN_POINT('Ctrl Pts',(-1.70658039029172,0.00119792360719225,
5.50680979980008));
#6961=CARTESIAN_POINT('',(-1.70721003800208,-0.00139829312648681,6.10680979980007));
#6962=CARTESIAN_POINT('Ctrl Pts',(-1.70658039029172,0.00119792360719225,
5.50680979980008));
#6963=CARTESIAN_POINT('Ctrl Pts',(-1.70413226191533,-0.368504868920307,
5.52743121288959));
#6964=CARTESIAN_POINT('Ctrl Pts',(-1.40556429020907,-1.30585481825115,5.57951406122808));
#6965=CARTESIAN_POINT('Ctrl Pts',(0.131615469299055,-2.00853248810358,5.66305834481553));
#6966=CARTESIAN_POINT('Ctrl Pts',(1.74980235607298,-0.99484646099087,5.75744265056247));
#6967=CARTESIAN_POINT('Ctrl Pts',(1.79328979108982,0.914133772091395,5.85182695630937));
#6968=CARTESIAN_POINT('Ctrl Pts',(0.222941955990293,2.00045366742654,5.94621126205633));
#6969=CARTESIAN_POINT('Ctrl Pts',(-1.37184809092268,1.35754094959989,6.03120554321987));
#6970=CARTESIAN_POINT('Ctrl Pts',(-1.70407444749312,0.393931601296323,6.08473838913446));
#6971=CARTESIAN_POINT('Ctrl Pts',(-1.70721003800208,-0.00139829312648681,
6.10680979980007));
#6972=CARTESIAN_POINT('',(-1.71069332253564,0.000492187094742366,6.70680979980008));
#6973=CARTESIAN_POINT('Ctrl Pts',(-1.70721003800208,-0.00139829312648681,
6.10680979980007));
#6974=CARTESIAN_POINT('Ctrl Pts',(-1.70854403846125,-0.169586791968197,
6.11619982438344));
#6975=CARTESIAN_POINT('Ctrl Pts',(-1.60895730772148,-0.899747975566428,
6.15705128421577));
#6976=CARTESIAN_POINT('Ctrl Pts',(-0.570578023721532,-1.93026152129124,
6.22936417929709));
#6977=CARTESIAN_POINT('Ctrl Pts',(1.29821511874949,-1.53826168179717,6.32374848504401));
#6978=CARTESIAN_POINT('Ctrl Pts',(1.9987084670187,0.238165610479905,6.41813279079093));
#6979=CARTESIAN_POINT('Ctrl Pts',(0.900498826589758,1.8000707639935,6.51251709653787));
#6980=CARTESIAN_POINT('Ctrl Pts',(-1.00808634131497,1.74239953938573,6.60690140228478));
#6981=CARTESIAN_POINT('Ctrl Pts',(-1.69522136426491,0.626405574154833,6.67166563670553));
#6982=CARTESIAN_POINT('Ctrl Pts',(-1.71083804055838,0.0332932687764938,
6.70496843587729));
#6983=CARTESIAN_POINT('Ctrl Pts',(-1.71069332253564,0.000492187094742366,
6.70680979980008));
#6984=CARTESIAN_POINT('',(0.433376258375141,-1.65493082312738,6.88122480138927));
#6985=CARTESIAN_POINT('Ctrl Pts',(-1.71069332253564,0.000492187094742366,
6.70680979980008));
#6986=CARTESIAN_POINT('Ctrl Pts',(-1.70836539696767,-0.527144075876519,
6.73642987112627));
#6987=CARTESIAN_POINT('Ctrl Pts',(-1.19174755964131,-1.566331294562,6.79456820498932));
#6988=CARTESIAN_POINT('Ctrl Pts',(-0.0592995318133123,-1.78055737442536,
6.85270653885239));
#6989=CARTESIAN_POINT('Ctrl Pts',(0.433376258375141,-1.65493082312738,6.88122480138927));
#6990=CARTESIAN_POINT('',(-1.03231334037779,-1.36104637311814,6.88122480138927));
#6991=CARTESIAN_POINT('Origin',(0.,0.,6.88122480138927));
#6992=CARTESIAN_POINT('',(-1.7090644143042,0.000376576228701876,6.79319020019992));
#6993=CARTESIAN_POINT('Ctrl Pts',(-1.03231334037779,-1.36104637311814,6.88122480138927));
#6994=CARTESIAN_POINT('Ctrl Pts',(-1.08459431799775,-1.32139280090265,6.87755669300638));
#6995=CARTESIAN_POINT('Ctrl Pts',(-1.13464020645309,-1.27868275150367,6.87388858462349));
#6996=CARTESIAN_POINT('Ctrl Pts',(-1.18208844104253,-1.23320111095216,6.8702204762406));
#6997=CARTESIAN_POINT('Ctrl Pts',(-1.22757216456718,-1.18960255808308,6.86670423946194));
#6998=CARTESIAN_POINT('Ctrl Pts',(-1.27066873038283,-1.14345778921077,6.86318800268328));
#6999=CARTESIAN_POINT('Ctrl Pts',(-1.31109333933297,-1.09505813455575,6.85967176590462));
#7000=CARTESIAN_POINT('Ctrl Pts',(-1.35150659787644,-1.04667206953777,6.85615651641362));
#7001=CARTESIAN_POINT('Ctrl Pts',(-1.38924907585107,-0.996032750533164,
6.85264126692262));
#7002=CARTESIAN_POINT('Ctrl Pts',(-1.42407536961439,-0.94346563485781,6.84912601743161));
#7003=CARTESIAN_POINT('Ctrl Pts',(-1.45890322424902,-0.890896163189488,
6.84561061039149));
#7004=CARTESIAN_POINT('Ctrl Pts',(-1.49081436599465,-0.836399131200913,
6.84209520335136));
#7005=CARTESIAN_POINT('Ctrl Pts',(-1.51960696700599,-0.78032860278658,6.83857979631123));
#7006=CARTESIAN_POINT('Ctrl Pts',(-1.54841023310964,-0.7242373052392,6.83506308712613));
#7007=CARTESIAN_POINT('Ctrl Pts',(-1.5740924429493,-0.666571789194321,6.83154637794103));
#7008=CARTESIAN_POINT('Ctrl Pts',(-1.59649873557777,-0.60770868826978,6.82802966875593));
#7009=CARTESIAN_POINT('Ctrl Pts',(-1.61893717283678,-0.548761140861256,
6.82450791441146));
#7010=CARTESIAN_POINT('Ctrl Pts',(-1.63809014229962,-0.488613038233603,
6.82098616006698));
#7011=CARTESIAN_POINT('Ctrl Pts',(-1.65385207374626,-0.42765801835719,6.8174644057225));
#7012=CARTESIAN_POINT('Ctrl Pts',(-1.66962716398094,-0.3666521104161,6.8139397112549));
#7013=CARTESIAN_POINT('Ctrl Pts',(-1.68200548521952,-0.304838423128845,
6.81041501678731));
#7014=CARTESIAN_POINT('Ctrl Pts',(-1.69093278872226,-0.242619798293478,
6.80689032231972));
#7015=CARTESIAN_POINT('Ctrl Pts',(-1.69987711779078,-0.180282514191069,
6.80335890578677));
#7016=CARTESIAN_POINT('Ctrl Pts',(-1.70535725198845,-0.117539237435382,
6.79982748925383));
#7017=CARTESIAN_POINT('Ctrl Pts',(-1.70737092020885,-0.0547960155959329,
6.79629607272089));
#7018=CARTESIAN_POINT('Ctrl Pts',(-1.70796125902744,-0.0364018436661475,
6.79526078188056));
#7019=CARTESIAN_POINT('Ctrl Pts',(-1.70825400928489,-0.0180076557448326,
6.79422549104024));
#7020=CARTESIAN_POINT('Ctrl Pts',(-1.70824995853226,0.000376396771052057,
6.79319020019992));
#7021=CARTESIAN_POINT('',(-1.70733856330343,-0.0014377884632695,6.19319020019993));
#7022=CARTESIAN_POINT('Ctrl Pts',(-1.71055216417171,0.000376904040357041,
6.79319020019992));
#7023=CARTESIAN_POINT('Ctrl Pts',(-1.71073076079401,0.0380123029285045,
6.79107363201406));
#7024=CARTESIAN_POINT('Ctrl Pts',(-1.69251520158208,0.635023283971082,6.75749562857924));
#7025=CARTESIAN_POINT('Ctrl Pts',(-0.99317638825687,1.75221471014715,6.69245618989542));
#7026=CARTESIAN_POINT('Ctrl Pts',(0.916129322380027,1.79161764679409,6.5980718841485));
#7027=CARTESIAN_POINT('Ctrl Pts',(2.00063946484888,0.221190637255988,6.50368757840157));
#7028=CARTESIAN_POINT('Ctrl Pts',(1.28489523215748,-1.54959303984541,6.40930327265464));
#7029=CARTESIAN_POINT('Ctrl Pts',(-0.587259843124623,-1.92516956402138,
6.31491896690772));
#7030=CARTESIAN_POINT('Ctrl Pts',(-1.61275586842781,-0.889773899116702,
6.24288127608948));
#7031=CARTESIAN_POINT('Ctrl Pts',(-1.70866489019705,-0.164666545902499,
6.20230502052022));
#7032=CARTESIAN_POINT('Ctrl Pts',(-1.70733856330343,-0.0014377884632695,
6.19319020019993));
#7033=CARTESIAN_POINT('',(-1.70647429782816,0.00114928838020923,5.59319020019992));
#7034=CARTESIAN_POINT('Ctrl Pts',(-1.70733856330343,-0.0014377884632695,
6.19319020019993));
#7035=CARTESIAN_POINT('Ctrl Pts',(-1.70408683531321,0.398746752713406,6.17084358527124));
#7036=CARTESIAN_POINT('Ctrl Pts',(-1.3652449466822,1.36733416363711,6.11703553509359));
#7037=CARTESIAN_POINT('Ctrl Pts',(0.240231051783908,1.99843873469232,6.03176604966692));
#7038=CARTESIAN_POINT('Ctrl Pts',(1.80112487550057,0.898601953609902,5.93738174392003));
#7039=CARTESIAN_POINT('Ctrl Pts',(1.74113633374771,-1.0099409559506,5.84299743817307));
#7040=CARTESIAN_POINT('Ctrl Pts',(0.114245086704342,-2.00959340467034,5.74861313242617));
#7041=CARTESIAN_POINT('Ctrl Pts',(-1.41175815753826,-1.29601290328604,5.66534405310177));
#7042=CARTESIAN_POINT('Ctrl Pts',(-1.70416640047656,-0.363676910033684,
5.61353640902636));
#7043=CARTESIAN_POINT('Ctrl Pts',(-1.70647429782816,0.00114928838020924,
5.59319020019992));
#7044=CARTESIAN_POINT('',(-1.71093671904409,-3.71626710015116E-5,4.99319020019992));
#7045=CARTESIAN_POINT('Ctrl Pts',(-1.70647429782816,0.00114928838020922,
5.59319020019992));
#7046=CARTESIAN_POINT('Ctrl Pts',(-1.70773511264835,0.200455499912553,5.58207497377739));
#7047=CARTESIAN_POINT('Ctrl Pts',(-1.58392193718951,0.962377793456982,5.53949831210587));
#7048=CARTESIAN_POINT('Ctrl Pts',(-0.465173068895533,1.95835109737102,5.46546021518539));
#7049=CARTESIAN_POINT('Ctrl Pts',(1.37963915910134,1.46564745709577,5.37107590943847));
#7050=CARTESIAN_POINT('Ctrl Pts',(1.98287289578746,-0.346036772783098,5.27669160369153));
#7051=CARTESIAN_POINT('Ctrl Pts',(0.801659924002396,-1.84631185111647,5.18230729794462));
#7052=CARTESIAN_POINT('Ctrl Pts',(-1.10099078479098,-1.68503579381714,5.08792299219768));
#7053=CARTESIAN_POINT('Ctrl Pts',(-1.71000378738849,-0.56451081151032,5.02488395961612));
#7054=CARTESIAN_POINT('Ctrl Pts',(-1.71093739349098,-0.00210604024018896,
4.99330636228354));
#7055=CARTESIAN_POINT('Ctrl Pts',(-1.71093671904409,-3.71626710014006E-5,
4.99319020019992));
#7056=CARTESIAN_POINT('',(-1.70638863318681,-0.00110593147553267,4.39319020019992));
#7057=CARTESIAN_POINT('Ctrl Pts',(-1.71093671904409,-3.71626710016226E-5,
4.99319020019992));
#7058=CARTESIAN_POINT('Ctrl Pts',(-1.71075472573678,0.558230479703889,4.96184492703456));
#7059=CARTESIAN_POINT('Ctrl Pts',(-1.11091973990757,1.67717074904876,4.89903821862023));
#7060=CARTESIAN_POINT('Ctrl Pts',(0.788163059251489,1.85211372924192,4.8047700749569));
#7061=CARTESIAN_POINT('Ctrl Pts',(1.9802944814926,0.360499692491619,4.71038576920999));
#7062=CARTESIAN_POINT('Ctrl Pts',(1.39029962886282,-1.45553880087964,4.61600146346305));
#7063=CARTESIAN_POINT('Ctrl Pts',(-0.450867470888686,-1.96169436651404,
4.52161715771613));
#7064=CARTESIAN_POINT('Ctrl Pts',(-1.58038891107441,-0.970812636144332,
4.44734673662842));
#7065=CARTESIAN_POINT('Ctrl Pts',(-1.70762300397305,-0.204603575060088,
4.40453775078968));
#7066=CARTESIAN_POINT('Ctrl Pts',(-1.70638863318681,-0.00110593147553267,
4.39319020019992));
#7067=CARTESIAN_POINT('',(-1.70745364674527,0.00144013658803385,3.79319020019992));
#7068=CARTESIAN_POINT('Ctrl Pts',(-1.70638863318681,-0.00110593147553267,
4.39319020019992));
#7069=CARTESIAN_POINT('Ctrl Pts',(-1.70420067276091,0.359599940607081,4.37307631554071));
#7070=CARTESIAN_POINT('Ctrl Pts',(-1.41693678240365,1.28769571311434,4.32150099563251));
#7071=CARTESIAN_POINT('Ctrl Pts',(0.0995750801122244,2.01037585185725,4.23846424047536));
#7072=CARTESIAN_POINT('Ctrl Pts',(1.73371824985778,1.02261786219037,4.14407993472842));
#7073=CARTESIAN_POINT('Ctrl Pts',(1.80763647646394,-0.88542454841268,4.04969562898151));
#7074=CARTESIAN_POINT('Ctrl Pts',(0.254808535468846,-1.99664690727106,3.95531132323457));
#7075=CARTESIAN_POINT('Ctrl Pts',(-1.3596124526819,-1.37555056956786,3.86980951364072));
#7076=CARTESIAN_POINT('Ctrl Pts',(-1.70410728468879,-0.402832987616667,
3.81576913929583));
#7077=CARTESIAN_POINT('Ctrl Pts',(-1.70745364674527,0.00144013658803385,
3.79319020019992));
#7078=CARTESIAN_POINT('',(-1.71054831940743,-0.000715229540035611,3.19319020019992));
#7079=CARTESIAN_POINT('Ctrl Pts',(-1.70745364674527,0.00144013658803385,
3.79319020019992));
#7080=CARTESIAN_POINT('Ctrl Pts',(-1.70877009691005,0.160480136442858,3.78430770404685));
#7081=CARTESIAN_POINT('Ctrl Pts',(-1.61592638481939,0.881326231316457,3.74396377264484));
#7082=CARTESIAN_POINT('Ctrl Pts',(-0.601281834025254,1.92093373599865,3.67215840599379));
#7083=CARTESIAN_POINT('Ctrl Pts',(1.27352556254399,1.55873631623992,3.57777410024688));
#7084=CARTESIAN_POINT('Ctrl Pts',(2.00224918884281,-0.206214567376117,3.48338979449994));
#7085=CARTESIAN_POINT('Ctrl Pts',(0.929088842915232,-1.78558678982326,3.38900548875303));
#7086=CARTESIAN_POINT('Ctrl Pts',(-0.980186360320026,-1.75805601761238,
3.29462118300609));
#7087=CARTESIAN_POINT('Ctrl Pts',(-1.69053325787773,-0.644891975364033,
3.22934942015507));
#7088=CARTESIAN_POINT('Ctrl Pts',(-1.71077187969281,-0.042575030137566,
3.19553909255301));
#7089=CARTESIAN_POINT('Ctrl Pts',(-1.71054831940743,-0.000715229540035611,
3.19319020019992));
#7090=CARTESIAN_POINT('',(-1.70576661654484,-0.000592994286356119,2.59319020019992));
#7091=CARTESIAN_POINT('Ctrl Pts',(-1.71054831940743,-0.000715229540035611,
3.19319020019992));
#7092=CARTESIAN_POINT('Ctrl Pts',(-1.70777747791287,0.518101751965672,3.16407765730403));
#7093=CARTESIAN_POINT('Ctrl Pts',(-1.18115523050738,1.60247259901729,3.10350367915917));
#7094=CARTESIAN_POINT('Ctrl Pts',(0.656418095559625,1.90279834608092,3.01146826576533));
#7095=CARTESIAN_POINT('Ctrl Pts',(1.95015896916594,0.498403708851651,2.91708396001839));
#7096=CARTESIAN_POINT('Ctrl Pts',(1.48889341829145,-1.35451934315334,2.82269965427146));
#7097=CARTESIAN_POINT('Ctrl Pts',(-0.312271882189301,-1.98846989759894,
2.72831534852454));
#7098=CARTESIAN_POINT('Ctrl Pts',(-1.54442260766096,-1.05185319082121,2.65181219716736));
#7099=CARTESIAN_POINT('Ctrl Pts',(-1.7065407794744,-0.244353809801757,2.60677048105915));
#7100=CARTESIAN_POINT('Ctrl Pts',(-1.70576661654484,-0.000592994286356119,
2.59319020019992));
#7101=CARTESIAN_POINT('',(-1.7086043211043,0.00146224045955247,1.99319020019992));
#7102=CARTESIAN_POINT('Ctrl Pts',(-1.70576661654484,-0.000592994286356119,
2.59319020019992));
#7103=CARTESIAN_POINT('Ctrl Pts',(-1.70474727629631,0.320366846057213,2.57530904581018));
#7104=CARTESIAN_POINT('Ctrl Pts',(-1.46438715133716,1.20746393579915,2.52596645617147));
#7105=CARTESIAN_POINT('Ctrl Pts',(-0.041568549553779,2.01241107082974,2.44516243128376));
#7106=CARTESIAN_POINT('Ctrl Pts',(1.65778400451944,1.14161221786942,2.35077812553685));
#7107=CARTESIAN_POINT('Ctrl Pts',(1.8652471156411,-0.756557637845384,2.25639381978991));
#7108=CARTESIAN_POINT('Ctrl Pts',(0.394118520517271,-1.97387863246546,2.16200951404299));
#7109=CARTESIAN_POINT('Ctrl Pts',(-1.30305340392856,-1.45423325181973,2.07427497417966));
#7110=CARTESIAN_POINT('Ctrl Pts',(-1.70463207257213,-0.442022540533928,
2.0180018695653));
#7111=CARTESIAN_POINT('Ctrl Pts',(-1.7086043211043,0.00146224045955247,
1.99319020019992));
#7112=CARTESIAN_POINT('',(-1.70965372155593,-0.00122376277469999,1.39319020019992));
#7113=CARTESIAN_POINT('Ctrl Pts',(-1.7086043211043,0.00146224045955247,
1.99319020019992));
#7114=CARTESIAN_POINT('Ctrl Pts',(-1.70966892189281,0.120320424611316,1.98654043431633));
#7115=CARTESIAN_POINT('Ctrl Pts',(-1.64451481097969,0.800362997705775,1.94842923318373));
#7116=CARTESIAN_POINT('Ctrl Pts',(-0.734433412509021,1.8740687918552,1.87885659680224));
#7117=CARTESIAN_POINT('Ctrl Pts',(1.16114866158118,1.64415936688714,1.78447229105527));
#7118=CARTESIAN_POINT('Ctrl Pts',(2.01177830590373,-0.0653782589161231,
1.69008798530838));
#7119=CARTESIAN_POINT('Ctrl Pts',(1.05194843294444,-1.7160800765306,1.59570367956143));
#7120=CARTESIAN_POINT('Ctrl Pts',(-0.854561305477856,-1.82242998781983,
1.50131937381452));
#7121=CARTESIAN_POINT('Ctrl Pts',(-1.66808598891422,-0.725507541111736,
1.433814880694));
#7122=CARTESIAN_POINT('Ctrl Pts',(-1.71031813974082,-0.0829856766656713,
1.39777182282248));
#7123=CARTESIAN_POINT('Ctrl Pts',(-1.70965372155593,-0.00122376277469999,
1.39319020019992));
#7124=CARTESIAN_POINT('',(-1.70798406265114,2.48985917316355E-5,0.793190198053302));
#7125=CARTESIAN_POINT('Ctrl Pts',(-1.70965372155593,-0.00122376277469999,
1.39319020019992));
#7126=CARTESIAN_POINT('Ctrl Pts',(-1.70575566233395,0.47846326219923,1.3663103875735));
#7127=CARTESIAN_POINT('Ctrl Pts',(-1.24660295336588,1.52614216487693,1.3079691396981));
#7128=CARTESIAN_POINT('Ctrl Pts',(0.521444772704797,1.9441245725567,1.21816645657374));
#7129=CARTESIAN_POINT('Ctrl Pts',(1.91043254963484,0.633857130546934,1.1237821508268));
#7130=CARTESIAN_POINT('Ctrl Pts',(1.5801645446874,-1.24683939123611,1.02939784507989));
#7131=CARTESIAN_POINT('Ctrl Pts',(-0.172140159774847,-2.00546387584604,
0.935013539332954));
#7132=CARTESIAN_POINT('Ctrl Pts',(-1.50469283484901,-1.13276427476656,0.856277657706305));
#7133=CARTESIAN_POINT('Ctrl Pts',(-1.70552555931313,-0.283899278264277,
0.809003211328624));
#7134=CARTESIAN_POINT('Ctrl Pts',(-1.7055606080675,2.48247144564451E-5,
0.793190200199919));
#7135=CARTESIAN_POINT('Ctrl Pts',(-1.70824999981843,2.49066986354841E-5,
0.793190197817743));
#7136=CARTESIAN_POINT('Ctrl Pts',(-1.70824904800449,0.0653059853313177,
0.789560124769425));
#7137=CARTESIAN_POINT('Ctrl Pts',(-1.70450170914895,0.130515412064531,0.785930051721107));
#7138=CARTESIAN_POINT('Ctrl Pts',(-1.69705822465692,0.195221527051415,0.782299978672789));
#7139=CARTESIAN_POINT('Ctrl Pts',(-1.68959377517735,0.260109890405459,0.778659681322087));
#7140=CARTESIAN_POINT('Ctrl Pts',(-1.67841243357824,0.324491680054332,0.775019383971384));
#7141=CARTESIAN_POINT('Ctrl Pts',(-1.66361588672389,0.387943609226772,0.771379086620682));
#7142=CARTESIAN_POINT('Ctrl Pts',(-1.64879657993075,0.45149313968672,0.767733189791556));
#7143=CARTESIAN_POINT('Ctrl Pts',(-1.63035110565223,0.514109545100054,0.764087292962431));
#7144=CARTESIAN_POINT('Ctrl Pts',(-1.60843066443068,0.575385835956247,0.760441396133305));
#7145=CARTESIAN_POINT('Ctrl Pts',(-1.58645287966122,0.636822424677127,0.756785961692349));
#7146=CARTESIAN_POINT('Ctrl Pts',(-1.5609821340813,0.696911497006324,0.753130527251392));
#7147=CARTESIAN_POINT('Ctrl Pts',(-1.53221724143077,0.755267096835475,0.749475092810436));
#7148=CARTESIAN_POINT('Ctrl Pts',(-1.52374443652028,0.772455953362547,0.748398371153326));
#7149=CARTESIAN_POINT('Ctrl Pts',(-1.5149861191257,0.789494590766846,0.747321649496215));
#7150=CARTESIAN_POINT('Ctrl Pts',(-1.50594809069531,0.806373617271273,0.746244927839105));
#7151=CARTESIAN_POINT('Ctrl Pts',(-1.47676075081638,0.860882616352725,0.742767771155749));
#7152=CARTESIAN_POINT('Ctrl Pts',(-1.44455193799279,0.913913534313018,0.739290614472393));
#7153=CARTESIAN_POINT('Ctrl Pts',(-1.40949556232082,0.965111559509007,0.735813457789037));
#7154=CARTESIAN_POINT('Ctrl Pts',(-1.37422869517758,1.01661699662204,0.732315422968335));
#7155=CARTESIAN_POINT('Ctrl Pts',(-1.33608013502565,1.0662669659466,0.728817388147633));
#7156=CARTESIAN_POINT('Ctrl Pts',(-1.29527450114133,1.11372439552749,0.72531935332693));
#7157=CARTESIAN_POINT('Ctrl Pts',(-1.25482121350369,1.16077204230149,0.721851523145208));
#7158=CARTESIAN_POINT('Ctrl Pts',(-1.21175688544118,1.2056644663069,0.718383692963486));
#7159=CARTESIAN_POINT('Ctrl Pts',(-1.16634294648347,1.24810343869739,0.714915862781763));
#7160=CARTESIAN_POINT('Ctrl Pts',(-1.12095606655812,1.29051712463281,0.711450098840743));
#7161=CARTESIAN_POINT('Ctrl Pts',(-1.07322272201843,1.33047991231744,0.707984334899722));
#7162=CARTESIAN_POINT('Ctrl Pts',(-1.02344149396535,1.36773007970505,0.704518570958701));
#7163=CARTESIAN_POINT('Ctrl Pts',(-0.973671791295235,1.40497162290917,0.70105360941365));
#7164=CARTESIAN_POINT('Ctrl Pts',(-0.921855552555898,1.43950148904052,0.697588647868598));
#7165=CARTESIAN_POINT('Ctrl Pts',(-0.868323161565795,1.47109923172721,0.694123686323547));
#7166=CARTESIAN_POINT('Ctrl Pts',(-0.813910752042225,1.50321640944502,0.690601764304266));
#7167=CARTESIAN_POINT('Ctrl Pts',(-0.757725698401431,1.53230387803247,0.687079842284985));
#7168=CARTESIAN_POINT('Ctrl Pts',(-0.700142113430193,1.55817812958002,0.683557920265704));
#7169=CARTESIAN_POINT('Ctrl Pts',(-0.643419138270495,1.58366568004325,0.680088634785931));
#7170=CARTESIAN_POINT('Ctrl Pts',(-0.585339659884467,1.60603528705814,0.676619349306157));
#7171=CARTESIAN_POINT('Ctrl Pts',(-0.526280215216498,1.62516066823304,0.673150063826383));
#7172=CARTESIAN_POINT('Ctrl Pts',(-0.465876681912426,1.64472130929979,0.669601823537349));
#7173=CARTESIAN_POINT('Ctrl Pts',(-0.404448563601747,1.66088807131683,0.666053583248315));
#7174=CARTESIAN_POINT('Ctrl Pts',(-0.342411013067568,1.673580819868,0.662505342959281));
#7175=CARTESIAN_POINT('Ctrl Pts',(-0.280373462533389,1.68627356841916,0.658957102670247));
#7176=CARTESIAN_POINT('Ctrl Pts',(-0.217727043916524,1.69549228730872,0.655408862381214));
#7177=CARTESIAN_POINT('Ctrl Pts',(-0.15489099546036,1.70121334406514,0.651860622092181));
#7178=CARTESIAN_POINT('Ctrl Pts',(-0.0933111593584229,1.70682002599448,
0.648383317888346));
#7179=CARTESIAN_POINT('Ctrl Pts',(-0.0313038835783991,1.70909001322935,
0.64490601368451));
#7180=CARTESIAN_POINT('Ctrl Pts',(0.0307388207184475,1.70797341530858,0.641428709480675));
#7181=CARTESIAN_POINT('Ctrl Pts',(0.0931510755020205,1.70685016649613,0.637930693100032));
#7182=CARTESIAN_POINT('Ctrl Pts',(0.155598673626593,1.70229973564838,0.634432676719391));
#7183=CARTESIAN_POINT('Ctrl Pts',(0.217676590514528,1.69432433862055,0.630934660338748));
#7184=CARTESIAN_POINT('Ctrl Pts',(0.279221525684353,1.6864174158751,0.627466676840554));
#7185=CARTESIAN_POINT('Ctrl Pts',(0.340402590208932,1.67514416271573,0.62399869334236));
#7186=CARTESIAN_POINT('Ctrl Pts',(0.400826897536886,1.6605589001029,0.620530709844166));
#7187=CARTESIAN_POINT('Ctrl Pts',(0.461215233697022,1.64598232023634,0.617064790869702));
#7188=CARTESIAN_POINT('Ctrl Pts',(0.520847213960595,1.62809775984405,0.613598871895239));
#7189=CARTESIAN_POINT('Ctrl Pts',(0.579340008693228,1.60701064614623,0.610132952920775));
#7190=CARTESIAN_POINT('Ctrl Pts',(0.637819286059113,1.5859284055657,0.606667834901337));
#7191=CARTESIAN_POINT('Ctrl Pts',(0.695159423647654,1.56164525319152,0.6032027168819));
#7192=CARTESIAN_POINT('Ctrl Pts',(0.750994572684008,1.534315878266,0.599737598862462));
#7193=CARTESIAN_POINT('Ctrl Pts',(0.807742640007617,1.50653966140347,0.596215825319362));
#7194=CARTESIAN_POINT('Ctrl Pts',(0.862935559076709,1.47561691060882,0.59269405177626));
#7195=CARTESIAN_POINT('Ctrl Pts',(0.916214371241624,1.44175909514395,0.58917227823316));
#7196=CARTESIAN_POINT('Ctrl Pts',(0.968701515358272,1.40840437180142,0.585702834602721));
#7197=CARTESIAN_POINT('Ctrl Pts',(1.01933067202352,1.37220157791386,0.582233390972282));
#7198=CARTESIAN_POINT('Ctrl Pts',(1.06778924659198,1.33339573546736,0.578763947341843));
#7199=CARTESIAN_POINT('Ctrl Pts',(1.11734417834837,1.29371192529939,0.575216008842412));
#7200=CARTESIAN_POINT('Ctrl Pts',(1.16462867286814,1.25130619195914,0.57166807034298));
#7201=CARTESIAN_POINT('Ctrl Pts',(1.20934754682838,1.20648107050222,0.568120131843548));
#7202=CARTESIAN_POINT('Ctrl Pts',(1.25406642078862,1.1616559490453,0.564572193344117));
#7203=CARTESIAN_POINT('Ctrl Pts',(1.29621935059572,1.11441190134086,0.561024254844686));
#7204=CARTESIAN_POINT('Ctrl Pts',(1.33555606823082,1.06508593602199,0.557476316345254));
#7205=CARTESIAN_POINT('Ctrl Pts',(1.37409908092581,1.01675523072233,0.553999965321431));
#7206=CARTESIAN_POINT('Ctrl Pts',(1.4100922720091,0.966233086539148,0.550523614297609));
#7207=CARTESIAN_POINT('Ctrl Pts',(1.44327838089219,0.91381922596826,0.547047263273786));
#7208=CARTESIAN_POINT('Ctrl Pts',(1.4766724500553,0.861076914684464,0.543549127745642));
#7209=CARTESIAN_POINT('Ctrl Pts',(1.50722375201572,0.806419454082804,0.540050992217498));
#7210=CARTESIAN_POINT('Ctrl Pts',(1.53471117517402,0.750186424361296,0.536552856689354));
#7211=CARTESIAN_POINT('Ctrl Pts',(1.56195415333876,0.694453473621678,0.533085829996392));
#7212=CARTESIAN_POINT('Ctrl Pts',(1.58618728991764,0.637173322256977,0.529618803303431));
#7213=CARTESIAN_POINT('Ctrl Pts',(1.60723987019004,0.578703777568036,0.52615177661047));
#7214=CARTESIAN_POINT('Ctrl Pts',(1.62827992233335,0.520269027379043,0.522686813102039));
#7215=CARTESIAN_POINT('Ctrl Pts',(1.6461430000243,0.460646764116287,0.519221849593608));
#7216=CARTESIAN_POINT('Ctrl Pts',(1.66070659833316,0.400214513420863,0.515756886085177));
#7217=CARTESIAN_POINT('Ctrl Pts',(1.6752668424373,0.339796181136028,0.512292720607337));
#7218=CARTESIAN_POINT('Ctrl Pts',(1.68652899719077,0.278568725063664,0.508828555129497));
#7219=CARTESIAN_POINT('Ctrl Pts',(1.69442103772059,0.216922588565335,0.505364389651658));
#7220=CARTESIAN_POINT('Ctrl Pts',(1.70244642726282,0.154234839141967,0.501841691397214));
#7221=CARTESIAN_POINT('Ctrl Pts',(1.70698664584483,0.0911146596408995,0.49831899314277));
#7222=CARTESIAN_POINT('Ctrl Pts',(1.70802086016062,0.0279786303485646,0.494796294888326));
#7223=CARTESIAN_POINT('Ctrl Pts',(1.70903916534196,-0.0341861886603169,
0.491327785673144));
#7224=CARTESIAN_POINT('Ctrl Pts',(1.70665866753178,-0.0963658581007371,
0.487859276457963));
#7225=CARTESIAN_POINT('Ctrl Pts',(1.70091210258035,-0.158164729935928,0.484390767242781));
#7226=CARTESIAN_POINT('Ctrl Pts',(1.69503086846078,-0.221411841324995,0.480840974468706));
#7227=CARTESIAN_POINT('Ctrl Pts',(1.68562385964258,-0.28425952079805,0.47729118169463));
#7228=CARTESIAN_POINT('Ctrl Pts',(1.67278165693898,-0.346294081249582,0.473741388920555));
#7229=CARTESIAN_POINT('Ctrl Pts',(1.65993945423537,-0.408328641701114,0.470191596146479));
#7230=CARTESIAN_POINT('Ctrl Pts',(1.64366226665055,-0.469549556576522,0.466641803372404));
#7231=CARTESIAN_POINT('Ctrl Pts',(1.6240943292254,-0.529561773807261,0.463092010598329));
#7232=CARTESIAN_POINT('Ctrl Pts',(1.60492317546848,-0.588357109198412,0.459614197807003));
#7233=CARTESIAN_POINT('Ctrl Pts',(1.58251700648443,-0.646227082357713,0.456136385015678));
#7234=CARTESIAN_POINT('Ctrl Pts',(1.55698484003375,-0.702791768879724,0.452658572224353));
#7235=CARTESIAN_POINT('Ctrl Pts',(1.53130481679242,-0.759684021534016,0.449160619417147));
#7236=CARTESIAN_POINT('Ctrl Pts',(1.5024625657549,-0.815255307085509,0.44566266660994));
#7237=CARTESIAN_POINT('Ctrl Pts',(1.47062003184681,-0.869134503072382,0.442164713802734));
#7238=CARTESIAN_POINT('Ctrl Pts',(1.43904583950905,-0.922559651397707,0.43869623874224));
#7239=CARTESIAN_POINT('Ctrl Pts',(1.40452198945138,-0.974320670287452,0.435227763681744));
#7240=CARTESIAN_POINT('Ctrl Pts',(1.36725357699574,-1.02407798467322,0.43175928862125));
#7241=CARTESIAN_POINT('Ctrl Pts',(1.33000743034862,-1.07380557182453,0.428292885782148));
#7242=CARTESIAN_POINT('Ctrl Pts',(1.29002027657257,-1.12153142346553,0.424826482943047));
#7243=CARTESIAN_POINT('Ctrl Pts',(1.24754019314874,-1.16694538388838,0.421360080103945));
#7244=CARTESIAN_POINT('Ctrl Pts',(1.20507002871248,-1.21234874027112,0.417894486660774));
#7245=CARTESIAN_POINT('Ctrl Pts',(1.16010843671315,-1.25544090714597,0.414428893217603));
#7246=CARTESIAN_POINT('Ctrl Pts',(1.11294204987345,-1.29594677981909,0.410963299774432));
#7247=CARTESIAN_POINT('Ctrl Pts',(1.06501750801737,-1.33710374604883,0.407442000197513));
#7248=CARTESIAN_POINT('Ctrl Pts',(1.01481704383944,-1.37559015414555,0.403920700620595));
#7249=CARTESIAN_POINT('Ctrl Pts',(0.962676466098439,-1.4111598364892,0.400399401043676));
#7250=CARTESIAN_POINT('Ctrl Pts',(0.911297074618249,-1.44621024661389,0.396929507971523));
#7251=CARTESIAN_POINT('Ctrl Pts',(0.858034319747585,-1.47842831995168,0.393459614899369));
#7252=CARTESIAN_POINT('Ctrl Pts',(0.803236798652172,-1.50762352986116,0.389989721827216));
#7253=CARTESIAN_POINT('Ctrl Pts',(0.747221538722687,-1.53746753081382,0.386442718997914));
#7254=CARTESIAN_POINT('Ctrl Pts',(0.689602974465432,-1.56415244023765,0.382895716168612));
#7255=CARTESIAN_POINT('Ctrl Pts',(0.630775216567448,-1.58752659463213,0.37934871333931));
#7256=CARTESIAN_POINT('Ctrl Pts',(0.571947458669463,-1.61090074902661,0.375801710510008));
#7257=CARTESIAN_POINT('Ctrl Pts',(0.511911057953301,-1.63096403346254,0.372254707680706));
#7258=CARTESIAN_POINT('Ctrl Pts',(0.451074060683048,-1.64761957207327,0.368707704851404));
#7259=CARTESIAN_POINT('Ctrl Pts',(0.39141703555149,-1.66395206595139,0.365229498391125));
#7260=CARTESIAN_POINT('Ctrl Pts',(0.330753587029018,-1.67707267458142,0.361751291930846));
#7261=CARTESIAN_POINT('Ctrl Pts',(0.269461118854683,-1.68686358900937,0.358273085470567));
#7262=CARTESIAN_POINT('Ctrl Pts',(0.207821550461703,-1.6967099495409,0.35477518187198));
#7263=CARTESIAN_POINT('Ctrl Pts',(0.145546295250199,-1.70318857969946,0.351277278273392));
#7264=CARTESIAN_POINT('Ctrl Pts',(0.0830343380000198,-1.70623074676695,
0.347779374674805));
#7265=CARTESIAN_POINT('Ctrl Pts',(0.0210405334683055,-1.7092476977445,0.34431046470141));
#7266=CARTESIAN_POINT('Ctrl Pts',(-0.0411855506182593,-1.70888490210486,
0.340841554728015));
#7267=CARTESIAN_POINT('Ctrl Pts',(-0.103247405107285,-1.70512698525318,
0.337372644754621));
#7268=CARTESIAN_POINT('Ctrl Pts',(-0.16527243721957,-1.70137129803887,0.333905792945793));
#7269=CARTESIAN_POINT('Ctrl Pts',(-0.227132927953601,-1.69422451512892,
0.330438941136966));
#7270=CARTESIAN_POINT('Ctrl Pts',(-0.288433314930252,-1.68372333990426,
0.326972089328139));
#7271=CARTESIAN_POINT('Ctrl Pts',(-0.349719623106744,-1.67322457647428,
0.32350603374779));
#7272=CARTESIAN_POINT('Ctrl Pts',(-0.410445583517242,-1.65937303606351,
0.320039978167441));
#7273=CARTESIAN_POINT('Ctrl Pts',(-0.470223716325484,-1.64225689802328,
0.316573922587091));
#7274=CARTESIAN_POINT('Ctrl Pts',(-0.530947338740359,-1.62487004007491,
0.313053045630207));
#7275=CARTESIAN_POINT('Ctrl Pts',(-0.59069236084168,-1.60411452105231,0.309532168673322));
#7276=CARTESIAN_POINT('Ctrl Pts',(-0.649068730272986,-1.58013538846575,
0.306011291716437));
#7277=CARTESIAN_POINT('Ctrl Pts',(-0.706607885549984,-1.55650015649181,
0.302540909986519));
#7278=CARTESIAN_POINT('Ctrl Pts',(-0.76281695348608,-1.52973345901734,0.2990705282566));
#7279=CARTESIAN_POINT('Ctrl Pts',(-0.817345024185866,-1.50002172448888,
0.295600146526682));
#7280=CARTESIAN_POINT('Ctrl Pts',(-0.873063197669847,-1.46966151629298,
0.292054021956314));
#7281=CARTESIAN_POINT('Ctrl Pts',(-0.927025640249061,-1.43622646714311,
0.288507897385946));
#7282=CARTESIAN_POINT('Ctrl Pts',(-0.978889264302855,-1.39996209617711,
0.284961772815579));
#7283=CARTESIAN_POINT('Ctrl Pts',(-1.03075288835665,-1.36369772521112,0.281415648245212));
#7284=CARTESIAN_POINT('Ctrl Pts',(-1.08051729591951,-1.32460442841043,0.277869523674845));
#7285=CARTESIAN_POINT('Ctrl Pts',(-1.12787743525702,-1.28296942813851,0.274323399104477));
#7286=CARTESIAN_POINT('Ctrl Pts',(-1.17357665734752,-1.24279456482983,0.270901636910178));
#7287=CARTESIAN_POINT('Ctrl Pts',(-1.21723191867275,-1.20008209836666,0.267479874715879));
#7288=CARTESIAN_POINT('Ctrl Pts',(-1.25854224632262,-1.15507119984926,0.26405811252158));
#7289=CARTESIAN_POINT('Ctrl Pts',(-1.29979693760062,-1.11012092159877,0.260640958725344));
#7290=CARTESIAN_POINT('Ctrl Pts',(-1.33871259591333,-1.06287872191206,0.257223804929107));
#7291=CARTESIAN_POINT('Ctrl Pts',(-1.37502237771953,-1.01362296899318,0.253806651132871));
#7292=CARTESIAN_POINT('Ctrl Pts',(-1.41129748651945,-0.964414251472054,
0.250392760451671));
#7293=CARTESIAN_POINT('Ctrl Pts',(-1.44497133744224,-0.913196209067784,
0.246978869770472));
#7294=CARTESIAN_POINT('Ctrl Pts',(-1.47581648429232,-0.860281214017284,
0.243564979089273));
#7295=CARTESIAN_POINT('Ctrl Pts',(-1.5066442567653,-0.807396024792727,0.24015301137587));
#7296=CARTESIAN_POINT('Ctrl Pts',(-1.53464621965069,-0.752816229991685,
0.236741043662468));
#7297=CARTESIAN_POINT('Ctrl Pts',(-1.55963878132793,-0.696882295856296,
0.233329075949065));
#7298=CARTESIAN_POINT('Ctrl Pts',(-1.58464105438738,-0.640926627421706,
0.229915782444293));
#7299=CARTESIAN_POINT('Ctrl Pts',(-1.60663136275903,-0.583616242298273,
0.22650248893952));
#7300=CARTESIAN_POINT('Ctrl Pts',(-1.62547330244632,-0.525313816241554,
0.223089195434747));
#7301=CARTESIAN_POINT('Ctrl Pts',(-1.64431781150788,-0.467003439795662,
0.219675436477445));
#7302=CARTESIAN_POINT('Ctrl Pts',(-1.66001295147116,-0.407701258110916,
0.216261677520142));
#7303=CARTESIAN_POINT('Ctrl Pts',(-1.67247241601735,-0.347784531227456,
0.21284791856284));
#7304=CARTESIAN_POINT('Ctrl Pts',(-1.68495043832639,-0.287778561310758,
0.20942907497859));
#7305=CARTESIAN_POINT('Ctrl Pts',(-1.69418307027723,-0.227156736665851,
0.206010231394339));
#7306=CARTESIAN_POINT('Ctrl Pts',(-1.7001355219736,-0.166304748650061,0.202591387810089));
#7307=CARTESIAN_POINT('Ctrl Pts',(-1.70559156909977,-0.11052751075362,0.199457658606699));
#7308=CARTESIAN_POINT('Ctrl Pts',(-1.7082923284714,-0.0545572754673946,
0.196323929403309));
#7309=CARTESIAN_POINT('Ctrl Pts',(-1.70824949798349,0.00130963321928915,
0.193190200199919));
#7310=CARTESIAN_POINT('Origin',(0.,0.,-1.10921167016993));
#7311=CARTESIAN_POINT('',(-0.547737204315715,1.25137522550529,6.88122480138927));
#7312=CARTESIAN_POINT('Ctrl Pts',(-0.547737204315715,1.25137522550529,6.88122480138927));
#7313=CARTESIAN_POINT('Ctrl Pts',(-0.444055474973596,1.29675756919484,6.87281718727783));
#7314=CARTESIAN_POINT('Ctrl Pts',(-0.335108563083047,1.32909106151286,6.86411225202577));
#7315=CARTESIAN_POINT('Ctrl Pts',(-0.181200932842352,1.35460353714937,6.85259070631041));
#7316=CARTESIAN_POINT('Ctrl Pts',(-0.138706804541676,1.35961230506898,6.8494816326893));
#7317=CARTESIAN_POINT('Ctrl Pts',(-0.0793406683804811,1.36379669669384,
6.84523694577867));
#7318=CARTESIAN_POINT('Ctrl Pts',(-0.0626169567451756,1.36466682082695,
6.84405188852941));
#7319=CARTESIAN_POINT('Ctrl Pts',(-0.0335989507531258,1.36564201927298,
6.84201309110666));
#7320=CARTESIAN_POINT('Ctrl Pts',(-0.021311752806731,1.36588902936461,6.84115520326926));
#7321=CARTESIAN_POINT('Ctrl Pts',(0.00412667620511559,1.3660570558976,6.83938955340606));
#7322=CARTESIAN_POINT('Ctrl Pts',(0.0172768296389448,1.36595404051807,6.83848259871138));
#7323=CARTESIAN_POINT('Ctrl Pts',(0.0517693845442809,1.36518562446532,6.83611738802191));
#7324=CARTESIAN_POINT('Ctrl Pts',(0.0731017158663196,1.36420968961024,6.8346684173855));
#7325=CARTESIAN_POINT('Ctrl Pts',(0.190616964260844,1.35606882325948,6.8267458012817));
#7326=CARTESIAN_POINT('Ctrl Pts',(0.285855327828977,1.3392334421401,6.82056909451464));
#7327=CARTESIAN_POINT('Ctrl Pts',(0.4220909484288,1.29994245299497,6.81139842562418));
#7328=CARTESIAN_POINT('Ctrl Pts',(0.464994375680968,1.28522016509727,6.8084541018543));
#7329=CARTESIAN_POINT('Ctrl Pts',(0.531466214665467,1.2586457766578,6.80369400648833));
#7330=CARTESIAN_POINT('Ctrl Pts',(0.555560869782164,1.24819767870632,6.80192541601101));
#7331=CARTESIAN_POINT('Ctrl Pts',(0.588279607063654,1.23287493246639,6.79944399880338));
#7332=CARTESIAN_POINT('Ctrl Pts',(0.597175573755726,1.22859058079316,6.7987610043893));
#7333=CARTESIAN_POINT('Ctrl Pts',(0.612271321412319,1.22111769395799,6.79758643684037));
#7334=CARTESIAN_POINT('Ctrl Pts',(0.618494767536184,1.21797734531252,6.79709761695324));
#7335=CARTESIAN_POINT('Ctrl Pts',(0.631763955612415,1.21115379244051,6.79604501855935));
#7336=CARTESIAN_POINT('Ctrl Pts',(0.638801942834561,1.20745653106315,6.79548046141145));
#7337=CARTESIAN_POINT('Ctrl Pts',(0.659131988689208,1.19654907358243,6.79383226734929));
#7338=CARTESIAN_POINT('Ctrl Pts',(0.672336639391703,1.18917957435487,6.79273994674508));
#7339=CARTESIAN_POINT('Ctrl Pts',(0.746188488001,1.14633976986416,6.78651741449112));
#7340=CARTESIAN_POINT('Ctrl Pts',(0.804146072057655,1.10645361193097,6.78120229325178));
#7341=CARTESIAN_POINT('Ctrl Pts',(0.908653805019832,1.02196783577947,6.77104647106142));
#7342=CARTESIAN_POINT('Ctrl Pts',(0.955635717510016,0.978177759687796,6.76621672168241));
#7343=CARTESIAN_POINT('Ctrl Pts',(1.02616944010302,0.902484174838384,6.75860017586617));
#7344=CARTESIAN_POINT('Ctrl Pts',(1.0517174803317,0.872577950102533,6.75574862906286));
#7345=CARTESIAN_POINT('Ctrl Pts',(1.08589247066364,0.828887433979547,6.75179622020007));
#7346=CARTESIAN_POINT('Ctrl Pts',(1.09561690389833,0.815990487313167,6.75065405063617));
#7347=CARTESIAN_POINT('Ctrl Pts',(1.11220629378608,0.793157540214015,6.74867333090079));
#7348=CARTESIAN_POINT('Ctrl Pts',(1.11917230506538,0.783297575307153,6.747831050253));
#7349=CARTESIAN_POINT('Ctrl Pts',(1.13342987687498,0.762538279518553,6.74608401406562));
#7350=CARTESIAN_POINT('Ctrl Pts',(1.14069707302286,0.751623656841593,6.7451802174939));
#7351=CARTESIAN_POINT('Ctrl Pts',(1.15957263621349,0.722369916348837,6.74279520509396));
#7352=CARTESIAN_POINT('Ctrl Pts',(1.17090330182126,0.703855481007286,6.74132399678973));
#7353=CARTESIAN_POINT('Ctrl Pts',(1.23174853529083,0.598894886043928,6.73317681849201));
#7354=CARTESIAN_POINT('Ctrl Pts',(1.27213241774242,0.507504613871995,6.72682833630085));
#7355=CARTESIAN_POINT('Ctrl Pts',(1.31650773539199,0.36742581360311,6.71737009128827));
#7356=CARTESIAN_POINT('Ctrl Pts',(1.32844184238847,0.321614716899254,6.71431170350496));
#7357=CARTESIAN_POINT('Ctrl Pts',(1.34171051078477,0.257123565763821,6.70994545798023));
#7358=CARTESIAN_POINT('Ctrl Pts',(1.34507599310962,0.238893546980178,6.70870449104615));
#7359=CARTESIAN_POINT('Ctrl Pts',(1.35035718418356,0.206620841289652,6.70648689448736));
#7360=CARTESIAN_POINT('Ctrl Pts',(1.3524272967231,0.19260598292506,6.70551703664031));
#7361=CARTESIAN_POINT('Ctrl Pts',(1.35528668381136,0.170919373947805,6.70400223335901));
#7362=CARTESIAN_POINT('Ctrl Pts',(1.35622964181346,0.16326842634506,6.70346512861712));
#7363=CARTESIAN_POINT('Ctrl Pts',(1.35788104280237,0.148866222001141,6.70244833728836));
#7364=CARTESIAN_POINT('Ctrl Pts',(1.358603993953,0.142117056891211,6.70196942000449));
#7365=CARTESIAN_POINT('Ctrl Pts',(1.36023955539263,0.125693210825868,6.70079834020808));
#7366=CARTESIAN_POINT('Ctrl Pts',(1.36109926562933,0.116013819553316,6.70010345493855));
#7367=CARTESIAN_POINT('Ctrl Pts',(1.36378012987047,0.0816766431119194,6.69762359453806));
#7368=CARTESIAN_POINT('Ctrl Pts',(1.3650349135384,0.0569808877648533,6.69581311537244));
#7369=CARTESIAN_POINT('Ctrl Pts',(1.36747715358494,-0.046381986422803,6.68815751231844));
#7370=CARTESIAN_POINT('Ctrl Pts',(1.36253775704882,-0.125041302655787,6.6821529400915));
#7371=CARTESIAN_POINT('Ctrl Pts',(1.33978057399129,-0.276600634351956,6.67060515621317));
#7372=CARTESIAN_POINT('Ctrl Pts',(1.3226798455,-0.349343878997171,6.66507322849514));
#7373=CARTESIAN_POINT('Ctrl Pts',(1.29387729252783,-0.438404063292854,6.65836244419621));
#7374=CARTESIAN_POINT('Ctrl Pts',(1.28765787036867,-0.456348380546274,6.65701294683789));
#7375=CARTESIAN_POINT('Ctrl Pts',(1.27673948944134,-0.485847337380051,6.65479769760526));
#7376=CARTESIAN_POINT('Ctrl Pts',(1.27225303688697,-0.497477223193274,6.65392517179943));
#7377=CARTESIAN_POINT('Ctrl Pts',(1.26312380975889,-0.520210564038238,6.65222061199698));
#7378=CARTESIAN_POINT('Ctrl Pts',(1.25849225947018,-0.531317267461592,6.6513882990959));
#7379=CARTESIAN_POINT('Ctrl Pts',(1.24792131460961,-0.555752893250382,6.6495573522297));
#7380=CARTESIAN_POINT('Ctrl Pts',(1.24191384743358,-0.569050884201948,6.64856108504092));
#7381=CARTESIAN_POINT('Ctrl Pts',(1.21965528737674,-0.616289615053219,6.64501948766852));
#7382=CARTESIAN_POINT('Ctrl Pts',(1.20221571569978,-0.649653501749628,6.64251392485358));
#7383=CARTESIAN_POINT('Ctrl Pts',(1.11883228547365,-0.79428748449609,6.63154375565138));
#7384=CARTESIAN_POINT('Ctrl Pts',(1.03867526544744,-0.896562574527913,6.6235514454688));
#7385=CARTESIAN_POINT('Ctrl Pts',(0.930589519284609,-1.00018866743715,6.6135292465496));
#7386=CARTESIAN_POINT('Ctrl Pts',(0.915512462838768,-1.01400741890669,6.6121437847811));
#7387=CARTESIAN_POINT('Ctrl Pts',(0.893495140935552,-1.03329583617809,6.61012830546018));
#7388=CARTESIAN_POINT('Ctrl Pts',(0.886802401097707,-1.03904539970548,6.60951663296651));
#7389=CARTESIAN_POINT('Ctrl Pts',(0.875427741473142,-1.04862713546565,6.60847777138842));
#7390=CARTESIAN_POINT('Ctrl Pts',(0.870775270048772,-1.05249371780724,6.60805301974325));
#7391=CARTESIAN_POINT('Ctrl Pts',(0.859958841950382,-1.06136223733428,6.60706575744925));
#7392=CARTESIAN_POINT('Ctrl Pts',(0.853776972137215,-1.06634135366425,6.60650176016272));
#7393=CARTESIAN_POINT('Ctrl Pts',(0.835904612804853,-1.0804814051409,6.60487273376766));
#7394=CARTESIAN_POINT('Ctrl Pts',(0.824108033693321,-1.08950561822569,6.60379937489742));
#7395=CARTESIAN_POINT('Ctrl Pts',(0.764459048151997,-1.13361324016885,6.59839038343062));
#7396=CARTESIAN_POINT('Ctrl Pts',(0.71450708418842,-1.16574224508069,6.59392164862438));
#7397=CARTESIAN_POINT('Ctrl Pts',(0.599224813697061,-1.22969222547908,6.58395374840633));
#7398=CARTESIAN_POINT('Ctrl Pts',(0.533114025374813,-1.25976367082325,6.57846521073137));
#7399=CARTESIAN_POINT('Ctrl Pts',(0.425337394258642,-1.29877501379294,6.57000324915296));
#7400=CARTESIAN_POINT('Ctrl Pts',(0.385106074064548,-1.31126747803365,6.56694293905821));
#7401=CARTESIAN_POINT('Ctrl Pts',(0.328382092306131,-1.32604440020571,6.56276279052938));
#7402=CARTESIAN_POINT('Ctrl Pts',(0.312331474880023,-1.32991640411673,6.56159452039775));
#7403=CARTESIAN_POINT('Ctrl Pts',(0.284394900029043,-1.33612204680169,6.55958523991947));
#7404=CARTESIAN_POINT('Ctrl Pts',(0.272541129647848,-1.3385902779876,6.55874012991516));
#7405=CARTESIAN_POINT('Ctrl Pts',(0.247959032714924,-1.3433687567822,6.55700224499999));
#7406=CARTESIAN_POINT('Ctrl Pts',(0.235227525636655,-1.34565646782956,6.55611024625341));
#7407=CARTESIAN_POINT('Ctrl Pts',(0.201835883054979,-1.35116817387901,6.55379051031716));
#7408=CARTESIAN_POINT('Ctrl Pts',(0.181130397009088,-1.35409933680979,6.55237181185296));
#7409=CARTESIAN_POINT('Ctrl Pts',(0.0573245200133942,-1.36873502905124,
6.54398948635327));
#7410=CARTESIAN_POINT('Ctrl Pts',(-0.0467682713600107,-1.36913718191617,
6.53738834890233));
#7411=CARTESIAN_POINT('Ctrl Pts',(-0.193737416610724,-1.35291022430366,
6.52785222370281));
#7412=CARTESIAN_POINT('Ctrl Pts',(-0.237302096321603,-1.34595225351311,
6.52499278431376));
#7413=CARTESIAN_POINT('Ctrl Pts',(-0.305717043762331,-1.33160037489074,
6.52034896384995));
#7414=CARTESIAN_POINT('Ctrl Pts',(-0.3308259542693,-1.32558532599812,6.51861100259614));
#7415=CARTESIAN_POINT('Ctrl Pts',(-0.365093904570292,-1.31634195917769,
6.51617372705014));
#7416=CARTESIAN_POINT('Ctrl Pts',(-0.374412981246757,-1.31372166704474,
6.51550417736877));
#7417=CARTESIAN_POINT('Ctrl Pts',(-0.390252564147855,-1.30908575212468,
6.51435337834624));
#7418=CARTESIAN_POINT('Ctrl Pts',(-0.396787196556692,-1.3071199213282,6.51387486167448));
#7419=CARTESIAN_POINT('Ctrl Pts',(-0.410761282430147,-1.30280161206176,
6.51284309939162));
#7420=CARTESIAN_POINT('Ctrl Pts',(-0.41819539404998,-1.30043434140424,6.51228911234275));
#7421=CARTESIAN_POINT('Ctrl Pts',(-0.43909712741647,-1.29358077245566,6.51071789339233));
#7422=CARTESIAN_POINT('Ctrl Pts',(-0.452515254216709,-1.28894817855045,
6.50969318499319));
#7423=CARTESIAN_POINT('Ctrl Pts',(-0.558815381398263,-1.25038382966089,
6.50145965743748));
#7424=CARTESIAN_POINT('Ctrl Pts',(-0.647830599009339,-1.20666826675332,
6.49388108254749));
#7425=CARTESIAN_POINT('Ctrl Pts',(-0.786348944914703,-1.11886225427749,
6.48154920476506));
#7426=CARTESIAN_POINT('Ctrl Pts',(-0.838796995776625,-1.08010143497704,
6.47672399020658));
#7427=CARTESIAN_POINT('Ctrl Pts',(-0.904636482967574,-1.02374415881705,
6.47048323590923));
#7428=CARTESIAN_POINT('Ctrl Pts',(-0.920655554718127,-1.00936252734762,
6.46894826253573));
#7429=CARTESIAN_POINT('Ctrl Pts',(-0.945821840723968,-0.985670851127824,
6.46650821723242));
#7430=CARTESIAN_POINT('Ctrl Pts',(-0.955186645712328,-0.976598419951707,
6.46559354564364));
#7431=CARTESIAN_POINT('Ctrl Pts',(-0.972935791576037,-0.958903813543366,
6.46384624658676));
#7432=CARTESIAN_POINT('Ctrl Pts',(-0.981338931448249,-0.95030231812153,
6.4630128496364));
#7433=CARTESIAN_POINT('Ctrl Pts',(-1.00054117584257,-0.93012043771098,6.4610931195179));
#7434=CARTESIAN_POINT('Ctrl Pts',(-1.0112548276038,-0.918460876587213,6.46001042243936));
#7435=CARTESIAN_POINT('Ctrl Pts',(-1.04531087051077,-0.880079488115456,
6.45652700759092));
#7436=CARTESIAN_POINT('Ctrl Pts',(-1.06781655698413,-0.852632893999194,
6.4541594263214));
#7437=CARTESIAN_POINT('Ctrl Pts',(-1.16850257324679,-0.71959277086434,6.44316659660916));
#7438=CARTESIAN_POINT('Ctrl Pts',(-1.23224079855161,-0.603976015019015,
6.43504592501645));
#7439=CARTESIAN_POINT('Ctrl Pts',(-1.28575916397003,-0.46174153678167,6.42487262525093));
#7440=CARTESIAN_POINT('Ctrl Pts',(-1.29258758701473,-0.442265863486875,
6.42347441551532));
#7441=CARTESIAN_POINT('Ctrl Pts',(-1.30172338697076,-0.414187532268361,
6.42144113458031));
#7442=CARTESIAN_POINT('Ctrl Pts',(-1.30439220737305,-0.40570438321826,6.42082457909091));
#7443=CARTESIAN_POINT('Ctrl Pts',(-1.30874482811647,-0.391382038252033,
6.41977889754312));
#7444=CARTESIAN_POINT('Ctrl Pts',(-1.31047281802553,-0.385556631417649,
6.41935224775471));
#7445=CARTESIAN_POINT('Ctrl Pts',(-1.31436706645888,-0.372099640699887,
6.41836338156362));
#7446=CARTESIAN_POINT('Ctrl Pts',(-1.31650570863623,-0.364460751156839,
6.4177997065548));
#7447=CARTESIAN_POINT('Ctrl Pts',(-1.3224595694033,-0.342458112451721,6.41617024721395));
#7448=CARTESIAN_POINT('Ctrl Pts',(-1.32610693607016,-0.328050636719565,
6.41509610514067));
#7449=CARTESIAN_POINT('Ctrl Pts',(-1.34502775195454,-0.247831913845801,
6.40908613189534));
#7450=CARTESIAN_POINT('Ctrl Pts',(-1.35563628089949,-0.181022156970859,
6.40397686935053));
#7451=CARTESIAN_POINT('Ctrl Pts',(-1.36873956463937,-0.0241564204154046,
6.39206829691884));
#7452=CARTESIAN_POINT('Ctrl Pts',(-1.36736595253409,0.0659287662872278,
6.38530757367569));
#7453=CARTESIAN_POINT('Ctrl Pts',(-1.35435234407392,0.179699755680297,6.37702130393148));
#7454=CARTESIAN_POINT('Ctrl Pts',(-1.35089308083831,0.204084043171095,6.37525875774045));
#7455=CARTESIAN_POINT('Ctrl Pts',(-1.34449507938174,0.241816421596295,6.37255067299858));
#7456=CARTESIAN_POINT('Ctrl Pts',(-1.34201234030731,0.255235386774298,6.37159138250401));
#7457=CARTESIAN_POINT('Ctrl Pts',(-1.33699345692545,0.280259778058949,6.36980885250657));
#7458=CARTESIAN_POINT('Ctrl Pts',(-1.33450623065413,0.291873573576734,6.36898418130947));
#7459=CARTESIAN_POINT('Ctrl Pts',(-1.32855036073377,0.318014066022518,6.36713310918047));
#7460=CARTESIAN_POINT('Ctrl Pts',(-1.3249942881647,0.332519432817389,6.36610954342743));
#7461=CARTESIAN_POINT('Ctrl Pts',(-1.31315609531256,0.377597967257694,6.36293715588306));
#7462=CARTESIAN_POINT('Ctrl Pts',(-1.30404781334725,0.407944483190907,6.36081417736566));
#7463=CARTESIAN_POINT('Ctrl Pts',(-1.25775384022177,0.54471708888294,6.35125293892159));
#7464=CARTESIAN_POINT('Ctrl Pts',(-1.20854286930759,0.646594109476209,6.34418992000542));
#7465=CARTESIAN_POINT('Ctrl Pts',(-1.14737960347042,0.741266514514222,6.33682691740051));
#7466=CARTESIAN_POINT('',(0.995642551412613,0.935228266155693,6.88122480138927));
#7467=CARTESIAN_POINT('Origin',(0.,0.,6.88122480138927));
#7468=CARTESIAN_POINT('',(-1.36599994346263,0.000393014108642856,6.50921167020825));
#7469=CARTESIAN_POINT('Ctrl Pts',(-1.36599994346263,0.000393014108642897,
6.50921167020824));
#7470=CARTESIAN_POINT('Ctrl Pts',(-1.36601509581434,-0.0522720457987859,
6.51291417912242));
#7471=CARTESIAN_POINT('Ctrl Pts',(-1.36298002712899,-0.105055605456886,
6.5166166880366));
#7472=CARTESIAN_POINT('Ctrl Pts',(-1.35688129899332,-0.15757265131422,6.52031919695078));
#7473=CARTESIAN_POINT('Ctrl Pts',(-1.35087780158986,-0.209269651316286,
6.52396389173928));
#7474=CARTESIAN_POINT('Ctrl Pts',(-1.34190568289767,-0.260707838473859,
6.52760858652779));
#7475=CARTESIAN_POINT('Ctrl Pts',(-1.33000442155041,-0.311519242834772,
6.53125328131629));
#7476=CARTESIAN_POINT('Ctrl Pts',(-1.31811417516861,-0.362283619754845,
6.53489460283317));
#7477=CARTESIAN_POINT('Ctrl Pts',(-1.30330027692159,-0.412421833881958,
6.53853592435005));
#7478=CARTESIAN_POINT('Ctrl Pts',(-1.28565356051786,-0.461574395225452,
6.54217724586693));
#7479=CARTESIAN_POINT('Ctrl Pts',(-1.26801571849919,-0.51070223815982,6.54581673619389));
#7480=CARTESIAN_POINT('Ctrl Pts',(-1.24754806506583,-0.558844898258482,
6.54945622652084));
#7481=CARTESIAN_POINT('Ctrl Pts',(-1.22439101530232,-0.605658849226993,
6.5530957168478));
#7482=CARTESIAN_POINT('Ctrl Pts',(-1.20054346040706,-0.653868715206742,
6.55684373078952));
#7483=CARTESIAN_POINT('Ctrl Pts',(-1.17384374886831,-0.700668785653974,
6.56059174473125));
#7484=CARTESIAN_POINT('Ctrl Pts',(-1.14449700594271,-0.745709463120968,
6.56433975867297));
#7485=CARTESIAN_POINT('Ctrl Pts',(-1.11597450395673,-0.789485115354654,
6.56798250483282));
#7486=CARTESIAN_POINT('Ctrl Pts',(-1.08495211768822,-0.831598503119688,
6.57162525099267));
#7487=CARTESIAN_POINT('Ctrl Pts',(-1.05166136614232,-0.871759353814842,
6.57526799715252));
#7488=CARTESIAN_POINT('Ctrl Pts',(-1.01692756445579,-0.913661051999237,
6.57906864498518));
#7489=CARTESIAN_POINT('Ctrl Pts',(-0.979724640210714,-0.953436539582381,
6.58286929281784));
#7490=CARTESIAN_POINT('Ctrl Pts',(-0.940358579361482,-0.990798537655993,
6.5866699406505));
#7491=CARTESIAN_POINT('Ctrl Pts',(-0.900992518512251,-1.02816053572961,
6.59047058848316));
#7492=CARTESIAN_POINT('Ctrl Pts',(-0.859463877262655,-1.06310867126732,
6.59427123631583));
#7493=CARTESIAN_POINT('Ctrl Pts',(-0.816114854989169,-1.09540519601927,
6.59807188414849));
#7494=CARTESIAN_POINT('Ctrl Pts',(-0.774111632074759,-1.12669905358215,
6.60175453832988));
#7495=CARTESIAN_POINT('Ctrl Pts',(-0.730220153355013,-1.15563740902186,
6.60543719251126));
#7496=CARTESIAN_POINT('Ctrl Pts',(-0.684734362040178,-1.1819876705962,6.60911984669265));
#7497=CARTESIAN_POINT('Ctrl Pts',(-0.639327745912801,-1.20829206538798,
6.61279609063412));
#7498=CARTESIAN_POINT('Ctrl Pts',(-0.592332782989818,-1.23201703962708,
6.61647233457559));
#7499=CARTESIAN_POINT('Ctrl Pts',(-0.544073299409954,-1.25297256349418,
6.62014857851706));
#7500=CARTESIAN_POINT('Ctrl Pts',(-0.495860259417331,-1.27390792034686,
6.62382128454342));
#7501=CARTESIAN_POINT('Ctrl Pts',(-0.446385597455214,-1.2920788943395,6.62749399056977));
#7502=CARTESIAN_POINT('Ctrl Pts',(-0.395996943868893,-1.30734173820256,
6.63116669659613));
#7503=CARTESIAN_POINT('Ctrl Pts',(-0.345636451000062,-1.32259605211685,
6.6348373500565));
#7504=CARTESIAN_POINT('Ctrl Pts',(-0.294363489648552,-1.33494530272762,
6.63850800351686));
#7505=CARTESIAN_POINT('Ctrl Pts',(-0.242542566451201,-1.34429502099028,
6.64217865697723));
#7506=CARTESIAN_POINT('Ctrl Pts',(-0.190729696309135,-1.3536432862916,6.64584874001211));
#7507=CARTESIAN_POINT('Ctrl Pts',(-0.138369559335716,-1.35999285101895,
6.64951882304699));
#7508=CARTESIAN_POINT('Ctrl Pts',(-0.0858362412672093,-1.36330045833085,
6.65318890608187));
#7509=CARTESIAN_POINT('Ctrl Pts',(-0.0332532529394221,-1.36661119298591,
6.65686245918075));
#7510=CARTESIAN_POINT('Ctrl Pts',(0.0195027089561627,-1.36687419367247,
6.66053601227963));
#7511=CARTESIAN_POINT('Ctrl Pts',(0.0720546955455641,-1.36409828122824,
6.66420956537851));
#7512=CARTESIAN_POINT('Ctrl Pts',(0.124633440876391,-1.36132095532796,6.66788498899959));
#7513=CARTESIAN_POINT('Ctrl Pts',(0.177007472065912,-1.35550169225283,6.67156041262067));
#7514=CARTESIAN_POINT('Ctrl Pts',(0.228805481142311,-1.34670117390579,6.67523583624175));
#7515=CARTESIAN_POINT('Ctrl Pts',(0.280697525684336,-1.33788467886669,6.67891793232337));
#7516=CARTESIAN_POINT('Ctrl Pts',(0.33201093872555,-1.32607624239086,6.68260002840499));
#7517=CARTESIAN_POINT('Ctrl Pts',(0.382386508246656,-1.31138726481194,6.68628212448661));
#7518=CARTESIAN_POINT('Ctrl Pts',(0.410542758955961,-1.30317720308346,6.68834014628955));
#7519=CARTESIAN_POINT('Ctrl Pts',(0.438406326130136,-1.294068154454,6.69039816809249));
#7520=CARTESIAN_POINT('Ctrl Pts',(0.465917295775467,-1.28408608492471,6.69245618989542));
#7521=CARTESIAN_POINT('Ctrl Pts',(0.514537992252857,-1.26644457031957,6.69609337370662));
#7522=CARTESIAN_POINT('Ctrl Pts',(0.562270734526597,-1.2459956382712,6.69973055751783));
#7523=CARTESIAN_POINT('Ctrl Pts',(0.608765467660196,-1.22284937968029,6.70336774132903));
#7524=CARTESIAN_POINT('Ctrl Pts',(0.655177339783475,-1.19974437140404,6.70699844310011));
#7525=CARTESIAN_POINT('Ctrl Pts',(0.700355089214269,-1.17395180847786,6.7106291448712));
#7526=CARTESIAN_POINT('Ctrl Pts',(0.743967007168403,-1.14563043440932,6.71425984664229));
#7527=CARTESIAN_POINT('Ctrl Pts',(0.787536231813736,-1.11733678517439,6.71788699418602));
#7528=CARTESIAN_POINT('Ctrl Pts',(0.829542199504999,-1.08651952047162,6.72151414172975));
#7529=CARTESIAN_POINT('Ctrl Pts',(0.869678231376943,-1.05338301385065,6.72514128927348));
#7530=CARTESIAN_POINT('Ctrl Pts',(0.909792204127563,-1.02026471934945,6.72876644330454));
#7531=CARTESIAN_POINT('Ctrl Pts',(0.948037853104004,-0.984830055780476,
6.73239159733561));
#7532=CARTESIAN_POINT('Ctrl Pts',(0.984140051541839,-0.947324843414985,
6.73601675136667));
#7533=CARTESIAN_POINT('Ctrl Pts',(1.02023790633019,-0.909824143503118,6.73964146923598));
#7534=CARTESIAN_POINT('Ctrl Pts',(1.0541924424754,-0.870253785592282,6.74326618710529));
#7535=CARTESIAN_POINT('Ctrl Pts',(1.0857658945044,-0.828895905606408,6.7468909049746));
#7536=CARTESIAN_POINT('Ctrl Pts',(1.11737436806205,-0.787492151125154,6.75051964341031));
#7537=CARTESIAN_POINT('Ctrl Pts',(1.14659615148461,-0.744297354419688,6.75414838184603));
#7538=CARTESIAN_POINT('Ctrl Pts',(1.1732353468568,-0.699624771492414,6.75777712028175));
#7539=CARTESIAN_POINT('Ctrl Pts',(1.19988999970509,-0.65492626715971,6.76140796430426));
#7540=CARTESIAN_POINT('Ctrl Pts',(1.22395883083609,-0.608748759074452,6.76503880832676));
#7541=CARTESIAN_POINT('Ctrl Pts',(1.2452924679255,-0.56142913117152,6.76866965234926));
#7542=CARTESIAN_POINT('Ctrl Pts',(1.26667062895704,-0.514010745782216,6.77230807405242));
#7543=CARTESIAN_POINT('Ctrl Pts',(1.28530200708757,-0.465445996734002,6.77594649575558));
#7544=CARTESIAN_POINT('Ctrl Pts',(1.30108634062948,-0.416089334431191,6.77958491745874));
#7545=CARTESIAN_POINT('Ctrl Pts',(1.31157847846954,-0.383281050012264,6.78200344351994));
#7546=CARTESIAN_POINT('Ctrl Pts',(1.32081369083876,-0.350123165431055,6.78442196958114));
#7547=CARTESIAN_POINT('Ctrl Pts',(1.32877511797438,-0.316721779882873,6.78684049564234));
#7548=CARTESIAN_POINT('Ctrl Pts',(1.34172091212639,-0.262408972099444,6.79077317504847));
#7549=CARTESIAN_POINT('Ctrl Pts',(1.35135491722136,-0.207204138267393,6.79470585445459));
#7550=CARTESIAN_POINT('Ctrl Pts',(1.35756883720119,-0.15153498691791,6.79863853386071));
#7551=CARTESIAN_POINT('Ctrl Pts',(1.36352526533053,-0.0981726487946194,
6.80240825125558));
#7552=CARTESIAN_POINT('Ctrl Pts',(1.36633940003821,-0.044384275270335,6.80617796865046));
#7553=CARTESIAN_POINT('Ctrl Pts',(1.36596737288208,0.00944119810278521,
6.80994768604533));
#7554=CARTESIAN_POINT('Ctrl Pts',(1.3655958134874,0.063198995016105,6.81371266365601));
#7555=CARTESIAN_POINT('Ctrl Pts',(1.36204604684839,0.116993301466068,6.81747764126669));
#7556=CARTESIAN_POINT('Ctrl Pts',(1.35532611850322,0.170432134596119,6.82124261887738));
#7557=CARTESIAN_POINT('Ctrl Pts',(1.34861248442448,0.223820913880939,6.82500406999626));
#7558=CARTESIAN_POINT('Ctrl Pts',(1.33873464674067,0.276854385991406,6.82876552111515));
#7559=CARTESIAN_POINT('Ctrl Pts',(1.32575254381536,0.329144637761449,6.83252697223403));
#7560=CARTESIAN_POINT('Ctrl Pts',(1.31277844339189,0.381402656476579,6.83628610469779));
#7561=CARTESIAN_POINT('Ctrl Pts',(1.29670399995535,0.432917880211148,6.84004523716155));
#7562=CARTESIAN_POINT('Ctrl Pts',(1.27764003146218,0.483313511093276,6.84380436962531));
#7563=CARTESIAN_POINT('Ctrl Pts',(1.25857628906331,0.533708544294783,6.84756345750662));
#7564=CARTESIAN_POINT('Ctrl Pts',(1.2365232586372,0.582983539062316,6.85132254538793));
#7565=CARTESIAN_POINT('Ctrl Pts',(1.21164079598937,0.630779344536778,6.85508163326924));
#7566=CARTESIAN_POINT('Ctrl Pts',(1.18675908331869,0.678573709407772,6.85884060784866));
#7567=CARTESIAN_POINT('Ctrl Pts',(1.15904834615365,0.724888533338292,6.86259958242808));
#7568=CARTESIAN_POINT('Ctrl Pts',(1.12871443519632,0.769389188759139,6.8663585570075));
#7569=CARTESIAN_POINT('Ctrl Pts',(1.09835975702567,0.813920310235141,6.87012010505748));
#7570=CARTESIAN_POINT('Ctrl Pts',(1.0653786097342,0.856634375336335,6.87388165310747));
#7571=CARTESIAN_POINT('Ctrl Pts',(1.03001932871992,0.897226940335258,6.87764320115746));
#7572=CARTESIAN_POINT('Ctrl Pts',(1.01879674984241,0.910110495924438,6.87883706790139));
#7573=CARTESIAN_POINT('Ctrl Pts',(1.00733490922091,0.922780600295316,6.88003093464533));
#7574=CARTESIAN_POINT('Ctrl Pts',(0.995642551412613,0.935228266155693,6.88122480138927));
#7575=CARTESIAN_POINT('Ctrl Pts',(-1.36599996455079,0.000311202912832261,
6.50809119519899));
#7576=CARTESIAN_POINT('Ctrl Pts',(-1.36599754429993,0.0109346978751973,
6.50731552338978));
#7577=CARTESIAN_POINT('Ctrl Pts',(-1.3658711942542,0.0215582237833071,6.50654460410721));
#7578=CARTESIAN_POINT('Ctrl Pts',(-1.36540521978107,0.0413330020605039,
6.50511969138689));
#7579=CARTESIAN_POINT('Ctrl Pts',(-1.36509749686988,0.0504843237358567,
6.50446429910442));
#7580=CARTESIAN_POINT('Ctrl Pts',(-1.36442613075401,0.065848712042639,6.50337144265674));
#7581=CARTESIAN_POINT('Ctrl Pts',(-1.36411201052067,0.0720634853177237,
6.50293145367623));
#7582=CARTESIAN_POINT('Ctrl Pts',(-1.36334680897726,0.0853951199963837,
6.50199233947414));
#7583=CARTESIAN_POINT('Ctrl Pts',(-1.36288244499507,0.0925110488199359,
6.50149398442202));
#7584=CARTESIAN_POINT('Ctrl Pts',(-1.36151936875785,0.111151324983536,6.50019539616074));
#7585=CARTESIAN_POINT('Ctrl Pts',(-1.36053004394861,0.122668784287314,6.49939990292469));
#7586=CARTESIAN_POINT('Ctrl Pts',(-1.35506128540604,0.178076452606176,6.49560011419122));
#7587=CARTESIAN_POINT('Ctrl Pts',(-1.34860313287363,0.221749230337503,6.49268687248508));
#7588=CARTESIAN_POINT('Ctrl Pts',(-1.32095139951885,0.361557908053979,6.48340854333537));
#7589=CARTESIAN_POINT('Ctrl Pts',(-1.29148954239672,0.455732446889767,6.4772123244871));
#7590=CARTESIAN_POINT('Ctrl Pts',(-1.23672911706547,0.581333874140369,6.46820920164614));
#7591=CARTESIAN_POINT('Ctrl Pts',(-1.21979842017135,0.616067672157524,6.46563716173223));
#7592=CARTESIAN_POINT('Ctrl Pts',(-1.19382967997553,0.664064090731224,6.46193362099985));
#7593=CARTESIAN_POINT('Ctrl Pts',(-1.18599445445098,0.677958361132938,6.46084315922013));
#7594=CARTESIAN_POINT('Ctrl Pts',(-1.17187685057423,0.701999270083489,6.45892207678362));
#7595=CARTESIAN_POINT('Ctrl Pts',(-1.16570136031198,0.71220688770795,6.45809531679904));
#7596=CARTESIAN_POINT('Ctrl Pts',(-1.1554403742083,0.728676483761021,6.45674261975205));
#7597=CARTESIAN_POINT('Ctrl Pts',(-1.15143572786607,0.734988186398318,6.45621965924215));
#7598=CARTESIAN_POINT('Ctrl Pts',(-1.14737960337948,0.741266514654979,6.45569480720057));
#7599=CARTESIAN_POINT('Ctrl Pts',(-0.595951749398983,1.22654481333082,-0.198948690821724));
#7600=CARTESIAN_POINT('Ctrl Pts',(-1.0000533487054,1.03020053595575,-0.167487255572748));
#7601=CARTESIAN_POINT('Ctrl Pts',(-1.59252126055165,0.210609571278056,-0.104564385074798));
#7602=CARTESIAN_POINT('Ctrl Pts',(-1.0508036035899,-1.21692831989964,-0.0101800793278729));
#7603=CARTESIAN_POINT('Ctrl Pts',(0.437846824792563,-1.54552130761885,0.0842042264190528));
#7604=CARTESIAN_POINT('Ctrl Pts',(1.53180658334325,-0.485155857487698,0.178588532165979));
#7605=CARTESIAN_POINT('Ctrl Pts',(1.24759243572345,1.01280491202726,0.272972837912904));
#7606=CARTESIAN_POINT('Ctrl Pts',(-0.159548416134459,1.59879372907719,0.36735714365983));
#7607=CARTESIAN_POINT('Ctrl Pts',(-1.42301181748291,0.746252543525721,0.461741449406754));
#7608=CARTESIAN_POINT('Ctrl Pts',(-1.40591424239536,-0.778006731171808,
0.556125755153681));
#7609=CARTESIAN_POINT('Ctrl Pts',(-0.123566114012858,-1.60203927132338,
0.650510060900605));
#7610=CARTESIAN_POINT('Ctrl Pts',(1.26996906566004,-0.98438823499133,0.744894366647532));
#7611=CARTESIAN_POINT('Ctrl Pts',(1.52062832125674,0.519164000491415,0.839278672394458));
#7612=CARTESIAN_POINT('Ctrl Pts',(0.402824829336517,1.55549410206089,0.933662978141383));
#7613=CARTESIAN_POINT('Ctrl Pts',(-1.0774907814505,1.19199423922429,1.02804728388831));
#7614=CARTESIAN_POINT('Ctrl Pts',(-1.58814124060392,-0.244219928936947,
1.12243158963524));
#7615=CARTESIAN_POINT('Ctrl Pts',(-0.669575311644667,-1.46065169016511,
1.21681589538216));
#7616=CARTESIAN_POINT('Ctrl Pts',(0.851561190150558,-1.36260011027521,1.31120020112909));
#7617=CARTESIAN_POINT('Ctrl Pts',(1.60635244239379,-0.0383034713654621,
1.40558450687601));
#7618=CARTESIAN_POINT('Ctrl Pts',(0.915538973494178,1.32046337807201,1.49996881262294));
#7619=CARTESIAN_POINT('Ctrl Pts',(-0.599195377524483,1.49090583294604,1.59435311836986));
#7620=CARTESIAN_POINT('Ctrl Pts',(-1.57469589658012,0.319637442586392,1.68873742411679));
#7621=CARTESIAN_POINT('Ctrl Pts',(-1.13308043611877,-1.13928221574075,1.78312172986372));
#7622=CARTESIAN_POINT('Ctrl Pts',(0.328228015712479,-1.57292772700279,1.87750603561064));
#7623=CARTESIAN_POINT('Ctrl Pts',(1.49415425557531,-0.591048489903462,1.97189034135757));
#7624=CARTESIAN_POINT('Ctrl Pts',(1.31544635921791,0.922732968463878,2.06627464710449));
#7625=CARTESIAN_POINT('Ctrl Pts',(-0.0470710861353782,1.60611941371602,
2.16065895285142));
#7626=CARTESIAN_POINT('Ctrl Pts',(-1.36722785270736,0.844110926180164,2.25504325859834));
#7627=CARTESIAN_POINT('Ctrl Pts',(-1.45697535334287,-0.677538247307762,
2.34942756434527));
#7628=CARTESIAN_POINT('Ctrl Pts',(-0.235547126457103,-1.58945047373708,
2.4438118700922));
#7629=CARTESIAN_POINT('Ctrl Pts',(1.19785700950514,-1.07096864650801,2.53819617583912));
#7630=CARTESIAN_POINT('Ctrl Pts',(1.55327377079637,0.411309919633114,2.63258048158605));
#7631=CARTESIAN_POINT('Ctrl Pts',(0.510852976384489,1.52343837867101,2.72696478733295));
#7632=CARTESIAN_POINT('Ctrl Pts',(-0.991299701281711,1.26457904430392,2.82134909307991));
#7633=CARTESIAN_POINT('Ctrl Pts',(-1.60135210822426,-0.1323128207854,2.91573339882681));
#7634=CARTESIAN_POINT('Ctrl Pts',(-0.770299824614874,-1.41013241834363,
3.01011770457376));
#7635=CARTESIAN_POINT('Ctrl Pts',(0.753968326190115,-1.41893164745954,3.10450201032066));
#7636=CARTESIAN_POINT('Ctrl Pts',(1.59971781403329,-0.150791818497472,3.1988863160676));
#7637=CARTESIAN_POINT('Ctrl Pts',(1.00583336157899,1.25305008112067,3.29327062181452));
#7638=CARTESIAN_POINT('Ctrl Pts',(-0.493230637487029,1.52923470903127,3.38765492756144));
#7639=CARTESIAN_POINT('Ctrl Pts',(-1.54842162351773,0.429215252389708,3.48203923330837));
#7640=CARTESIAN_POINT('Ctrl Pts',(-1.21014164638715,-1.05706785626069,3.5764235390553));
#7641=CARTESIAN_POINT('Ctrl Pts',(0.217181017787342,-1.59206396309263,3.67080784480223));
#7642=CARTESIAN_POINT('Ctrl Pts',(1.44905598384148,-0.694314059163175,3.76519215054915));
#7643=CARTESIAN_POINT('Ctrl Pts',(1.37688209988584,0.828269847373295,3.85957645629608));
#7644=CARTESIAN_POINT('Ctrl Pts',(0.0656108042523692,1.60546892821194,3.95396076204301));
#7645=CARTESIAN_POINT('Ctrl Pts',(-1.30470561785572,0.93785846894309,4.04834506778992));
#7646=CARTESIAN_POINT('Ctrl Pts',(-1.50087840470022,-0.573758896513456,
4.14272937353686));
#7647=CARTESIAN_POINT('Ctrl Pts',(-0.346365793965792,-1.56903345853926,
4.23711367928378));
#7648=CARTESIAN_POINT('Ctrl Pts',(1.11985176146982,-1.15228784995173,4.33149798503071));
#7649=CARTESIAN_POINT('Ctrl Pts',(1.57828119965777,0.301436082316522,4.42588229077763));
#7650=CARTESIAN_POINT('Ctrl Pts',(0.616368148442064,1.48388866288936,4.52026659652455));
#7651=CARTESIAN_POINT('Ctrl Pts',(-0.900233047455315,1.33094542162297,4.61465090227147));
#7652=CARTESIAN_POINT('Ctrl Pts',(-1.60668757995471,-0.0197554369790745,
4.7090352080184));
#7653=CARTESIAN_POINT('Ctrl Pts',(-0.867235871345144,-1.35267779168764,
4.80341951376534));
#7654=CARTESIAN_POINT('Ctrl Pts',(0.652667354478971,-1.46828490635015,4.89780381951226));
#7655=CARTESIAN_POINT('Ctrl Pts',(1.5852156931868,-0.26253850666854,4.99218812525918));
#7656=CARTESIAN_POINT('Ctrl Pts',(1.0911809852017,1.17947418822689,5.08657243100611));
#7657=CARTESIAN_POINT('Ctrl Pts',(-0.384840152259307,1.56004269237261,5.18095673675304));
#7658=CARTESIAN_POINT('Ctrl Pts',(-1.51453211481263,0.53668221351591,5.27534104249995));
#7659=CARTESIAN_POINT('Ctrl Pts',(-1.28125130434305,-0.969654895419948,
5.36972534824688));
#7660=CARTESIAN_POINT('Ctrl Pts',(0.105065915886374,-1.60337007932205,5.46410965399381));
#7661=CARTESIAN_POINT('Ctrl Pts',(1.39683114864801,-0.7941654210324,5.55849395974075));
#7662=CARTESIAN_POINT('Ctrl Pts',(1.43154627152773,0.729734145377444,5.65287826548766));
#7663=CARTESIAN_POINT('Ctrl Pts',(0.177969967514853,1.59692092332055,5.7472625712346));
#7664=CARTESIAN_POINT('Ctrl Pts',(-1.23576666361313,1.02699683734509,5.84164687698152));
#7665=CARTESIAN_POINT('Ctrl Pts',(-1.53740021748705,-0.46716399282643,5.93603118272843));
#7666=CARTESIAN_POINT('Ctrl Pts',(-0.455480673861307,-1.540887980073,6.03041548847536));
#7667=CARTESIAN_POINT('Ctrl Pts',(1.03633836657119,-1.22796258928818,6.1247997942223));
#7668=CARTESIAN_POINT('Ctrl Pts',(1.59552776581231,0.19012269705805,6.2191840999692));
#7669=CARTESIAN_POINT('Ctrl Pts',(0.718849649468088,1.43695938240689,6.31356840571614));
#7670=CARTESIAN_POINT('Ctrl Pts',(-0.804734544554861,1.39092163269575,6.40795271146306));
#7671=CARTESIAN_POINT('Ctrl Pts',(-1.60412976727155,0.092602940459203,6.50233701721));
#7672=CARTESIAN_POINT('Ctrl Pts',(-0.959890180152371,-1.28800496751056,
6.5967213229569));
#7673=CARTESIAN_POINT('Ctrl Pts',(0.548121242644853,-1.51151111555712,6.69110562870386));
#7674=CARTESIAN_POINT('Ctrl Pts',(1.56310784547845,-0.37065643167945,6.78549853239035));
#7675=CARTESIAN_POINT('Ctrl Pts',(1.3014618734641,0.606427672763405,6.84843000082788));
#7676=CARTESIAN_POINT('Ctrl Pts',(0.993685314990144,0.933895149917456,6.87990003401645));
#7677=CARTESIAN_POINT('Ctrl Pts',(-0.646459514637458,1.33049624488324,-0.132223047397372));
#7678=CARTESIAN_POINT('Ctrl Pts',(-1.08480930388685,1.11751150848179,-0.100761612148397));
#7679=CARTESIAN_POINT('Ctrl Pts',(-1.72748972074385,0.228459034416341,-0.037838741650446));
#7680=CARTESIAN_POINT('Ctrl Pts',(-1.13986071563865,-1.3200647398456,0.0565455640964797));
#7681=CARTESIAN_POINT('Ctrl Pts',(0.474954970979457,-1.67650645441138,0.150929869843405));
#7682=CARTESIAN_POINT('Ctrl Pts',(1.66162938758921,-0.526273512027314,0.24531417559033));
#7683=CARTESIAN_POINT('Ctrl Pts',(1.35332768345178,1.09864158048345,0.339698481337256));
#7684=CARTESIAN_POINT('Ctrl Pts',(-0.173070373162715,1.73429378997042,0.434082787084181));
#7685=CARTESIAN_POINT('Ctrl Pts',(-1.54361410933203,0.809498516568055,0.528467092831108));
#7686=CARTESIAN_POINT('Ctrl Pts',(-1.52506749024128,-0.843943917146358,
0.622851398578033));
#7687=CARTESIAN_POINT('Ctrl Pts',(-0.13403851934482,-1.73781439657543,0.717235704324959));
#7688=CARTESIAN_POINT('Ctrl Pts',(1.37760076485913,-1.06781654932485,0.811620010071883));
#7689=CARTESIAN_POINT('Ctrl Pts',(1.64950375176345,0.56316389391153,0.906004315818811));
#7690=CARTESIAN_POINT('Ctrl Pts',(0.436964811193913,1.68732445748138,1.00038862156574));
#7691=CARTESIAN_POINT('Ctrl Pts',(-1.16880967008705,1.2930174600825,1.09477292731266));
#7692=CARTESIAN_POINT('Ctrl Pts',(-1.72273848782547,-0.264917918077412,
1.18915723305959));
#7693=CARTESIAN_POINT('Ctrl Pts',(-0.7263227793451,-1.58444401519218,1.28354153880651));
#7694=CARTESIAN_POINT('Ctrl Pts',(0.9237322219861,-1.47808242332004,1.37792584455344));
#7695=CARTESIAN_POINT('Ctrl Pts',(1.74249311507829,-0.0415497454832925,
1.47231015030036));
#7696=CARTESIAN_POINT('Ctrl Pts',(0.993132214199591,1.43237454264688,1.56669445604729));
#7697=CARTESIAN_POINT('Ctrl Pts',(-0.649978044897315,1.61726223995226,1.66107876179422));
#7698=CARTESIAN_POINT('Ctrl Pts',(-1.70815363161769,0.346727174142455,1.75546306754114));
#7699=CARTESIAN_POINT('Ctrl Pts',(-1.22911062769304,-1.2358380170301,1.84984737328807));
#7700=CARTESIAN_POINT('Ctrl Pts',(0.356045810658149,-1.70623560713348,1.94423167903499));
#7701=CARTESIAN_POINT('Ctrl Pts',(1.62078597105695,-0.6411406968694,2.03861598478192));
#7702=CARTESIAN_POINT('Ctrl Pts',(1.4269323242515,1.00093591055773,2.13300029052884));
#7703=CARTESIAN_POINT('Ctrl Pts',(-0.0510604281759689,1.74224033688597,
2.22738459627577));
#7704=CARTESIAN_POINT('Ctrl Pts',(-1.48310237355857,0.915650537462024,2.3217689020227));
#7705=CARTESIAN_POINT('Ctrl Pts',(-1.58045610355311,-0.734960585222904,
2.41615320776962));
#7706=CARTESIAN_POINT('Ctrl Pts',(-0.255510083152334,-1.72415868034384,
2.51053751351654));
#7707=CARTESIAN_POINT('Ctrl Pts',(1.29937710855069,-1.16173477485675,2.60492181926348));
#7708=CARTESIAN_POINT('Ctrl Pts',(1.68491594995867,0.446169025059073,2.69930612501039));
#7709=CARTESIAN_POINT('Ctrl Pts',(0.554148498595194,1.65255196557264,2.79369043075733));
#7710=CARTESIAN_POINT('Ctrl Pts',(-1.075313772293,1.37175393146487,2.88807473650425));
#7711=CARTESIAN_POINT('Ctrl Pts',(-1.7370689954184,-0.143526522057367,2.98245904225118));
#7712=CARTESIAN_POINT('Ctrl Pts',(-0.835583839208558,-1.52964316264918,
3.0768433479981));
#7713=CARTESIAN_POINT('Ctrl Pts',(0.817868222876148,-1.53918813904903,3.17122765374503));
#7714=CARTESIAN_POINT('Ctrl Pts',(1.7352961924515,-0.163571641320779,3.26561195949195));
#7715=CARTESIAN_POINT('Ctrl Pts',(1.09107918113888,1.35924787212158,3.35999626523888));
#7716=CARTESIAN_POINT('Ctrl Pts',(-0.535032641209211,1.65883954324172,3.4543805709858));
#7717=CARTESIAN_POINT('Ctrl Pts',(-1.67965257624115,0.465591860439508,3.54876487673272));
#7718=CARTESIAN_POINT('Ctrl Pts',(-1.31270288602219,-1.14665587270498,3.64314918247966));
#7719=CARTESIAN_POINT('Ctrl Pts',(0.235587420439429,-1.7269936666695,3.73753348822658));
#7720=CARTESIAN_POINT('Ctrl Pts',(1.57186555613167,-0.753158171186272,3.83191779397351));
#7721=CARTESIAN_POINT('Ctrl Pts',(1.49357483202773,0.898466904513287,3.92630209972043));
#7722=CARTESIAN_POINT('Ctrl Pts',(0.0711714139856785,1.74153472180275,4.02068640546736));
#7723=CARTESIAN_POINT('Ctrl Pts',(-1.41528128965875,1.01734331888955,4.11507071121428));
#7724=CARTESIAN_POINT('Ctrl Pts',(-1.62808000146129,-0.62238578564972,4.20945501696121));
#7725=CARTESIAN_POINT('Ctrl Pts',(-0.375720791624429,-1.70201129383405,
4.30383932270812));
#7726=CARTESIAN_POINT('Ctrl Pts',(1.21476080390027,-1.24994589738797,4.39822362845507));
#7727=CARTESIAN_POINT('Ctrl Pts',(1.71204279427179,0.326983222492551,4.49260793420197));
#7728=CARTESIAN_POINT('Ctrl Pts',(0.668606232772531,1.60965035467203,4.58699223994891));
#7729=CARTESIAN_POINT('Ctrl Pts',(-0.976529088983251,1.44374495441797,4.68137654569583));
#7730=CARTESIAN_POINT('Ctrl Pts',(-1.74285665602802,-0.0214297385884319,
4.77576085144276));
#7731=CARTESIAN_POINT('Ctrl Pts',(-0.940735354886333,-1.46731917400552,
4.87014515718968));
#7732=CARTESIAN_POINT('Ctrl Pts',(0.707981848566931,-1.59272415739343,4.96452946293661));
#7733=CARTESIAN_POINT('Ctrl Pts',(1.71956499607009,-0.28478902153699,5.05891376868354));
#7734=CARTESIAN_POINT('Ctrl Pts',(1.18366013823523,1.27943631681177,5.15329807443046));
#7735=CARTESIAN_POINT('Ctrl Pts',(-0.417455906947926,1.6922585473438,5.24768238017739));
#7736=CARTESIAN_POINT('Ctrl Pts',(-1.64289088308245,0.582166800607521,5.34206668592431));
#7737=CARTESIAN_POINT('Ctrl Pts',(-1.38983918944704,-1.05183453810009,5.43645099167124));
#7738=CARTESIAN_POINT('Ctrl Pts',(0.113970402901476,-1.73925799246011,5.53083529741816));
#7739=CARTESIAN_POINT('Ctrl Pts',(1.51521459127547,-0.861472079141013,5.62521960316509));
#7740=CARTESIAN_POINT('Ctrl Pts',(1.55287187059388,0.791580160492583,5.71960390891201));
#7741=CARTESIAN_POINT('Ctrl Pts',(0.193053177435471,1.73226226124066,5.81398821465895));
#7742=CARTESIAN_POINT('Ctrl Pts',(-1.34049966019928,1.1140362918204,5.90837252040586));
#7743=CARTESIAN_POINT('Ctrl Pts',(-1.66769709024686,-0.506756811039214,
6.00275682615279));
#7744=CARTESIAN_POINT('Ctrl Pts',(-0.494083314040241,-1.67148044571272,
6.09714113189972));
#7745=CARTESIAN_POINT('Ctrl Pts',(1.1241695290423,-1.33203417938579,6.19152543764664));
#7746=CARTESIAN_POINT('Ctrl Pts',(1.73075103163608,0.20623586823205,6.28590974339357));
#7747=CARTESIAN_POINT('Ctrl Pts',(0.779773187948709,1.55874375038136,6.38029404914049));
#7748=CARTESIAN_POINT('Ctrl Pts',(-0.872936951036021,1.50880423537318,6.47467835488741));
#7749=CARTESIAN_POINT('Ctrl Pts',(-1.74008206505257,0.100451172437426,6.56906266063435));
#7750=CARTESIAN_POINT('Ctrl Pts',(-1.04124224921292,-1.3971652352514,6.66344696638127));
#7751=CARTESIAN_POINT('Ctrl Pts',(0.594575303856428,-1.63961384980852,6.7578312721282));
#7752=CARTESIAN_POINT('Ctrl Pts',(1.69558347657019,-0.40207009571229,6.8522241758147));
#7753=CARTESIAN_POINT('Ctrl Pts',(1.41176263327905,0.657823287527416,6.91515564425223));
#7754=CARTESIAN_POINT('Ctrl Pts',(1.07790157018373,1.01304410289385,6.9466256774408));
#7755=CARTESIAN_POINT('Ctrl Pts',(-0.696967279875932,1.43444767643566,-0.0654974039730188));
#7756=CARTESIAN_POINT('Ctrl Pts',(-1.1695652590683,1.20482248100781,-0.0340359687240437));
#7757=CARTESIAN_POINT('Ctrl Pts',(-1.86245818093606,0.246308497554627,0.0288869017739064));
#7758=CARTESIAN_POINT('Ctrl Pts',(-1.22891782768739,-1.42320115979157,0.123271207520832));
#7759=CARTESIAN_POINT('Ctrl Pts',(0.512063117166348,-1.80749160120389,0.217655513267758));
#7760=CARTESIAN_POINT('Ctrl Pts',(1.79145219183517,-0.567391166566931,0.312039819014683));
#7761=CARTESIAN_POINT('Ctrl Pts',(1.45906293118009,1.18447824893965,0.406424124761609));
#7762=CARTESIAN_POINT('Ctrl Pts',(-0.186592330190968,1.86979385086363,0.500808430508534));
#7763=CARTESIAN_POINT('Ctrl Pts',(-1.66421640118114,0.872744489610393,0.59519273625546));
#7764=CARTESIAN_POINT('Ctrl Pts',(-1.64422073808718,-0.909881103120909,
0.689577042002386));
#7765=CARTESIAN_POINT('Ctrl Pts',(-0.144510924676781,-1.87358952182748,
0.78396134774931));
#7766=CARTESIAN_POINT('Ctrl Pts',(1.48523246405823,-1.15124486365837,0.878345653496237));
#7767=CARTESIAN_POINT('Ctrl Pts',(1.77837918227017,0.607163787331645,0.972729959243162));
#7768=CARTESIAN_POINT('Ctrl Pts',(0.471104793051308,1.81915481290187,1.06711426499009));
#7769=CARTESIAN_POINT('Ctrl Pts',(-1.26012855872361,1.3940406809407,1.16149857073701));
#7770=CARTESIAN_POINT('Ctrl Pts',(-1.85733573504703,-0.285615907217876,
1.25588287648394));
#7771=CARTESIAN_POINT('Ctrl Pts',(-0.783070247045533,-1.70823634021925,
1.35026718223087));
#7772=CARTESIAN_POINT('Ctrl Pts',(0.995903253821642,-1.59356473636487,1.44465148797779));
#7773=CARTESIAN_POINT('Ctrl Pts',(1.8786337877628,-0.0447960196011254,1.53903579372472));
#7774=CARTESIAN_POINT('Ctrl Pts',(1.070725454905,1.54428570722175,1.63342009947164));
#7775=CARTESIAN_POINT('Ctrl Pts',(-0.700760712270145,1.74361864695846,1.72780440521857));
#7776=CARTESIAN_POINT('Ctrl Pts',(-1.84161136665526,0.373816905698525,1.82218871096549));
#7777=CARTESIAN_POINT('Ctrl Pts',(-1.32514081926731,-1.33239381831945,1.91657301671242));
#7778=CARTESIAN_POINT('Ctrl Pts',(0.383863605603818,-1.83954348726417,2.01095732245934));
#7779=CARTESIAN_POINT('Ctrl Pts',(1.74741768653858,-0.691232903835339,2.10534162820627));
#7780=CARTESIAN_POINT('Ctrl Pts',(1.53841828928508,1.07913885265157,2.19972593395319));
#7781=CARTESIAN_POINT('Ctrl Pts',(-0.0550497702165604,1.87836126005592,
2.29411023970012));
#7782=CARTESIAN_POINT('Ctrl Pts',(-1.5989768944098,0.987190148743883,2.38849454544705));
#7783=CARTESIAN_POINT('Ctrl Pts',(-1.70393685376336,-0.792382923138043,
2.48287885119397));
#7784=CARTESIAN_POINT('Ctrl Pts',(-0.275473039847566,-1.85886688695062,
2.5772631569409));
#7785=CARTESIAN_POINT('Ctrl Pts',(1.40089720759624,-1.25250090320548,2.67164746268782));
#7786=CARTESIAN_POINT('Ctrl Pts',(1.81655812912099,0.481028130485029,2.76603176843475));
#7787=CARTESIAN_POINT('Ctrl Pts',(0.597444020805899,1.78166555247427,2.86041607418167));
#7788=CARTESIAN_POINT('Ctrl Pts',(-1.15932784330429,1.47892881862582,2.9548003799286));
#7789=CARTESIAN_POINT('Ctrl Pts',(-1.87278588261255,-0.154740223329332,
3.04918468567552));
#7790=CARTESIAN_POINT('Ctrl Pts',(-0.900867853802242,-1.64915390695474,
3.14356899142245));
#7791=CARTESIAN_POINT('Ctrl Pts',(0.881768119562182,-1.65944463063851,3.23795329716937));
#7792=CARTESIAN_POINT('Ctrl Pts',(1.87087457086971,-0.176351464144087,3.3323376029163));
#7793=CARTESIAN_POINT('Ctrl Pts',(1.17632500069877,1.46544566312249,3.42672190866323));
#7794=CARTESIAN_POINT('Ctrl Pts',(-0.576834644931392,1.78844437745218,3.52110621441015));
#7795=CARTESIAN_POINT('Ctrl Pts',(-1.81088352896457,0.501968468489308,3.61549052015708));
#7796=CARTESIAN_POINT('Ctrl Pts',(-1.41526412565724,-1.23624388914925,3.709874825904));
#7797=CARTESIAN_POINT('Ctrl Pts',(0.253993823091515,-1.86192337024639,3.80425913165093));
#7798=CARTESIAN_POINT('Ctrl Pts',(1.69467512842186,-0.81200228320937,3.89864343739786));
#7799=CARTESIAN_POINT('Ctrl Pts',(1.61026756416961,0.968663961653281,3.99302774314478));
#7800=CARTESIAN_POINT('Ctrl Pts',(0.0767320237189894,1.87760051539355,4.08741204889171));
#7801=CARTESIAN_POINT('Ctrl Pts',(-1.52585696146177,1.09682816883599,4.18179635463863));
#7802=CARTESIAN_POINT('Ctrl Pts',(-1.75528159822236,-0.671012674785984,
4.27618066038555));
#7803=CARTESIAN_POINT('Ctrl Pts',(-0.405075789283068,-1.83498912912884,
4.37056496613248));
#7804=CARTESIAN_POINT('Ctrl Pts',(1.30966984633074,-1.34760394482421,4.46494927187941));
#7805=CARTESIAN_POINT('Ctrl Pts',(1.84580438888581,0.35253036266858,4.55933357762632));
#7806=CARTESIAN_POINT('Ctrl Pts',(0.720844317102997,1.7354120464547,4.65371788337327));
#7807=CARTESIAN_POINT('Ctrl Pts',(-1.05282513051118,1.55654448721296,4.74810218912018));
#7808=CARTESIAN_POINT('Ctrl Pts',(-1.87902573210135,-0.023104040197789,
4.84248649486711));
#7809=CARTESIAN_POINT('Ctrl Pts',(-1.01423483842752,-1.58196055632341,4.93687080061403));
#7810=CARTESIAN_POINT('Ctrl Pts',(0.763296342654892,-1.7171634084367,5.03125510636096));
#7811=CARTESIAN_POINT('Ctrl Pts',(1.85391429895339,-0.307039536405439,5.12563941210788));
#7812=CARTESIAN_POINT('Ctrl Pts',(1.27613929126875,1.37939844539666,5.22002371785481));
#7813=CARTESIAN_POINT('Ctrl Pts',(-0.450071661636544,1.82447440231499,5.31440802360174));
#7814=CARTESIAN_POINT('Ctrl Pts',(-1.77124965135225,0.627651387699125,5.40879232934866));
#7815=CARTESIAN_POINT('Ctrl Pts',(-1.49842707455103,-1.13401418078021,5.50317663509559));
#7816=CARTESIAN_POINT('Ctrl Pts',(0.122874889916577,-1.87514590559817,5.59756094084251));
#7817=CARTESIAN_POINT('Ctrl Pts',(1.63359803390294,-0.928778737249626,5.69194524658944));
#7818=CARTESIAN_POINT('Ctrl Pts',(1.67419746966002,0.853426175607722,5.78632955233636));
#7819=CARTESIAN_POINT('Ctrl Pts',(0.208136387356091,1.86760359916079,5.88071385808329));
#7820=CARTESIAN_POINT('Ctrl Pts',(-1.44523265678541,1.20107574629571,5.97509816383021));
#7821=CARTESIAN_POINT('Ctrl Pts',(-1.79799396300668,-0.546349629251995,
6.06948246957714));
#7822=CARTESIAN_POINT('Ctrl Pts',(-0.532685954219177,-1.80207291135245,
6.16386677532407));
#7823=CARTESIAN_POINT('Ctrl Pts',(1.21200069151341,-1.4361057694834,6.25825108107099));
#7824=CARTESIAN_POINT('Ctrl Pts',(1.86597429745986,0.222349039406046,6.35263538681792));
#7825=CARTESIAN_POINT('Ctrl Pts',(0.84069672642933,1.68052811835584,6.44701969256484));
#7826=CARTESIAN_POINT('Ctrl Pts',(-0.941139357517183,1.62668683805062,6.54140399831177));
#7827=CARTESIAN_POINT('Ctrl Pts',(-1.87603436283358,0.108299404415651,6.6357883040587));
#7828=CARTESIAN_POINT('Ctrl Pts',(-1.12259431827347,-1.50632550299225,6.73017260980562));
#7829=CARTESIAN_POINT('Ctrl Pts',(0.641029365068003,-1.76771658405992,6.82455691555255));
#7830=CARTESIAN_POINT('Ctrl Pts',(1.82805910766192,-0.433483759745132,6.91894981923906));
#7831=CARTESIAN_POINT('Ctrl Pts',(1.52206339309401,0.709218902291427,6.98188128767659));
#7832=CARTESIAN_POINT('Ctrl Pts',(1.16211782537732,1.09219305587025,7.01335132086515));
#7833=CARTESIAN_POINT('Ctrl Pts',(-0.747475045114406,1.53839910798808,0.00122823945133365));
#7834=CARTESIAN_POINT('Ctrl Pts',(-1.25432121424975,1.29213345353384,0.0326896747003088));
#7835=CARTESIAN_POINT('Ctrl Pts',(-1.99742664112827,0.264157960692912,0.0956125451982589));
#7836=CARTESIAN_POINT('Ctrl Pts',(-1.31797493973614,-1.52633757973754,0.189996850945185));
#7837=CARTESIAN_POINT('Ctrl Pts',(0.549171263353243,-1.93847674799641,0.28438115669211));
#7838=CARTESIAN_POINT('Ctrl Pts',(1.92127499608112,-0.608508821106544,0.378765462439036));
#7839=CARTESIAN_POINT('Ctrl Pts',(1.56479817890842,1.27031491739583,0.473149768185962));
#7840=CARTESIAN_POINT('Ctrl Pts',(-0.200114287219223,2.00529391175686,0.567534073932887));
#7841=CARTESIAN_POINT('Ctrl Pts',(-1.78481869303027,0.935990462652723,0.661918379679812));
#7842=CARTESIAN_POINT('Ctrl Pts',(-1.7633739859331,-0.975818289095456,0.756302685426739));
#7843=CARTESIAN_POINT('Ctrl Pts',(-0.154983330008743,-2.00936464707954,
0.850686991173664));
#7844=CARTESIAN_POINT('Ctrl Pts',(1.59286416325733,-1.23467317799189,0.945071296920589));
#7845=CARTESIAN_POINT('Ctrl Pts',(1.90725461277688,0.65116368075176,1.03945560266751));
#7846=CARTESIAN_POINT('Ctrl Pts',(0.505244774908705,1.95098516832236,1.13383990841444));
#7847=CARTESIAN_POINT('Ctrl Pts',(-1.35144744736016,1.4950639017989,1.22822421416136));
#7848=CARTESIAN_POINT('Ctrl Pts',(-1.99193298226858,-0.306313896358341,
1.32260851990829));
#7849=CARTESIAN_POINT('Ctrl Pts',(-0.839817714745969,-1.83202866524631,
1.41699282565521));
#7850=CARTESIAN_POINT('Ctrl Pts',(1.06807428565718,-1.70904704940972,1.51137713140214));
#7851=CARTESIAN_POINT('Ctrl Pts',(2.01477446044731,-0.0480422937189565,
1.60576143714906));
#7852=CARTESIAN_POINT('Ctrl Pts',(1.14831869561041,1.65619687179661,1.70014574289599));
#7853=CARTESIAN_POINT('Ctrl Pts',(-0.751543379642974,1.86997505396467,1.79453004864291));
#7854=CARTESIAN_POINT('Ctrl Pts',(-1.97506910169283,0.400906637254589,1.88891435438984));
#7855=CARTESIAN_POINT('Ctrl Pts',(-1.42117101084157,-1.42894961960879,1.98329866013677));
#7856=CARTESIAN_POINT('Ctrl Pts',(0.411681400549486,-1.97285136739486,2.07768296588369));
#7857=CARTESIAN_POINT('Ctrl Pts',(1.8740494020202,-0.741325110801277,2.17206727163062));
#7858=CARTESIAN_POINT('Ctrl Pts',(1.64990425431865,1.15734179474542,2.26645157737754));
#7859=CARTESIAN_POINT('Ctrl Pts',(-0.0590391122571503,2.01448218322587,
2.36083588312447));
#7860=CARTESIAN_POINT('Ctrl Pts',(-1.71485141526102,1.05872976002574,2.45522018887139));
#7861=CARTESIAN_POINT('Ctrl Pts',(-1.8274176039736,-0.849805261053182,2.54960449461832));
#7862=CARTESIAN_POINT('Ctrl Pts',(-0.295435996542797,-1.99357509355738,
2.64398880036524));
#7863=CARTESIAN_POINT('Ctrl Pts',(1.50241730664178,-1.34326703155423,2.73837310611218));
#7864=CARTESIAN_POINT('Ctrl Pts',(1.9482003082833,0.515887235910986,2.83275741185909));
#7865=CARTESIAN_POINT('Ctrl Pts',(0.640739543016601,1.9107791393759,2.92714171760603));
#7866=CARTESIAN_POINT('Ctrl Pts',(-1.24334191431558,1.58610370578677,3.02152602335295));
#7867=CARTESIAN_POINT('Ctrl Pts',(-2.0085027698067,-0.165953924601296,3.11591032909987));
#7868=CARTESIAN_POINT('Ctrl Pts',(-0.966151868395926,-1.76866465126028,
3.2102946348468));
#7869=CARTESIAN_POINT('Ctrl Pts',(0.945668016248215,-1.779701122228,3.30467894059372));
#7870=CARTESIAN_POINT('Ctrl Pts',(2.00645294928792,-0.189131286967392,3.39906324634065));
#7871=CARTESIAN_POINT('Ctrl Pts',(1.26157082025866,1.5716434541234,3.49344755208758));
#7872=CARTESIAN_POINT('Ctrl Pts',(-0.618636648653572,1.91804921166265,3.58783185783451));
#7873=CARTESIAN_POINT('Ctrl Pts',(-1.94211448168799,0.538345076539106,3.68221616358144));
#7874=CARTESIAN_POINT('Ctrl Pts',(-1.51782536529229,-1.32583190559354,3.77660046932835));
#7875=CARTESIAN_POINT('Ctrl Pts',(0.2724002257436,-1.99685307382326,3.87098477507528));
#7876=CARTESIAN_POINT('Ctrl Pts',(1.81748470071205,-0.870846395232466,3.9653690808222));
#7877=CARTESIAN_POINT('Ctrl Pts',(1.72696029631149,1.03886101879327,4.05975338656913));
#7878=CARTESIAN_POINT('Ctrl Pts',(0.0822926334523,2.01366630898437,4.15413769231605));
#7879=CARTESIAN_POINT('Ctrl Pts',(-1.63643263326479,1.17631301878244,4.24852199806298));
#7880=CARTESIAN_POINT('Ctrl Pts',(-1.88248319498343,-0.719639563922248,
4.3429063038099));
#7881=CARTESIAN_POINT('Ctrl Pts',(-0.434430786941708,-1.96796696442363,
4.43729060955683));
#7882=CARTESIAN_POINT('Ctrl Pts',(1.40457888876119,-1.44526199226046,4.53167491530376));
#7883=CARTESIAN_POINT('Ctrl Pts',(1.97956598349983,0.378077502844609,4.62605922105068));
#7884=CARTESIAN_POINT('Ctrl Pts',(0.773082401433464,1.86117373823736,4.72044352679761));
#7885=CARTESIAN_POINT('Ctrl Pts',(-1.12912117203912,1.66934402000796,4.81482783254453));
#7886=CARTESIAN_POINT('Ctrl Pts',(-2.01519480817465,-0.0247783418071453,
4.90921213829146));
#7887=CARTESIAN_POINT('Ctrl Pts',(-1.08773432196871,-1.6966019386413,5.00359644403838));
#7888=CARTESIAN_POINT('Ctrl Pts',(0.818610836742852,-1.84160265947997,5.09798074978531));
#7889=CARTESIAN_POINT('Ctrl Pts',(1.98826360183667,-0.32929005127389,5.19236505553224));
#7890=CARTESIAN_POINT('Ctrl Pts',(1.36861844430227,1.47936057398154,5.28674936127916));
#7891=CARTESIAN_POINT('Ctrl Pts',(-0.48268741632516,1.95669025728617,5.38113366702608));
#7892=CARTESIAN_POINT('Ctrl Pts',(-1.89960841962207,0.673135974790736,5.47551797277302));
#7893=CARTESIAN_POINT('Ctrl Pts',(-1.60701495965502,-1.21619382346035,5.56990227851994));
#7894=CARTESIAN_POINT('Ctrl Pts',(0.13177937693168,-2.01103381873623,5.66428658426686));
#7895=CARTESIAN_POINT('Ctrl Pts',(1.7519814765304,-0.99608539535824,5.7586708900138));
#7896=CARTESIAN_POINT('Ctrl Pts',(1.79552306872616,0.915272190722859,5.85305519576071));
#7897=CARTESIAN_POINT('Ctrl Pts',(0.223219597276707,2.00294493708091,5.94743950150766));
#7898=CARTESIAN_POINT('Ctrl Pts',(-1.54996565337156,1.28811520077101,6.04182380725456));
#7899=CARTESIAN_POINT('Ctrl Pts',(-1.92829083576649,-0.585942447464776,
6.13620811300149));
#7900=CARTESIAN_POINT('Ctrl Pts',(-0.57128859439811,-1.93266537699218,6.23059241874842));
#7901=CARTESIAN_POINT('Ctrl Pts',(1.29983185398451,-1.54017735958102,6.32497672449534));
#7902=CARTESIAN_POINT('Ctrl Pts',(2.00119756328365,0.238462210580048,6.41936103024226));
#7903=CARTESIAN_POINT('Ctrl Pts',(0.901620264909948,1.8023124863303,6.5137453359892));
#7904=CARTESIAN_POINT('Ctrl Pts',(-1.00934176399834,1.74456944072806,6.60812964173611));
#7905=CARTESIAN_POINT('Ctrl Pts',(-2.0119866606146,0.116147636393871,6.70251394748306));
#7906=CARTESIAN_POINT('Ctrl Pts',(-1.20394638733402,-1.61548577073308,6.79689825322996));
#7907=CARTESIAN_POINT('Ctrl Pts',(0.687483426279577,-1.89581931831132,6.8912825589769));
#7908=CARTESIAN_POINT('Ctrl Pts',(1.96053473875365,-0.46489742377797,6.98567546266341));
#7909=CARTESIAN_POINT('Ctrl Pts',(1.63236415290896,0.760614517055437,7.04860693110094));
#7910=CARTESIAN_POINT('Ctrl Pts',(1.24633408057091,1.17134200884666,7.08007696428951));
#7911=CARTESIAN_POINT('Ctrl Pts',(0.433521463884974,-1.65487835139843,6.88122480138926));
#7912=CARTESIAN_POINT('Ctrl Pts',(0.48286633167622,-1.63704432698362,6.88122480138927));
#7913=CARTESIAN_POINT('Ctrl Pts',(0.531233565484471,-1.61684089219081,6.88122480138927));
#7914=CARTESIAN_POINT('Ctrl Pts',(0.578448771240116,-1.59422718307761,6.88122480138927));
#7915=CARTESIAN_POINT('Ctrl Pts',(0.637301800459365,-1.56603954178929,6.88122480138927));
#7916=CARTESIAN_POINT('Ctrl Pts',(0.694366366669772,-1.53410742466645,6.88122480138927));
#7917=CARTESIAN_POINT('Ctrl Pts',(0.749419640704226,-1.49872451372066,6.88122480138927));
#7918=CARTESIAN_POINT('Ctrl Pts',(0.77114866472208,-1.48475920220656,6.88122480138927));
#7919=CARTESIAN_POINT('Ctrl Pts',(0.792563942974927,-1.47025593156819,6.88122480138927));
#7920=CARTESIAN_POINT('Ctrl Pts',(0.813649982189817,-1.45523144121435,6.88122480138927));
#7921=CARTESIAN_POINT('Ctrl Pts',(0.826217216190941,-1.44627687729175,6.88122480138927));
#7922=CARTESIAN_POINT('Ctrl Pts',(0.838668448552751,-1.43713623173645,6.88122480138927));
#7923=CARTESIAN_POINT('Ctrl Pts',(0.850984238037051,-1.42782560626945,6.88122480138927));
#7924=CARTESIAN_POINT('Ctrl Pts',(0.902467037297749,-1.3889050756352,6.88122480138927));
#7925=CARTESIAN_POINT('Ctrl Pts',(0.95165412885067,-1.34696984463084,6.88122480138927));
#7926=CARTESIAN_POINT('Ctrl Pts',(0.998333866062454,-1.30231142297158,6.88122480138927));
#7927=CARTESIAN_POINT('Ctrl Pts',(1.03120466603183,-1.27086398703916,6.88122480138927));
#7928=CARTESIAN_POINT('Ctrl Pts',(1.06283139573338,-1.23806535986098,6.88122480138927));
#7929=CARTESIAN_POINT('Ctrl Pts',(1.09312668212505,-1.204009648788,6.88122480138927));
#7930=CARTESIAN_POINT('Ctrl Pts',(1.11086405824911,-1.18407060782089,6.88122480138928));
#7931=CARTESIAN_POINT('Ctrl Pts',(1.12814480788324,-1.16370055148135,6.88122480138927));
#7932=CARTESIAN_POINT('Ctrl Pts',(1.14494937865368,-1.14291778130075,6.88122480138928));
#7933=CARTESIAN_POINT('Ctrl Pts',(1.15221458967818,-1.13393265379595,6.88122480138928));
#7934=CARTESIAN_POINT('Ctrl Pts',(1.15938472523217,-1.12487785140287,6.88122480138927));
#7935=CARTESIAN_POINT('Ctrl Pts',(1.16645787983334,-1.11575613827896,6.88122480138927));
#7936=CARTESIAN_POINT('Ctrl Pts',(1.20502462160414,-1.06601952507116,6.88122480138927));
#7937=CARTESIAN_POINT('Ctrl Pts',(1.2407199156978,-1.01428551684517,6.88122480138927));
#7938=CARTESIAN_POINT('Ctrl Pts',(1.27334306155911,-0.960820138530249,6.88122480138927));
#7939=CARTESIAN_POINT('Ctrl Pts',(1.30592057494354,-0.907429546308939,6.88122480138927));
#7940=CARTESIAN_POINT('Ctrl Pts',(1.33543504029667,-0.852311439716943,6.88122480138928));
#7941=CARTESIAN_POINT('Ctrl Pts',(1.36163634733777,-0.795715456114972,6.88122480138927));
#7942=CARTESIAN_POINT('Ctrl Pts',(1.38783765437887,-0.739119472513,6.88122480138927));
#7943=CARTESIAN_POINT('Ctrl Pts',(1.41072631426025,-0.681044662516224,6.88122480138927));
#7944=CARTESIAN_POINT('Ctrl Pts',(1.42999425119658,-0.621739849690903,6.88122480138927));
#7945=CARTESIAN_POINT('Ctrl Pts',(1.43427223611634,-0.608572633305774,6.88122480138927));
#7946=CARTESIAN_POINT('Ctrl Pts',(1.43837246784893,-0.595341002512054,6.88122480138927));
#7947=CARTESIAN_POINT('Ctrl Pts',(1.44228388835249,-0.582073867848763,6.88122480138927));
#7948=CARTESIAN_POINT('Ctrl Pts',(1.45898642628307,-0.525420583001915,6.88122480138927));
#7949=CARTESIAN_POINT('Ctrl Pts',(1.47228074592207,-0.468032401322888,6.88122480138927));
#7950=CARTESIAN_POINT('Ctrl Pts',(1.4819610710342,-0.410128498806204,6.88122480138927));
#7951=CARTESIAN_POINT('Ctrl Pts',(1.48501607616399,-0.391854658085531,6.88122480138927));
#7952=CARTESIAN_POINT('Ctrl Pts',(1.48771075601926,-0.373529425782789,6.88122480138927));
#7953=CARTESIAN_POINT('Ctrl Pts',(1.49003754927256,-0.355159679252195,6.88122480138927));
#7954=CARTESIAN_POINT('Ctrl Pts',(1.49778245475607,-0.294014603112158,6.88122480138927));
#7955=CARTESIAN_POINT('Ctrl Pts',(1.5014555591722,-0.23237502353427,6.88122480138927));
#7956=CARTESIAN_POINT('Ctrl Pts',(1.50117058949863,-0.17058848658511,6.88122480138927));
#7957=CARTESIAN_POINT('Ctrl Pts',(1.5010450609477,-0.143371645042982,6.88122480138927));
#7958=CARTESIAN_POINT('Ctrl Pts',(1.50015079106509,-0.116126514557446,6.88122480138927));
#7959=CARTESIAN_POINT('Ctrl Pts',(1.49849429649857,-0.0888842916021443,
6.88122480138927));
#7960=CARTESIAN_POINT('Ctrl Pts',(1.49741398382498,-0.0711177867731435,
6.88122480138927));
#7961=CARTESIAN_POINT('Ctrl Pts',(1.49600944105652,-0.0533525402256336,
6.88122480138926));
#7962=CARTESIAN_POINT('Ctrl Pts',(1.49428207131083,-0.0355975031972548,
6.88122480138926));
#7963=CARTESIAN_POINT('Ctrl Pts',(1.49320087544153,-0.0244842642729668,
6.88122480138926));
#7964=CARTESIAN_POINT('Ctrl Pts',(1.49199294904392,-0.0133738365360173,
6.88122480138926));
#7965=CARTESIAN_POINT('Ctrl Pts',(1.49066097672539,-0.00228582989250978,
6.88122480138926));
#7966=CARTESIAN_POINT('Ctrl Pts',(1.48365926906569,0.0559999017000902,6.88122480138927));
#7967=CARTESIAN_POINT('Ctrl Pts',(1.47322434547187,0.113778347564274,6.88122480138927));
#7968=CARTESIAN_POINT('Ctrl Pts',(1.4594842086581,0.170755138432216,6.88122480138927));
#7969=CARTESIAN_POINT('Ctrl Pts',(1.44587229152792,0.227200235460672,6.88122480138927));
#7970=CARTESIAN_POINT('Ctrl Pts',(1.42901593858198,0.282859526726203,6.88122480138927));
#7971=CARTESIAN_POINT('Ctrl Pts',(1.40899511525678,0.337423685152158,6.88122480138927));
#7972=CARTESIAN_POINT('Ctrl Pts',(1.38913180150897,0.391558571644822,6.88122480138927));
#7973=CARTESIAN_POINT('Ctrl Pts',(1.36615305512817,0.444616362809891,6.88122480138927));
#7974=CARTESIAN_POINT('Ctrl Pts',(1.34010169134689,0.49625853363983,6.88122480138927));
#7975=CARTESIAN_POINT('Ctrl Pts',(1.3336683238708,0.509011534404064,6.88122480138926));
#7976=CARTESIAN_POINT('Ctrl Pts',(1.3270447516601,0.521682626600951,6.88122480138927));
#7977=CARTESIAN_POINT('Ctrl Pts',(1.32024668026891,0.534238885958241,6.88122480138927));
#7978=CARTESIAN_POINT('Ctrl Pts',(1.29340017822458,0.583825249958668,6.88122480138927));
#7979=CARTESIAN_POINT('Ctrl Pts',(1.26380097432666,0.631696741779596,6.88122480138926));
#7980=CARTESIAN_POINT('Ctrl Pts',(1.23153271624108,0.677572305460653,6.88122480138926));
#7981=CARTESIAN_POINT('Ctrl Pts',(1.2003110151207,0.721959986201897,6.88122480138927));
#7982=CARTESIAN_POINT('Ctrl Pts',(1.16658992943844,0.764479679279131,6.88122480138927));
#7983=CARTESIAN_POINT('Ctrl Pts',(1.13041488599057,0.804840324534032,6.88122480138927));
#7984=CARTESIAN_POINT('Ctrl Pts',(1.09445590942473,0.844959903077031,6.88122480138927));
#7985=CARTESIAN_POINT('Ctrl Pts',(1.0560717388421,0.882946797134589,6.88122480138927));
#7986=CARTESIAN_POINT('Ctrl Pts',(1.01528449697062,0.91846928819733,6.88122480138927));
#7987=CARTESIAN_POINT('Ctrl Pts',(1.00879798113654,0.924118535122891,6.88122480138927));
#7988=CARTESIAN_POINT('Ctrl Pts',(1.00225064991045,0.929705347318732,6.88122480138927));
#7989=CARTESIAN_POINT('Ctrl Pts',(0.995642551412613,0.935228266155693,6.88122480138927));
#7990=CARTESIAN_POINT('Ctrl Pts',(-0.795414167084174,-1.11297035801352,
-9.15933995315754E-16));
#7991=CARTESIAN_POINT('Ctrl Pts',(-0.832947493180536,-1.09280171046842,
-4.40215524741542E-15));
#7992=CARTESIAN_POINT('Ctrl Pts',(-0.86936688691735,-1.07084409499352,-3.25857603395726E-15));
#7993=CARTESIAN_POINT('Ctrl Pts',(-0.904527909503487,-1.04713770592261,
-3.07219527595493E-15));
#7994=CARTESIAN_POINT('Ctrl Pts',(-0.949274147286779,-1.01696873914267,
-2.93443362582291E-15));
#7995=CARTESIAN_POINT('Ctrl Pts',(-0.991983854002586,-0.983969661606057,
-3.24217105220443E-15));
#7996=CARTESIAN_POINT('Ctrl Pts',(-1.0325919733568,-0.948460486377737,-3.64291929955129E-15));
#7997=CARTESIAN_POINT('Ctrl Pts',(-1.07423105118419,-0.912049804611821,
-4.05384173885249E-15));
#7998=CARTESIAN_POINT('Ctrl Pts',(-1.11366113367805,-0.872999428421004,
-7.68613341355709E-16));
#7999=CARTESIAN_POINT('Ctrl Pts',(-1.15078992234189,-0.831604028494677,
-1.89431803576667E-15));
#8000=CARTESIAN_POINT('Ctrl Pts',(-1.1663202195496,-0.814289085373092,-2.36517984142906E-15));
#8001=CARTESIAN_POINT('Ctrl Pts',(-1.18144756318774,-0.796563309565334,
-2.96565948945709E-15));
#8002=CARTESIAN_POINT('Ctrl Pts',(-1.19616365544476,-0.778446114115039,
-2.76167977375508E-15));
#8003=CARTESIAN_POINT('Ctrl Pts',(-1.20483314424882,-0.767772980216839,
-2.64151201246017E-15));
#8004=CARTESIAN_POINT('Ctrl Pts',(-1.21335930009043,-0.756964325554185,
-1.86449801195046E-15));
#8005=CARTESIAN_POINT('Ctrl Pts',(-1.22172559193317,-0.746044338928061,
-1.72084568816899E-15));
#8006=CARTESIAN_POINT('Ctrl Pts',(-1.23769793947646,-0.725196653377617,
-1.44659457621046E-15));
#8007=CARTESIAN_POINT('Ctrl Pts',(-1.25310066142752,-0.70392782386896,-1.09877265170518E-15));
#8008=CARTESIAN_POINT('Ctrl Pts',(-1.26792826560863,-0.68227084872173,-1.16573417585641E-15));
#8009=CARTESIAN_POINT('Ctrl Pts',(-1.30064000206196,-0.634492579573223,
-1.313460518143E-15));
#8010=CARTESIAN_POINT('Ctrl Pts',(-1.33055288609126,-0.584830241555012,
-1.18464778661716E-15));
#8011=CARTESIAN_POINT('Ctrl Pts',(-1.35757841478232,-0.533616942208867,
-4.44089209850063E-16));
#8012=CARTESIAN_POINT('Ctrl Pts',(-1.38506646201561,-0.481527171551913,
3.09143386259586E-16));
#8013=CARTESIAN_POINT('Ctrl Pts',(-1.40956822217026,-0.427832070929981,
-9.2928198748492E-16));
#8014=CARTESIAN_POINT('Ctrl Pts',(-1.43095548368543,-0.372841920597751,
-1.0547118733939E-15));
#8015=CARTESIAN_POINT('Ctrl Pts',(-1.44153762134738,-0.345633512431298,
-1.11677294272112E-15));
#8016=CARTESIAN_POINT('Ctrl Pts',(-1.45135667973785,-0.318107521778687,
-1.09151072745545E-15));
#8017=CARTESIAN_POINT('Ctrl Pts',(-1.46039315561881,-0.290298981848618,
-6.66133814775094E-16));
#8018=CARTESIAN_POINT('Ctrl Pts',(-1.46494353283797,-0.276295807573305,
-4.5083568064057E-16));
#8019=CARTESIAN_POINT('Ctrl Pts',(-1.46929683648255,-0.26221562433059,-2.38820861466436E-15));
#8020=CARTESIAN_POINT('Ctrl Pts',(-1.473441618016,-0.248093948282024,-2.15105711021124E-15));
#8021=CARTESIAN_POINT('Ctrl Pts',(-1.4905537552228,-0.189791223233013,-1.04000775610132E-15));
#8022=CARTESIAN_POINT('Ctrl Pts',(-1.50414431451018,-0.130700983448934,
-7.32518070969078E-16));
#8023=CARTESIAN_POINT('Ctrl Pts',(-1.51411149444636,-0.0711710784181553,
-1.47104550762833E-15));
#8024=CARTESIAN_POINT('Ctrl Pts',(-1.5240471929564,-0.0118291991198427,
-2.6702633386109E-15));
#8025=CARTESIAN_POINT('Ctrl Pts',(-1.53038298344941,0.0479506119131717,
6.12492081269896E-16));
#8026=CARTESIAN_POINT('Ctrl Pts',(-1.53297599397982,0.107852419831135,1.01307850997046E-15));
#8027=CARTESIAN_POINT('Ctrl Pts',(-1.5343216654729,0.13893912555559,8.07247865597284E-16));
#8028=CARTESIAN_POINT('Ctrl Pts',(-1.53465858251287,0.170059062380459,6.33636663361729E-16));
#8029=CARTESIAN_POINT('Ctrl Pts',(-1.53396143973122,0.201169701697847,-2.91433543964104E-16));
#8030=CARTESIAN_POINT('Ctrl Pts',(-1.53315235769005,0.237275733666988,-1.31380156557419E-15));
#8031=CARTESIAN_POINT('Ctrl Pts',(-1.53095064843268,0.273369292680589,-3.47125944024131E-16));
#8032=CARTESIAN_POINT('Ctrl Pts',(-1.52739541139815,0.309398947352701,-1.02695629777827E-15));
#8033=CARTESIAN_POINT('Ctrl Pts',(-1.52629773176855,0.320523105210736,-1.40527035743221E-15));
#8034=CARTESIAN_POINT('Ctrl Pts',(-1.52507166732445,0.331633629961292,-1.02948525143009E-16));
#8035=CARTESIAN_POINT('Ctrl Pts',(-1.5237196856603,0.342722587468097,-8.32667268468867E-17));
#8036=CARTESIAN_POINT('Ctrl Pts',(-1.516518466799,0.401787005328014,-1.28384931635538E-16));
#8037=CARTESIAN_POINT('Ctrl Pts',(-1.50574358938221,0.46029506897729,-2.5884345523775E-15));
#8038=CARTESIAN_POINT('Ctrl Pts',(-1.49164313082402,0.518014064605472,-1.62370117351429E-15));
#8039=CARTESIAN_POINT('Ctrl Pts',(-1.47706888159878,0.577672480950095,-6.26551709089525E-16));
#8040=CARTESIAN_POINT('Ctrl Pts',(-1.45894176921365,0.636488725124688,7.13174734340251E-16));
#8041=CARTESIAN_POINT('Ctrl Pts',(-1.43747991265361,0.694213509478351,-4.16333634234434E-16));
#8042=CARTESIAN_POINT('Ctrl Pts',(-1.42099781437687,0.738544509737268,-1.28376408616919E-15));
#8043=CARTESIAN_POINT('Ctrl Pts',(-1.40254775675702,0.782232068197874,-9.02083324469551E-16));
#8044=CARTESIAN_POINT('Ctrl Pts',(-1.38220782814776,0.825161373923281,-6.66133814775094E-16));
#8045=CARTESIAN_POINT('Ctrl Pts',(-1.37469143189959,0.841025425301725,-6.32268855604997E-16));
#8046=CARTESIAN_POINT('Ctrl Pts',(-1.36691678867014,0.856785892169704,-1.94116254897675E-15));
#8047=CARTESIAN_POINT('Ctrl Pts',(-1.35888726366717,0.872436807123193,-1.72084568816899E-15));
#8048=CARTESIAN_POINT('Ctrl Pts',(-1.35063706597361,0.888517850821735,-1.41388399025223E-15));
#8049=CARTESIAN_POINT('Ctrl Pts',(-1.34211487275061,0.904488002686463,-1.61566361807131E-15));
#8050=CARTESIAN_POINT('Ctrl Pts',(-1.33334349594405,0.920306971938382,-1.58206781009085E-15));
#8051=CARTESIAN_POINT('Ctrl Pts',(-1.30214685892829,0.976569364103196,-1.46257958721175E-15));
#8052=CARTESIAN_POINT('Ctrl Pts',(-1.26776287350155,1.03100157507453,4.98596072913018E-16));
#8053=CARTESIAN_POINT('Ctrl Pts',(-1.23041822401205,1.08333236977297,2.77555756156289E-17));
#8054=CARTESIAN_POINT('Ctrl Pts',(-1.19893362730352,1.12745151372103,-3.6920150857429E-16));
#8055=CARTESIAN_POINT('Ctrl Pts',(-1.16534352389359,1.17007731567397,-1.15789935301514E-15));
#8056=CARTESIAN_POINT('Ctrl Pts',(-1.12975612292984,1.2110393106172,-1.94289029309402E-16));
#8057=CARTESIAN_POINT('Ctrl Pts',(-1.11980830251754,1.2224895024938,8.16785287875133E-19));
#8058=CARTESIAN_POINT('Ctrl Pts',(-1.10970427564496,1.23380962006102,-8.83756491716252E-16));
#8059=CARTESIAN_POINT('Ctrl Pts',(-1.09944608615852,1.24499576190878,-3.05311331771918E-16));
#8060=CARTESIAN_POINT('Ctrl Pts',(-1.09148793970747,1.25367379960387,2.16835242351985E-16));
#8061=CARTESIAN_POINT('Ctrl Pts',(-1.08343792396404,1.2622701055878,-4.67419621806966E-16));
#8062=CARTESIAN_POINT('Ctrl Pts',(-1.07530384816136,1.27077601604308,-2.22044604925031E-16));
#8063=CARTESIAN_POINT('Ctrl Pts',(-1.02993327554411,1.3182206228244,5.7724852838323E-16));
#8064=CARTESIAN_POINT('Ctrl Pts',(-0.98189595159246,1.36291522819749,-1.37872740780286E-15));
#8065=CARTESIAN_POINT('Ctrl Pts',(-0.931398621857827,1.40457604009645,-6.10622663543836E-16));
#8066=CARTESIAN_POINT('Ctrl Pts',(-0.881340571334673,1.44587444216707,1.50800292823326E-16));
#8067=CARTESIAN_POINT('Ctrl Pts',(-0.828864591896417,1.48419258027966,-3.05515458637289E-15));
#8068=CARTESIAN_POINT('Ctrl Pts',(-0.774129732122116,1.51922639018999,-1.52655665885959E-15));
#8069=CARTESIAN_POINT('Ctrl Pts',(-0.764997683666341,1.52507148508949,-1.24297269028027E-15));
#8070=CARTESIAN_POINT('Ctrl Pts',(-0.75580267106898,1.53082507493498,-1.52747238928381E-15));
#8071=CARTESIAN_POINT('Ctrl Pts',(-0.746545333137423,1.53648564199954,-3.88578058618805E-16));
#8072=CARTESIAN_POINT('Ctrl Pts',(0.993445330382434,-1.39216647130147,-0.198796524485181));
#8073=CARTESIAN_POINT('Ctrl Pts',(1.45224744664474,-1.06478123128123,-0.167326491865807));
#8074=CARTESIAN_POINT('Ctrl Pts',(2.01346727495692,0.0729463614329333,-0.104395023997457));
#8075=CARTESIAN_POINT('Ctrl Pts',(1.04452544803256,1.72489834357427,-0.0100021208801329));
#8076=CARTESIAN_POINT('Ctrl Pts',(-0.865118107719488,1.81944815671647,0.0843821848667926));
#8077=CARTESIAN_POINT('Ctrl Pts',(-1.99580016919685,0.279114534669996,0.178766490613719));
#8078=CARTESIAN_POINT('Ctrl Pts',(-1.33062056689224,-1.51369898506524,0.273150796360644));
#8079=CARTESIAN_POINT('Ctrl Pts',(0.532139236212413,-1.94360970629842,0.367535102107569));
#8080=CARTESIAN_POINT('Ctrl Pts',(1.91595060805295,-0.624764979528343,0.461919407854496));
#8081=CARTESIAN_POINT('Ctrl Pts',(1.57557243209307,1.25651211697159,0.556303713601421));
#8082=CARTESIAN_POINT('Ctrl Pts',(-0.18272721901878,2.00691771985262,0.650688019348347));
#8083=CARTESIAN_POINT('Ctrl Pts',(-1.77657640637496,0.951289839344929,0.745072325095271));
#8084=CARTESIAN_POINT('Ctrl Pts',(-1.77163592240772,-0.960459485878452,
0.839456630842199));
#8085=CARTESIAN_POINT('Ctrl Pts',(-0.172344824174458,-2.00784825297573,
0.933840936589122));
#8086=CARTESIAN_POINT('Ctrl Pts',(1.58204326623752,-1.24832180902719,1.02822524233605));
#8087=CARTESIAN_POINT('Ctrl Pts',(1.91270394017647,0.634610748931089,1.12260954808298));
#8088=CARTESIAN_POINT('Ctrl Pts',(0.522064739489251,1.94643602090733,1.2169938538299));
#8089=CARTESIAN_POINT('Ctrl Pts',(-1.33839596074812,1.50660635374839,1.31137815957683));
#8090=CARTESIAN_POINT('Ctrl Pts',(-1.9943941749754,-0.289064038131091,1.40576246532376));
#8091=CARTESIAN_POINT('Ctrl Pts',(-0.855577327983737,-1.82459674855572,
1.50014677107068));
#8092=CARTESIAN_POINT('Ctrl Pts',(1.05319913699118,-1.71812039355476,1.59453107681761));
#8093=CARTESIAN_POINT('Ctrl Pts',(2.01417019051478,-0.0654559897729185,
1.68891538256453));
#8094=CARTESIAN_POINT('Ctrl Pts',(1.16252919819725,1.64611417447018,1.78329968831146));
#8095=CARTESIAN_POINT('Ctrl Pts',(-0.735306610103401,1.87629694805414,1.87768399405838));
#8096=CARTESIAN_POINT('Ctrl Pts',(-1.97141799434173,0.417943928532112,1.97206829980531));
#8097=CARTESIAN_POINT('Ctrl Pts',(-1.43339131998399,-1.41652933494684,2.06645260555223));
#8098=CARTESIAN_POINT('Ctrl Pts',(0.394587103969732,-1.97622545662158,2.16083691129916));
#8099=CARTESIAN_POINT('Ctrl Pts',(1.86746478339235,-0.757457139826309,2.25522121704609));
#8100=CARTESIAN_POINT('Ctrl Pts',(1.65975501098531,1.14296952681729,2.34960552279301));
#8101=CARTESIAN_POINT('Ctrl Pts',(-0.0416179720839357,2.01480370776058,
2.44398982853993));
#8102=CARTESIAN_POINT('Ctrl Pts',(-1.70553769649486,1.07345572889199,2.53837413428687));
#8103=CARTESIAN_POINT('Ctrl Pts',(-1.83459300117589,-0.833927188731956,
2.63275844003379));
#8104=CARTESIAN_POINT('Ctrl Pts',(-0.312643154862414,-1.99083406990042,
2.72714274578071));
#8105=CARTESIAN_POINT('Ctrl Pts',(1.49066362390716,-1.35612978599523,2.82152705152764));
#8106=CARTESIAN_POINT('Ctrl Pts',(1.95247759205483,0.498996281183202,2.91591135727456));
#8107=CARTESIAN_POINT('Ctrl Pts',(0.657198537587743,1.9050606600091,3.0102956630215));
#8108=CARTESIAN_POINT('Ctrl Pts',(-1.22951315076462,1.5967039325468,3.10467996876841));
#8109=CARTESIAN_POINT('Ctrl Pts',(-2.0097491554954,-0.148574453055689,3.19906427451535));
#8110=CARTESIAN_POINT('Ctrl Pts',(-0.981351743535662,-1.76014624153099,
3.29344858026226));
#8111=CARTESIAN_POINT('Ctrl Pts',(0.930193474225359,-1.78770974619056,3.3878328860092));
#8112=CARTESIAN_POINT('Ctrl Pts',(2.0046297439011,-0.206459744217345,3.48221719175612));
#8113=CARTESIAN_POINT('Ctrl Pts',(1.27503970860364,1.5605895609024,3.57660149750304));
#8114=CARTESIAN_POINT('Ctrl Pts',(-0.601996722321556,1.92321761182553,3.67098580324997));
#8115=CARTESIAN_POINT('Ctrl Pts',(-1.93727828510637,0.555084572084459,3.76537010899689));
#8116=CARTESIAN_POINT('Ctrl Pts',(-1.52914513651331,-1.31258568771001,3.85975441474383));
#8117=CARTESIAN_POINT('Ctrl Pts',(0.255111487644501,-1.9990208015502,3.95413872049074));
#8118=CARTESIAN_POINT('Ctrl Pts',(1.80978564859574,-0.886477265476602,4.04852302623767));
#8119=CARTESIAN_POINT('Ctrl Pts',(1.73577953761973,1.02383369393503,4.1429073319846));
#8120=CARTESIAN_POINT('Ctrl Pts',(0.0996934689531183,2.01276606903392,4.23729163773152));
#8121=CARTESIAN_POINT('Ctrl Pts',(-1.62610973620759,1.1903500163963,4.33167594347845));
#8122=CARTESIAN_POINT('Ctrl Pts',(-1.88852812046539,-0.703297642606548,
4.42606024922538));
#8123=CARTESIAN_POINT('Ctrl Pts',(-0.45140352546393,-1.96402670430346,4.5204445549723));
#8124=CARTESIAN_POINT('Ctrl Pts',(1.39195261233386,-1.45726934984146,4.61482886071923));
#8125=CARTESIAN_POINT('Ctrl Pts',(1.98264893371114,0.360928305159485,4.70921316646615));
#8126=CARTESIAN_POINT('Ctrl Pts',(0.789100138196465,1.8543157821788,4.80359747221308));
#8127=CARTESIAN_POINT('Ctrl Pts',(-1.1145834876982,1.67894897510415,4.89798177796));
#8128=CARTESIAN_POINT('Ctrl Pts',(-2.01522007683398,-0.00735424236076328,
4.99236608370693));
#8129=CARTESIAN_POINT('Ctrl Pts',(-1.10229979727379,-1.68703920103769,5.08675038945385));
#8130=CARTESIAN_POINT('Ctrl Pts',(0.802613049915853,-1.8485070059658,5.18113469520079));
#8131=CARTESIAN_POINT('Ctrl Pts',(1.98523041358707,-0.346448189900541,5.2755190009477));
#8132=CARTESIAN_POINT('Ctrl Pts',(1.38127946790861,1.46739002464785,5.36990330669464));
#8133=CARTESIAN_POINT('Ctrl Pts',(-0.465726131974941,1.96067946021252,5.46428761244155));
#8134=CARTESIAN_POINT('Ctrl Pts',(-1.89361099983627,0.689495864182337,5.55867191818849));
#8135=CARTESIAN_POINT('Ctrl Pts',(-1.61737836162868,-1.20218778503015,5.6530562239354));
#8136=CARTESIAN_POINT('Ctrl Pts',(0.114380917309485,-2.01198269156394,5.74744052968234));
#8137=CARTESIAN_POINT('Ctrl Pts',(1.74320644116969,-1.01114171560858,5.84182483542925));
#8138=CARTESIAN_POINT('Ctrl Pts',(1.80326630572656,0.899670337824012,5.93620914117619));
#8139=CARTESIAN_POINT('Ctrl Pts',(0.240516672199542,2.00081475934751,6.03059344692311));
#8140=CARTESIAN_POINT('Ctrl Pts',(-1.53868838529779,1.30141816562462,6.12497775267004));
#8141=CARTESIAN_POINT('Ctrl Pts',(-1.93316787609034,-0.569262659056326,
6.21936205841696));
#8142=CARTESIAN_POINT('Ctrl Pts',(-0.587958060108795,-1.92745847599559,
6.31374636416389));
#8143=CARTESIAN_POINT('Ctrl Pts',(1.28642289607729,-1.5514354136967,6.40813066991081));
#8144=CARTESIAN_POINT('Ctrl Pts',(2.00301810604117,0.221453619752493,6.50251497565774));
#8145=CARTESIAN_POINT('Ctrl Pts',(0.917218545591866,1.79374777349143,6.59689928140466));
#8146=CARTESIAN_POINT('Ctrl Pts',(-0.994357215842109,1.75429798909866,6.69128358715159));
#8147=CARTESIAN_POINT('Ctrl Pts',(-2.01046165517952,0.131074529887547,6.78567042953023));
#8148=CARTESIAN_POINT('Ctrl Pts',(-1.48244620740138,-1.02224374889723,6.84859583665991));
#8149=CARTESIAN_POINT('Ctrl Pts',(-1.03343210425486,-1.36274693512055,6.88005980854061));
#8150=CARTESIAN_POINT('Ctrl Pts',(0.926331970733012,-1.29811703926643,-0.132089456432433));
#8151=CARTESIAN_POINT('Ctrl Pts',(1.35413917414512,-0.992848691525437,-0.100619423813059));
#8152=CARTESIAN_POINT('Ctrl Pts',(1.87744514144454,0.0680183847841591,-0.0376879559447101));
#8153=CARTESIAN_POINT('Ctrl Pts',(0.973961311373108,1.60837082127324,0.0567049471726145));
#8154=CARTESIAN_POINT('Ctrl Pts',(-0.806674043484716,1.69653321135336,0.15108925291954));
#8155=CARTESIAN_POINT('Ctrl Pts',(-1.86097155764947,0.260258626271408,0.245473558666466));
#8156=CARTESIAN_POINT('Ctrl Pts',(-1.24072894031588,-1.41143928211153,0.33985786441339));
#8157=CARTESIAN_POINT('Ctrl Pts',(0.496189948565409,-1.81230688243118,0.434242170160317));
#8158=CARTESIAN_POINT('Ctrl Pts',(1.78651632687384,-0.582558251603697,0.528626475907242));
#8159=CARTESIAN_POINT('Ctrl Pts',(1.46913279615649,1.17162697328914,0.623010781654168));
#8160=CARTESIAN_POINT('Ctrl Pts',(-0.170382868310501,1.87133804918526,0.717395087401093));
#8161=CARTESIAN_POINT('Ctrl Pts',(-1.65655771218086,0.887024343130625,0.811779393148019));
#8162=CARTESIAN_POINT('Ctrl Pts',(-1.65195098837856,-0.895574523482337,
0.906163698894944));
#8163=CARTESIAN_POINT('Ctrl Pts',(-0.160701868276632,-1.87220571905636,
1.00054800464187));
#8164=CARTESIAN_POINT('Ctrl Pts',(1.47516648554233,-1.16398997116428,1.09493231038879));
#8165=CARTESIAN_POINT('Ctrl Pts',(1.78348899143789,0.591738878554484,1.18931661613572));
#8166=CARTESIAN_POINT('Ctrl Pts',(0.486796046235497,1.81494226205554,1.28370092188264));
#8167=CARTESIAN_POINT('Ctrl Pts',(-1.24797905835808,1.40482580178756,1.37808522762957));
#8168=CARTESIAN_POINT('Ctrl Pts',(-1.85966054700985,-0.269535979405069,
1.4724695333765));
#8169=CARTESIAN_POINT('Ctrl Pts',(-0.797777802267743,-1.70133398405729,
1.56685383912342));
#8170=CARTESIAN_POINT('Ctrl Pts',(0.982049039143188,-1.60205076358401,1.66123814487035));
#8171=CARTESIAN_POINT('Ctrl Pts',(1.87810057072086,-0.0610340339304603,
1.75562245061727));
#8172=CARTESIAN_POINT('Ctrl Pts',(1.08399318036572,1.53490900873377,1.8500067563642));
#8173=CARTESIAN_POINT('Ctrl Pts',(-0.685632113211391,1.74954151619218,1.94439106211112));
#8174=CARTESIAN_POINT('Ctrl Pts',(-1.83823654909533,0.389709238276857,2.03877536785805));
#8175=CARTESIAN_POINT('Ctrl Pts',(-1.33655689514511,-1.32083404120213,2.13315967360497));
#8176=CARTESIAN_POINT('Ctrl Pts',(0.367930311278841,-1.8427192376457,2.2275439793519));
#8177=CARTESIAN_POINT('Ctrl Pts',(1.74130601873017,-0.706286238026784,2.32192828509883));
#8178=CARTESIAN_POINT('Ctrl Pts',(1.54762832260548,1.06575488543175,2.41631259084575));
#8179=CARTESIAN_POINT('Ctrl Pts',(-0.0388064213695487,1.87869128996917,
2.51069689659268));
#8180=CARTESIAN_POINT('Ctrl Pts',(-1.59031810532073,1.00093717331819,2.6050812023396));
#8181=CARTESIAN_POINT('Ctrl Pts',(-1.71065492815597,-0.777590263460737,
2.69946550808653));
#8182=CARTESIAN_POINT('Ctrl Pts',(-0.291522181364917,-1.85634094899147,
2.79384981383345));
#8183=CARTESIAN_POINT('Ctrl Pts',(1.38996010168205,-1.26451485432732,2.88823411958038));
#8184=CARTESIAN_POINT('Ctrl Pts',(1.82057568780754,0.465286004574547,2.9826184253273));
#8185=CARTESIAN_POINT('Ctrl Pts',(0.612800722765632,1.77636206198968,3.07700273107423));
#8186=CARTESIAN_POINT('Ctrl Pts',(-1.14645195377939,1.48883673341525,3.17138703682116));
#8187=CARTESIAN_POINT('Ctrl Pts',(-1.87397820388604,-0.138537332342868,
3.26577134256808));
#8188=CARTESIAN_POINT('Ctrl Pts',(-0.915055380271112,-1.64123750631354,
3.36015564831501));
#8189=CARTESIAN_POINT('Ctrl Pts',(0.867353167597517,-1.66693892622134,3.45453995406193));
#8190=CARTESIAN_POINT('Ctrl Pts',(1.86920464012152,-0.192512115049408,3.54892425980886));
#8191=CARTESIAN_POINT('Ctrl Pts',(1.18890291182804,1.45516211032929,3.64330856555578));
#8192=CARTESIAN_POINT('Ctrl Pts',(-0.561328130606112,1.79329239971861,3.73769287130272));
#8193=CARTESIAN_POINT('Ctrl Pts',(-1.80640318779295,0.517585185472195,3.83207717704963));
#8194=CARTESIAN_POINT('Ctrl Pts',(-1.42584195075725,-1.22391242846177,3.92646148279657));
#8195=CARTESIAN_POINT('Ctrl Pts',(0.237877133123564,-1.86397461642245,4.02084578854348));
#8196=CARTESIAN_POINT('Ctrl Pts',(1.68752346525464,-0.826590258391798,4.11523009429042));
#8197=CARTESIAN_POINT('Ctrl Pts',(1.61851692354558,0.954667412891863,4.20961440003733));
#8198=CARTESIAN_POINT('Ctrl Pts',(0.0929585602148776,1.87679130630668,4.30399870578427));
#8199=CARTESIAN_POINT('Ctrl Pts',(-1.51625599366343,1.10993453069628,4.39838301153119));
#8200=CARTESIAN_POINT('Ctrl Pts',(-1.76094639746502,-0.655785548900625,
4.49276731727812));
#8201=CARTESIAN_POINT('Ctrl Pts',(-0.420908433056757,-1.83134458628871,
4.58715162302504));
#8202=CARTESIAN_POINT('Ctrl Pts',(1.29791762779116,-1.35882181680575,4.68153592877197));
#8203=CARTESIAN_POINT('Ctrl Pts',(1.84870876923778,0.336545371936081,4.77592023451889));
#8204=CARTESIAN_POINT('Ctrl Pts',(0.735791556682662,1.7290453136518,4.87030454026581));
#8205=CARTESIAN_POINT('Ctrl Pts',(-1.03928649834056,1.56552561605949,4.96468884601275));
#8206=CARTESIAN_POINT('Ctrl Pts',(-1.8790795307435,-0.00685741792825145,
5.05907315175966));
#8207=CARTESIAN_POINT('Ctrl Pts',(-1.02783264697026,-1.57306929733063,5.1534574575066));
#8208=CARTESIAN_POINT('Ctrl Pts',(0.748391587867626,-1.72362895610057,5.24784176325352));
#8209=CARTESIAN_POINT('Ctrl Pts',(1.8511158542255,-0.323043477776379,5.34222606900045));
#8210=CARTESIAN_POINT('Ctrl Pts',(1.28796552010391,1.36825877760454,5.43661037474737));
#8211=CARTESIAN_POINT('Ctrl Pts',(-0.434263459155965,1.82822346918195,5.53099468049429));
#8212=CARTESIAN_POINT('Ctrl Pts',(-1.76568589698316,0.642916165738485,5.62537898624123));
#8213=CARTESIAN_POINT('Ctrl Pts',(-1.50811447729253,-1.12097258504345,5.71976329198815));
#8214=CARTESIAN_POINT('Ctrl Pts',(0.106653780842439,-1.87606085081667,5.81414759773507));
#8215=CARTESIAN_POINT('Ctrl Pts',(1.62544209395152,-0.942832855985621,5.908531903482));
#8216=CARTESIAN_POINT('Ctrl Pts',(1.68144454420765,0.838892057327132,6.00291620922892));
#8217=CARTESIAN_POINT('Ctrl Pts',(0.224268287482887,1.86564738130541,6.09730051497587));
#8218=CARTESIAN_POINT('Ctrl Pts',(-1.43474049422346,1.21349934137462,6.19168482072277));
#8219=CARTESIAN_POINT('Ctrl Pts',(-1.80257046225899,-0.530805455218523,
6.28606912646971));
#8220=CARTESIAN_POINT('Ctrl Pts',(-0.548237866616442,-1.7972467673563,6.38045343221663));
#8221=CARTESIAN_POINT('Ctrl Pts',(1.19951709477623,-1.44662638223021,6.47483773796356));
#8222=CARTESIAN_POINT('Ctrl Pts',(1.86770187833963,0.206493061809774,6.56922204371047));
#8223=CARTESIAN_POINT('Ctrl Pts',(0.855254775422712,1.67256904753542,6.66360634945741));
#8224=CARTESIAN_POINT('Ctrl Pts',(-0.927182252705367,1.6357843394051,6.75799065520433));
#8225=CARTESIAN_POINT('Ctrl Pts',(-1.87464256982179,0.122219636924447,6.85237749758299));
#8226=CARTESIAN_POINT('Ctrl Pts',(-1.38229782234636,-0.953184878448155,
6.91530290471266));
#8227=CARTESIAN_POINT('Ctrl Pts',(-0.963617391391471,-1.27068497421457,
6.94676687659335));
#8228=CARTESIAN_POINT('Ctrl Pts',(0.859218611083588,-1.20406760723138,-0.0653823883796859));
#8229=CARTESIAN_POINT('Ctrl Pts',(1.25603090164551,-0.920916151769643,-0.0339123557603118));
#8230=CARTESIAN_POINT('Ctrl Pts',(1.74142300793214,0.0630904081353831,0.0290191121080374));
#8231=CARTESIAN_POINT('Ctrl Pts',(0.903397174713665,1.49184329897221,0.123412015225362));
#8232=CARTESIAN_POINT('Ctrl Pts',(-0.748229979249945,1.57361826599023,0.217796320972287));
#8233=CARTESIAN_POINT('Ctrl Pts',(-1.72614294610208,0.24140271787282,0.312180626719213));
#8234=CARTESIAN_POINT('Ctrl Pts',(-1.15083731373951,-1.30917957915784,0.406564932466139));
#8235=CARTESIAN_POINT('Ctrl Pts',(0.460240660918409,-1.68100405856396,0.500949238213064));
#8236=CARTESIAN_POINT('Ctrl Pts',(1.65708204569473,-0.540351523679055,0.59533354395999));
#8237=CARTESIAN_POINT('Ctrl Pts',(1.36269316021993,1.08674182960668,0.689717849706915));
#8238=CARTESIAN_POINT('Ctrl Pts',(-0.158038517602226,1.7357583785179,0.784102155453842));
#8239=CARTESIAN_POINT('Ctrl Pts',(-1.53653901798676,0.822758846916326,0.878486461200766));
#8240=CARTESIAN_POINT('Ctrl Pts',(-1.53226605434941,-0.830689561086225,
0.972870766947694));
#8241=CARTESIAN_POINT('Ctrl Pts',(-0.149058912378804,-1.73656318513701,
1.06725507269462));
#8242=CARTESIAN_POINT('Ctrl Pts',(1.36828970484713,-1.07965813330138,1.16163937844154));
#8243=CARTESIAN_POINT('Ctrl Pts',(1.65427404269931,0.54886700817788,1.25602368418847));
#8244=CARTESIAN_POINT('Ctrl Pts',(0.451527352981743,1.68344850320373,1.3504079899354));
#8245=CARTESIAN_POINT('Ctrl Pts',(-1.15756215596805,1.30304524982673,1.44479229568232));
#8246=CARTESIAN_POINT('Ctrl Pts',(-1.72492691904432,-0.250007920679045,
1.53917660142925));
#8247=CARTESIAN_POINT('Ctrl Pts',(-0.739978276551748,-1.57807121955886,
1.63356090717617));
#8248=CARTESIAN_POINT('Ctrl Pts',(0.910898941295185,-1.48598113361326,1.7279452129231));
#8249=CARTESIAN_POINT('Ctrl Pts',(1.74203095092696,-0.0566120780880063,
1.82232951867002));
#8250=CARTESIAN_POINT('Ctrl Pts',(1.00545716253417,1.42370384299737,1.91671382441695));
#8251=CARTESIAN_POINT('Ctrl Pts',(-0.635957616319379,1.6227860843302,2.01109813016387));
#8252=CARTESIAN_POINT('Ctrl Pts',(-1.70505510384895,0.361474548021605,2.1054824359108));
#8253=CARTESIAN_POINT('Ctrl Pts',(-1.23972247030623,-1.22513874745744,2.19986674165772));
#8254=CARTESIAN_POINT('Ctrl Pts',(0.341273518587947,-1.70921301866982,2.29425104740465));
#8255=CARTESIAN_POINT('Ctrl Pts',(1.61514725406801,-0.655115336227261,2.38863535315157));
#8256=CARTESIAN_POINT('Ctrl Pts',(1.43550163422564,0.988540244046207,2.4830196588985));
#8257=CARTESIAN_POINT('Ctrl Pts',(-0.0359948706551594,1.74257887217777,
2.57740396464543));
#8258=CARTESIAN_POINT('Ctrl Pts',(-1.47509851414659,0.928418617744392,2.67178827039235));
#8259=CARTESIAN_POINT('Ctrl Pts',(-1.58671685513604,-0.721253338189517,
2.76617257613928));
#8260=CARTESIAN_POINT('Ctrl Pts',(-0.27040120786742,-1.72184782808252,2.8605568818862));
#8261=CARTESIAN_POINT('Ctrl Pts',(1.28925657945695,-1.1728999226594,2.95494118763313));
#8262=CARTESIAN_POINT('Ctrl Pts',(1.68867378356024,0.431575727965893,3.04932549338005));
#8263=CARTESIAN_POINT('Ctrl Pts',(0.56840290794352,1.64766346397025,3.14370979912698));
#8264=CARTESIAN_POINT('Ctrl Pts',(-1.06339075679415,1.38096953428369,3.2380941048739));
#8265=CARTESIAN_POINT('Ctrl Pts',(-1.73820725227668,-0.128500211630046,
3.33247841062083));
#8266=CARTESIAN_POINT('Ctrl Pts',(-0.848759017006559,-1.52232877109609,
3.42686271636775));
#8267=CARTESIAN_POINT('Ctrl Pts',(0.804512860969673,-1.54616810625213,3.52124702211469));
#8268=CARTESIAN_POINT('Ctrl Pts',(1.73377953634196,-0.17856448588147,3.61563132786161));
#8269=CARTESIAN_POINT('Ctrl Pts',(1.10276611505244,1.34973465975617,3.71001563360853));
#8270=CARTESIAN_POINT('Ctrl Pts',(-0.520659538890669,1.6633671876117,3.80439993935546));
#8271=CARTESIAN_POINT('Ctrl Pts',(-1.67552809047953,0.480085798859931,3.89878424510239));
#8272=CARTESIAN_POINT('Ctrl Pts',(-1.32253876500119,-1.13523916921351,3.99316855084931));
#8273=CARTESIAN_POINT('Ctrl Pts',(0.220642778602628,-1.7289284312947,4.08755285659624));
#8274=CARTESIAN_POINT('Ctrl Pts',(1.56526128191355,-0.766703251306995,4.18193716234316));
#8275=CARTESIAN_POINT('Ctrl Pts',(1.50125430947145,0.88550113184869,4.27632146809009));
#8276=CARTESIAN_POINT('Ctrl Pts',(0.0862236514766394,1.74081654357945,4.37070577383701));
#8277=CARTESIAN_POINT('Ctrl Pts',(-1.40640225111927,1.02951904499627,4.46509007958394));
#8278=CARTESIAN_POINT('Ctrl Pts',(-1.63336467446466,-0.608273455194703,
4.55947438533086));
#8279=CARTESIAN_POINT('Ctrl Pts',(-0.390413340649585,-1.69866246827398,
4.65385869107779));
#8280=CARTESIAN_POINT('Ctrl Pts',(1.20388264324848,-1.26037428377003,4.74824299682472));
#8281=CARTESIAN_POINT('Ctrl Pts',(1.71476860476443,0.312162438712672,4.84262730257164));
#8282=CARTESIAN_POINT('Ctrl Pts',(0.682482975168861,1.60377484512479,4.93701160831856));
#8283=CARTESIAN_POINT('Ctrl Pts',(-0.963989508982937,1.45210225701483,5.03139591406549));
#8284=CARTESIAN_POINT('Ctrl Pts',(-1.74293898465302,-0.00636059349573666,
5.12578021981242));
#8285=CARTESIAN_POINT('Ctrl Pts',(-0.953365496666722,-1.45909939362356,
5.22016452555934));
#8286=CARTESIAN_POINT('Ctrl Pts',(0.694170125819397,-1.59875090623536,5.31454883130627));
#8287=CARTESIAN_POINT('Ctrl Pts',(1.71700129486393,-0.299638765652215,5.40893313705319));
#8288=CARTESIAN_POINT('Ctrl Pts',(1.19465157229921,1.26912753056122,5.50331744280012));
#8289=CARTESIAN_POINT('Ctrl Pts',(-0.402800786336985,1.69576747815139,5.59770174854704));
#8290=CARTESIAN_POINT('Ctrl Pts',(-1.63776079413004,0.596336467294631,5.69208605429397));
#8291=CARTESIAN_POINT('Ctrl Pts',(-1.39885059295638,-1.03975738505673,5.7864703600409));
#8292=CARTESIAN_POINT('Ctrl Pts',(0.09892664437539,-1.74013901006941,5.88085466578782));
#8293=CARTESIAN_POINT('Ctrl Pts',(1.50767774673337,-0.874523996362657,5.97523897153475));
#8294=CARTESIAN_POINT('Ctrl Pts',(1.55962278268874,0.778113776830252,6.06962327728167));
#8295=CARTESIAN_POINT('Ctrl Pts',(0.208019902766231,1.73048000326329,6.1640075830286));
#8296=CARTESIAN_POINT('Ctrl Pts',(-1.33079260314915,1.12558051712463,6.25839188877553));
#8297=CARTESIAN_POINT('Ctrl Pts',(-1.67197304842765,-0.49234825138072,6.35277619452245));
#8298=CARTESIAN_POINT('Ctrl Pts',(-0.508517673124086,-1.667035058717,6.44716050026938));
#8299=CARTESIAN_POINT('Ctrl Pts',(1.11261129347517,-1.34181735076373,6.5415448060163));
#8300=CARTESIAN_POINT('Ctrl Pts',(1.7323856506381,0.191532503867054,6.63592911176323));
#8301=CARTESIAN_POINT('Ctrl Pts',(0.793291005253558,1.55139032157942,6.73031341751015));
#8302=CARTESIAN_POINT('Ctrl Pts',(-0.860007289568625,1.51727068971153,6.82469772325708));
#8303=CARTESIAN_POINT('Ctrl Pts',(-1.73882348446406,0.113364743961346,6.91908456563572));
#8304=CARTESIAN_POINT('Ctrl Pts',(-1.28214943729133,-0.884126007999086,
6.9820099727654));
#8305=CARTESIAN_POINT('Ctrl Pts',(-0.893802678528082,-1.17862301330859,
7.0134739446461));
#8306=CARTESIAN_POINT('Ctrl Pts',(0.792105251434166,-1.11001817519634,0.00132467967306148));
#8307=CARTESIAN_POINT('Ctrl Pts',(1.1579226291459,-0.84898361201385,0.0327947122924356));
#8308=CARTESIAN_POINT('Ctrl Pts',(1.60540087441976,0.058162431486608,0.0957261801607845));
#8309=CARTESIAN_POINT('Ctrl Pts',(0.83283303805422,1.37531577667117,0.19011908327811));
#8310=CARTESIAN_POINT('Ctrl Pts',(-0.689785915015175,1.45070332062712,0.284503389025035));
#8311=CARTESIAN_POINT('Ctrl Pts',(-1.59131433455471,0.222546809474231,0.378887694771962));
#8312=CARTESIAN_POINT('Ctrl Pts',(-1.06094568716315,-1.20691987620413,0.473272000518886));
#8313=CARTESIAN_POINT('Ctrl Pts',(0.424291373271407,-1.54970123469673,0.567656306265813));
#8314=CARTESIAN_POINT('Ctrl Pts',(1.52764776451562,-0.498144795754411,0.662040612012736));
#8315=CARTESIAN_POINT('Ctrl Pts',(1.25625352428336,1.00185668592423,0.756424917759663));
#8316=CARTESIAN_POINT('Ctrl Pts',(-0.145694166893949,1.60017870785054,0.850809223506588));
#8317=CARTESIAN_POINT('Ctrl Pts',(-1.41652032379266,0.758493350702024,0.945193529253515));
#8318=CARTESIAN_POINT('Ctrl Pts',(-1.41258112032025,-0.765804598690109,
1.03957783500044));
#8319=CARTESIAN_POINT('Ctrl Pts',(-0.137415956480979,-1.60092065121764,
1.13396214074737));
#8320=CARTESIAN_POINT('Ctrl Pts',(1.26141292415194,-0.995326295438471,1.22834644649429));
#8321=CARTESIAN_POINT('Ctrl Pts',(1.52505909396075,0.505995137801276,1.32273075224122));
#8322=CARTESIAN_POINT('Ctrl Pts',(0.416258659727988,1.55195474435194,1.41711505798814));
#8323=CARTESIAN_POINT('Ctrl Pts',(-1.06714525357801,1.20126469786591,1.51149936373507));
#8324=CARTESIAN_POINT('Ctrl Pts',(-1.59019329107878,-0.230479861953022,
1.605883669482));
#8325=CARTESIAN_POINT('Ctrl Pts',(-0.682178750835754,-1.45480845506043,
1.70026797522892));
#8326=CARTESIAN_POINT('Ctrl Pts',(0.839748843447184,-1.3699115036425,1.79465228097585));
#8327=CARTESIAN_POINT('Ctrl Pts',(1.60596133113304,-0.0521901222455495,
1.88903658672277));
#8328=CARTESIAN_POINT('Ctrl Pts',(0.926921144702626,1.31249867726097,1.9834208924697));
#8329=CARTESIAN_POINT('Ctrl Pts',(-0.586283119427368,1.49603065246823,2.07780519821662));
#8330=CARTESIAN_POINT('Ctrl Pts',(-1.57187365860257,0.33323985776635,2.17218950396355));
#8331=CARTESIAN_POINT('Ctrl Pts',(-1.14288804546734,-1.12944345371274,2.26657380971047));
#8332=CARTESIAN_POINT('Ctrl Pts',(0.314616725897053,-1.57570679969394,2.3609581154574));
#8333=CARTESIAN_POINT('Ctrl Pts',(1.48898848940584,-0.603944434427737,2.45534242120432));
#8334=CARTESIAN_POINT('Ctrl Pts',(1.32337494584579,0.911325602660668,2.54972672695125));
#8335=CARTESIAN_POINT('Ctrl Pts',(-0.0331833199407702,1.60646645438636,
2.64411103269818));
#8336=CARTESIAN_POINT('Ctrl Pts',(-1.35987892297247,0.855900062170592,2.7384953384451));
#8337=CARTESIAN_POINT('Ctrl Pts',(-1.46277878211612,-0.664916412918296,
2.83287964419203));
#8338=CARTESIAN_POINT('Ctrl Pts',(-0.249280234369926,-1.58735470717356,
2.92726394993895));
#8339=CARTESIAN_POINT('Ctrl Pts',(1.18855305723184,-1.08128499099147,3.02164825568588));
#8340=CARTESIAN_POINT('Ctrl Pts',(1.55677187931295,0.397865451357236,3.1160325614328));
#8341=CARTESIAN_POINT('Ctrl Pts',(0.524005093121412,1.51896486595083,3.21041686717973));
#8342=CARTESIAN_POINT('Ctrl Pts',(-0.98032955980891,1.27310233515215,3.30480117292666));
#8343=CARTESIAN_POINT('Ctrl Pts',(-1.60243630066732,-0.118463090917224,
3.39918547867358));
#8344=CARTESIAN_POINT('Ctrl Pts',(-0.782462653742007,-1.40342003587865,
3.49356978442051));
#8345=CARTESIAN_POINT('Ctrl Pts',(0.74167255434183,-1.42539728628291,3.58795409016743));
#8346=CARTESIAN_POINT('Ctrl Pts',(1.59835443256238,-0.164616856713533,3.68233839591436));
#8347=CARTESIAN_POINT('Ctrl Pts',(1.01662931827683,1.24430720918307,3.77672270166128));
#8348=CARTESIAN_POINT('Ctrl Pts',(-0.479990947175226,1.53344197550478,3.87110700740821));
#8349=CARTESIAN_POINT('Ctrl Pts',(-1.54465299316611,0.442586412247669,3.96549131315514));
#8350=CARTESIAN_POINT('Ctrl Pts',(-1.21923557924511,-1.04656590996525,4.05987561890206));
#8351=CARTESIAN_POINT('Ctrl Pts',(0.203408424081691,-1.59388224616695,4.15425992464898));
#8352=CARTESIAN_POINT('Ctrl Pts',(1.44299909857244,-0.706816244222193,4.24864423039592));
#8353=CARTESIAN_POINT('Ctrl Pts',(1.3839916953973,0.816334850805521,4.34302853614283));
#8354=CARTESIAN_POINT('Ctrl Pts',(0.0794887427383994,1.60484178085219,4.43741284188977));
#8355=CARTESIAN_POINT('Ctrl Pts',(-1.29654850857511,0.949103559296265,4.53179714763668));
#8356=CARTESIAN_POINT('Ctrl Pts',(-1.50578295146431,-0.56076136148878,4.62618145338362));
#8357=CARTESIAN_POINT('Ctrl Pts',(-0.359918248242413,-1.56598035025924,
4.72056575913053));
#8358=CARTESIAN_POINT('Ctrl Pts',(1.10984765870579,-1.16192675073432,4.81495006487747));
#8359=CARTESIAN_POINT('Ctrl Pts',(1.58082844029107,0.287779505489267,4.90933437062438));
#8360=CARTESIAN_POINT('Ctrl Pts',(0.62917439365506,1.47850437659778,5.00371867637132));
#8361=CARTESIAN_POINT('Ctrl Pts',(-0.888692519625303,1.33867889797018,5.09810298211823));
#8362=CARTESIAN_POINT('Ctrl Pts',(-1.60679843856254,-0.00586376906322344,
5.19248728786518));
#8363=CARTESIAN_POINT('Ctrl Pts',(-0.878898346363189,-1.34512948991649,
5.28687159361209));
#8364=CARTESIAN_POINT('Ctrl Pts',(0.639948663771169,-1.47387285637013,5.38125589935902));
#8365=CARTESIAN_POINT('Ctrl Pts',(1.58288673550236,-0.276234053528054,5.47564020510594));
#8366=CARTESIAN_POINT('Ctrl Pts',(1.10133762449452,1.16999628351791,5.57002451085287));
#8367=CARTESIAN_POINT('Ctrl Pts',(-0.371338113518008,1.56331148712083,5.6644088165998));
#8368=CARTESIAN_POINT('Ctrl Pts',(-1.50983569127691,0.54975676885078,5.75879312234672));
#8369=CARTESIAN_POINT('Ctrl Pts',(-1.28958670862024,-0.958542185070025,
5.85317742809365));
#8370=CARTESIAN_POINT('Ctrl Pts',(0.0911995079083431,-1.60421716932215,
5.94756173384057));
#8371=CARTESIAN_POINT('Ctrl Pts',(1.38991339951521,-0.806215136739692,6.0419460395875));
#8372=CARTESIAN_POINT('Ctrl Pts',(1.43780102116983,0.717335496333373,6.13633034533442));
#8373=CARTESIAN_POINT('Ctrl Pts',(0.191771518049578,1.59531262522119,6.23071465108135));
#8374=CARTESIAN_POINT('Ctrl Pts',(-1.22684471207484,1.03766169287464,6.32509895682827));
#8375=CARTESIAN_POINT('Ctrl Pts',(-1.5413756345963,-0.453891047542918,6.4194832625752));
#8376=CARTESIAN_POINT('Ctrl Pts',(-0.468797479631732,-1.53682335007771,
6.51386756832213));
#8377=CARTESIAN_POINT('Ctrl Pts',(1.0257054921741,-1.23700831929723,6.60825187406904));
#8378=CARTESIAN_POINT('Ctrl Pts',(1.59706942293656,0.176571945924337,6.70263617981598));
#8379=CARTESIAN_POINT('Ctrl Pts',(0.731327235084403,1.43021159562341,6.79702048556289));
#8380=CARTESIAN_POINT('Ctrl Pts',(-0.792832326431882,1.39875704001798,6.89140479130984));
#8381=CARTESIAN_POINT('Ctrl Pts',(-1.60300439910634,0.104509850998243,6.98579163368847));
#8382=CARTESIAN_POINT('Ctrl Pts',(-1.1820010522363,-0.815067137550017,7.04871704081814));
#8383=CARTESIAN_POINT('Ctrl Pts',(-0.823987965664692,-1.08656105240261,
7.08018101269885));
#8384=CARTESIAN_POINT('',(-0.562200904851585,1.2460199179177,6.88180017065881));
#8385=CARTESIAN_POINT('Ctrl Pts',(-0.562671582971943,1.24691123662228,6.88122480138927));
#8386=CARTESIAN_POINT('Ctrl Pts',(-0.603396319682483,1.23447102102747,6.88122480138927));
#8387=CARTESIAN_POINT('Ctrl Pts',(-0.643403900568493,1.22005362851167,6.88122480138927));
#8388=CARTESIAN_POINT('Ctrl Pts',(-0.682543476113644,1.20366219176739,6.88122480138927));
#8389=CARTESIAN_POINT('Ctrl Pts',(-0.732386709520514,1.18278812258959,6.88122480138928));
#8390=CARTESIAN_POINT('Ctrl Pts',(-0.78082328725544,1.15871479259185,6.88122480138927));
#8391=CARTESIAN_POINT('Ctrl Pts',(-0.827721022731547,1.13172823854745,6.88122480138928));
#8392=CARTESIAN_POINT('Ctrl Pts',(-0.84745147406581,1.12037466495062,6.88122480138928));
#8393=CARTESIAN_POINT('Ctrl Pts',(-0.86690944613167,1.10850482371099,6.88122480138928));
#8394=CARTESIAN_POINT('Ctrl Pts',(-0.886084452197379,1.09613742275174,6.88122480138928));
#8395=CARTESIAN_POINT('Ctrl Pts',(-0.895254546003681,1.09022294081897,6.88122480138927));
#8396=CARTESIAN_POINT('Ctrl Pts',(-0.904359213369853,1.08419499716347,6.88122480138927));
#8397=CARTESIAN_POINT('Ctrl Pts',(-0.9133886633195,1.07806173785588,6.88122480138927));
#8398=CARTESIAN_POINT('Ctrl Pts',(-0.960084073216897,1.04634385260573,6.88122480138927));
#8399=CARTESIAN_POINT('Ctrl Pts',(-1.00483130342816,1.01177396154596,6.88122480138927));
#8400=CARTESIAN_POINT('Ctrl Pts',(-1.0474874886513,0.974668896684433,6.88122480138927));
#8401=CARTESIAN_POINT('Ctrl Pts',(-1.07964127198061,0.946699489440531,6.88122480138927));
#8402=CARTESIAN_POINT('Ctrl Pts',(-1.11060686174787,0.917288339612735,6.88122480138928));
#8403=CARTESIAN_POINT('Ctrl Pts',(-1.14031679043589,0.886552719621228,6.88122480138927));
#8404=CARTESIAN_POINT('Ctrl Pts',(-1.15037276608795,0.876149576297283,6.88122480138927));
#8405=CARTESIAN_POINT('Ctrl Pts',(-1.16028482946549,0.865594576601913,6.88122480138927));
#8406=CARTESIAN_POINT('Ctrl Pts',(-1.17005016216063,0.854891914773771,6.88122480138927));
#8407=CARTESIAN_POINT('Ctrl Pts',(-1.17927582847417,0.844780719407922,6.88122480138927));
#8408=CARTESIAN_POINT('Ctrl Pts',(-1.18837165555294,0.834536200457194,6.88122480138927));
#8409=CARTESIAN_POINT('Ctrl Pts',(-1.1973208397126,0.824179036166977,6.88122480138927));
#8410=CARTESIAN_POINT('Ctrl Pts',(-1.23576374944636,0.779687882023377,6.88122480138927));
#8411=CARTESIAN_POINT('Ctrl Pts',(-1.27156408809512,0.733055964514648,6.88122480138927));
#8412=CARTESIAN_POINT('Ctrl Pts',(-1.30457263970431,0.684606290778475,6.88122480138927));
#8413=CARTESIAN_POINT('Ctrl Pts',(-1.33817782711293,0.635280880046517,6.88122480138927));
#8414=CARTESIAN_POINT('Ctrl Pts',(-1.36889028667294,0.584070719971771,6.88122480138927));
#8415=CARTESIAN_POINT('Ctrl Pts',(-1.39652600638908,0.531270056701515,6.88122480138927));
#8416=CARTESIAN_POINT('Ctrl Pts',(-1.41410396658768,0.497685696787698,6.88122480138927));
#8417=CARTESIAN_POINT('Ctrl Pts',(-1.43043659202958,0.463456956653398,6.88122480138927));
#8418=CARTESIAN_POINT('Ctrl Pts',(-1.44546851334572,0.428652056108916,6.88122480138927));
#8419=CARTESIAN_POINT('Ctrl Pts',(-1.45233683119575,0.412749157560524,6.88122480138927));
#8420=CARTESIAN_POINT('Ctrl Pts',(-1.45893350142566,0.396725904291308,6.88122480138927));
#8421=CARTESIAN_POINT('Ctrl Pts',(-1.46525271318191,0.380588495018258,6.88122480138927));
#8422=CARTESIAN_POINT('Ctrl Pts',(-1.46896921857413,0.371097632725099,6.88122480138927));
#8423=CARTESIAN_POINT('Ctrl Pts',(-1.47258974601173,0.361567281164457,6.88122480138927));
#8424=CARTESIAN_POINT('Ctrl Pts',(-1.47611305419256,0.3519986756308,6.88122480138927));
#8425=CARTESIAN_POINT('Ctrl Pts',(-1.47979874984576,0.341989057961137,6.88122480138927));
#8426=CARTESIAN_POINT('Ctrl Pts',(-1.48337460810265,0.33194690923843,6.88122480138927));
#8427=CARTESIAN_POINT('Ctrl Pts',(-1.48683919026953,0.321875619808138,6.88122480138927));
#8428=CARTESIAN_POINT('Ctrl Pts',(-1.50680459825216,0.26383762483459,6.88122480138927));
#8429=CARTESIAN_POINT('Ctrl Pts',(-1.5230840690397,0.204817247296188,6.88122480138927));
#8430=CARTESIAN_POINT('Ctrl Pts',(-1.53549722234912,0.145128489083916,6.88122480138927));
#8431=CARTESIAN_POINT('Ctrl Pts',(-1.538454112368,0.13091025710066,6.88122480138927));
#8432=CARTESIAN_POINT('Ctrl Pts',(-1.54119145123912,0.116653938738659,6.88122480138927));
#8433=CARTESIAN_POINT('Ctrl Pts',(-1.54370646449436,0.10236349960097,6.88122480138927));
#8434=CARTESIAN_POINT('Ctrl Pts',(-1.55390853471807,0.0443947937474662,
6.88122480138927));
#8435=CARTESIAN_POINT('Ctrl Pts',(-1.56045619814385,-0.0141339339575868,
6.88122480138927));
#8436=CARTESIAN_POINT('Ctrl Pts',(-1.56350967632926,-0.0729601076848401,
6.88122480138927));
#8437=CARTESIAN_POINT('Ctrl Pts',(-1.56505061044946,-0.102646666013803,
6.88122480138927));
#8438=CARTESIAN_POINT('Ctrl Pts',(-1.56570089209292,-0.132409272280549,
6.88122480138927));
#8439=CARTESIAN_POINT('Ctrl Pts',(-1.5654763879049,-0.162215441966596,6.88122480138927));
#8440=CARTESIAN_POINT('Ctrl Pts',(-1.56533644256305,-0.180795204965318,
6.88122480138927));
#8441=CARTESIAN_POINT('Ctrl Pts',(-1.56485656325647,-0.199390994007395,
6.88122480138927));
#8442=CARTESIAN_POINT('Ctrl Pts',(-1.56403984705495,-0.217997968754189,
6.88122480138927));
#8443=CARTESIAN_POINT('Ctrl Pts',(-1.56345932716366,-0.231223761186564,
6.88122480138927));
#8444=CARTESIAN_POINT('Ctrl Pts',(-1.56270841160904,-0.244455267230033,
6.88122480138927));
#8445=CARTESIAN_POINT('Ctrl Pts',(-1.56179009164389,-0.257668068879168,
6.88122480138927));
#8446=CARTESIAN_POINT('Ctrl Pts',(-1.55754402835719,-0.318760492136378,
6.88122480138927));
#8447=CARTESIAN_POINT('Ctrl Pts',(-1.5497211828875,-0.379535249490823,6.88122480138927));
#8448=CARTESIAN_POINT('Ctrl Pts',(-1.53851766179682,-0.439705870790377,
6.88122480138927));
#8449=CARTESIAN_POINT('Ctrl Pts',(-1.52699040597737,-0.50161517045804,6.88122480138927));
#8450=CARTESIAN_POINT('Ctrl Pts',(-1.51188432995146,-0.562885842520045,
6.88122480138927));
#8451=CARTESIAN_POINT('Ctrl Pts',(-1.49335852869952,-0.623218541410667,
6.88122480138927));
#8452=CARTESIAN_POINT('Ctrl Pts',(-1.47483272744757,-0.68355124030129,6.88122480138927));
#8453=CARTESIAN_POINT('Ctrl Pts',(-1.45288698918659,-0.742947024621097,
6.88122480138927));
#8454=CARTESIAN_POINT('Ctrl Pts',(-1.42762827080073,-0.80110390561782,6.88122480138928));
#8455=CARTESIAN_POINT('Ctrl Pts',(-1.42298648268494,-0.811791380529987,
6.88122480138927));
#8456=CARTESIAN_POINT('Ctrl Pts',(-1.41823267413198,-0.822436983453104,
6.88122480138927));
#8457=CARTESIAN_POINT('Ctrl Pts',(-1.41336732622985,-0.833038785828612,
6.88122480138927));
#8458=CARTESIAN_POINT('Ctrl Pts',(-1.40898307425986,-0.84259225947229,6.88122480138927));
#8459=CARTESIAN_POINT('Ctrl Pts',(-1.40451005729422,-0.852106110738308,
6.88122480138927));
#8460=CARTESIAN_POINT('Ctrl Pts',(-1.39995239732874,-0.861571908632687,
6.88122480138927));
#8461=CARTESIAN_POINT('Ctrl Pts',(-1.37164075215683,-0.920372326672761,
6.88122480138927));
#8462=CARTESIAN_POINT('Ctrl Pts',(-1.34002926990105,-0.97740157812146,6.88122480138927));
#8463=CARTESIAN_POINT('Ctrl Pts',(-1.30529384686795,-1.03235040180416,6.88122480138927));
#8464=CARTESIAN_POINT('Ctrl Pts',(-1.27069709177016,-1.08707986325481,6.88122480138927));
#8465=CARTESIAN_POINT('Ctrl Pts',(-1.23300099244043,-1.13974654572362,6.88122480138928));
#8466=CARTESIAN_POINT('Ctrl Pts',(-1.19232907000199,-1.19003713909265,6.88122480138928));
#8467=CARTESIAN_POINT('Ctrl Pts',(-1.15202924701569,-1.23986763367317,6.88122480138928));
#8468=CARTESIAN_POINT('Ctrl Pts',(-1.10880748201239,-1.28736635050648,6.88122480138928));
#8469=CARTESIAN_POINT('Ctrl Pts',(-1.06273912028356,-1.33220527792149,6.88122480138928));
#8470=CARTESIAN_POINT('Ctrl Pts',(-1.0527315145224,-1.34194580898193,6.88122480138928));
#8471=CARTESIAN_POINT('Ctrl Pts',(-1.04258941726239,-1.35156070196631,6.88122480138927));
#8472=CARTESIAN_POINT('Ctrl Pts',(-1.03231334037779,-1.36104637311814,6.88122480138928));
#8473=CARTESIAN_POINT('Ctrl Pts',(-0.547737204315714,1.25137522550529,6.88122480138927));
#8474=CARTESIAN_POINT('Ctrl Pts',(-0.552435712024308,1.24931865012781,6.88141659114578));
#8475=CARTESIAN_POINT('Ctrl Pts',(-0.557122636949875,1.24723561241451,6.8816083809023));
#8476=CARTESIAN_POINT('Ctrl Pts',(-0.56179768176358,1.24512624450899,6.88180017065881));
#8477=CARTESIAN_POINT('Ctrl Pts',(0.748315817581761,1.5383870784886,2.15322551455621E-15));
#8478=CARTESIAN_POINT('Ctrl Pts',(0.79330974013975,1.51121254923536,2.00324072560254E-15));
#8479=CARTESIAN_POINT('Ctrl Pts',(0.83683948866918,1.48192024638845,2.72835309894076E-15));
#8480=CARTESIAN_POINT('Ctrl Pts',(0.878734943125877,1.45051315882962,1.8249290967276E-15));
#8481=CARTESIAN_POINT('Ctrl Pts',(0.930187061785903,1.41194188142498,7.84580135121318E-16));
#8482=CARTESIAN_POINT('Ctrl Pts',(0.979175755310881,1.37018143662514,2.88535685585316E-15));
#8483=CARTESIAN_POINT('Ctrl Pts',(1.02556564781079,1.32556170063658,2.99760216648792E-15));
#8484=CARTESIAN_POINT('Ctrl Pts',(1.07240876425823,1.28050603492728,3.11094410097838E-15));
#8485=CARTESIAN_POINT('Ctrl Pts',(1.11660252973995,1.23253384670277,9.75804439780424E-16));
#8486=CARTESIAN_POINT('Ctrl Pts',(1.15796154596301,1.18195995627099,1.7277845820729E-15));
#8487=CARTESIAN_POINT('Ctrl Pts',(1.17178013931695,1.16506255178646,1.97903107547438E-15));
#8488=CARTESIAN_POINT('Ctrl Pts',(1.18528187595262,1.14787458382087,2.54865482595334E-15));
#8489=CARTESIAN_POINT('Ctrl Pts',(1.19845856877168,1.13040751148756,1.48492329543615E-15));
#8490=CARTESIAN_POINT('Ctrl Pts',(1.20535439611853,1.12126637746256,9.04097576277068E-16));
#8491=CARTESIAN_POINT('Ctrl Pts',(1.21216118957793,1.11204880118057,1.55361878839882E-15));
#8492=CARTESIAN_POINT('Ctrl Pts',(1.21887770206587,1.10275642073377,2.51187959321442E-15));
#8493=CARTESIAN_POINT('Ctrl Pts',(1.2257756336561,1.09321304465169,3.19792110923887E-15));
#8494=CARTESIAN_POINT('Ctrl Pts',(1.23257353957357,1.08359733938013,3.17391878255083E-15));
#8495=CARTESIAN_POINT('Ctrl Pts',(1.23926703280866,1.07391651229646,3.08780778723872E-15));
#8496=CARTESIAN_POINT('Ctrl Pts',(1.27551793785583,1.02148667767015,2.571274784078E-15));
#8497=CARTESIAN_POINT('Ctrl Pts',(1.30874446989807,0.967101148680756,6.0414663234747E-16));
#8498=CARTESIAN_POINT('Ctrl Pts',(1.338811224237,0.911076311564746,1.38777878078145E-15));
#8499=CARTESIAN_POINT('Ctrl Pts',(1.3702518095946,0.852491548685597,2.20721719352362E-15));
#8500=CARTESIAN_POINT('Ctrl Pts',(1.39823810519405,0.79211305995548,-1.27615658727163E-16));
#8501=CARTESIAN_POINT('Ctrl Pts',(1.42255628167792,0.730287083244153,2.35922392732846E-16));
#8502=CARTESIAN_POINT('Ctrl Pts',(1.44502502073072,0.673163074035149,5.71812775773418E-16));
#8503=CARTESIAN_POINT('Ctrl Pts',(1.46436199499226,0.614802389501134,-4.25826032830452E-15));
#8504=CARTESIAN_POINT('Ctrl Pts',(1.48034796790375,0.555481066013023,2.77555756156289E-17));
#8505=CARTESIAN_POINT('Ctrl Pts',(1.48166379860548,0.55059823409877,3.80544320203479E-16));
#8506=CARTESIAN_POINT('Ctrl Pts',(1.48295689684359,0.545708899972741,7.86156538718846E-16));
#8507=CARTESIAN_POINT('Ctrl Pts',(1.48422712470284,0.540813221486026,1.41553435639707E-15));
#8508=CARTESIAN_POINT('Ctrl Pts',(1.4867316679211,0.531160277517357,2.65882271871602E-15));
#8509=CARTESIAN_POINT('Ctrl Pts',(1.48914639934276,0.521485933259116,2.32141274649425E-15));
#8510=CARTESIAN_POINT('Ctrl Pts',(1.49146863316748,0.511799559522065,2.23432383705813E-15));
#8511=CARTESIAN_POINT('Ctrl Pts',(1.50564287428223,0.452676746214071,2.4148937701561E-15));
#8512=CARTESIAN_POINT('Ctrl Pts',(1.51639877554924,0.393016146915013,2.33379373485162E-15));
#8513=CARTESIAN_POINT('Ctrl Pts',(1.52358166896565,0.333090755615199,9.29811783123569E-16));
#8514=CARTESIAN_POINT('Ctrl Pts',(1.53054106613352,0.27502994720298,-1.32152166187657E-15));
#8515=CARTESIAN_POINT('Ctrl Pts',(1.53414632425553,0.216719733480015,-1.71265129966507E-15));
#8516=CARTESIAN_POINT('Ctrl Pts',(1.53420883231942,0.158413996521009,-4.44089209850063E-16));
#8517=CARTESIAN_POINT('Ctrl Pts',(1.53424500829747,0.124670077262913,4.98577800183531E-16));
#8518=CARTESIAN_POINT('Ctrl Pts',(1.53309367734275,0.0909278273352152,-6.71329225516391E-16));
#8519=CARTESIAN_POINT('Ctrl Pts',(1.53071060824393,0.0572389507155212,-9.85322934354826E-16));
#8520=CARTESIAN_POINT('Ctrl Pts',(1.52842944993871,0.0249907625566291,-1.07107518135246E-15));
#8521=CARTESIAN_POINT('Ctrl Pts',(1.52501947762763,-0.00720854617748223,
-2.07868045293857E-15));
#8522=CARTESIAN_POINT('Ctrl Pts',(1.52050115185295,-0.0393112549066445,
-2.06779038336435E-15));
#8523=CARTESIAN_POINT('Ctrl Pts',(1.51864265927286,-0.0525158463745993,
-1.87592535676816E-15));
#8524=CARTESIAN_POINT('Ctrl Pts',(1.51659588303773,-0.0657074995902743,
-1.62350288100921E-15));
#8525=CARTESIAN_POINT('Ctrl Pts',(1.5143668392248,-0.0788573464476957,-1.70696790036118E-15));
#8526=CARTESIAN_POINT('Ctrl Pts',(1.5045273247336,-0.136903809222598,-2.16891961470101E-15));
#8527=CARTESIAN_POINT('Ctrl Pts',(1.49112862123246,-0.194234466941921,-2.81475207116788E-15));
#8528=CARTESIAN_POINT('Ctrl Pts',(1.47436851148242,-0.250588170236329,-1.1518563880486E-15));
#8529=CARTESIAN_POINT('Ctrl Pts',(1.4568136293047,-0.309614193118367,5.89894604418642E-16));
#8530=CARTESIAN_POINT('Ctrl Pts',(1.43557050341456,-0.367569697988627,3.94366376571076E-16));
#8531=CARTESIAN_POINT('Ctrl Pts',(1.41081400323684,-0.424124826119812,3.05311331771918E-16));
#8532=CARTESIAN_POINT('Ctrl Pts',(1.38734333111861,-0.47774253700151,2.20881717652363E-16));
#8533=CARTESIAN_POINT('Ctrl Pts',(1.36071371363536,-0.530102124474644,-3.10126693863359E-16));
#8534=CARTESIAN_POINT('Ctrl Pts',(1.33104076585779,-0.580883676744975,-2.3037127760972E-15));
#8535=CARTESIAN_POINT('Ctrl Pts',(1.32941514948567,-0.583665716581097,-2.41293030981866E-15));
#8536=CARTESIAN_POINT('Ctrl Pts',(1.32778039253364,-0.586443008841638,-2.36550771100398E-15));
#8537=CARTESIAN_POINT('Ctrl Pts',(1.32613651184916,-0.589215496846285,-2.44249065417534E-15));
#8538=CARTESIAN_POINT('Ctrl Pts',(1.32062943215923,-0.598503465568777,-2.53258028311659E-15));
#8539=CARTESIAN_POINT('Ctrl Pts',(1.31502183376448,-0.607734246301079,-2.0661488452891E-15));
#8540=CARTESIAN_POINT('Ctrl Pts',(1.30931903080635,-0.616898915910521,-1.99840144432528E-15));
#8541=CARTESIAN_POINT('Ctrl Pts',(1.27896983478356,-0.665671485557963,-1.81941077559367E-15));
#8542=CARTESIAN_POINT('Ctrl Pts',(1.24589105028342,-0.712635601535066,-7.13006852229392E-16));
#8543=CARTESIAN_POINT('Ctrl Pts',(1.210222326866,-0.757511300638567,-5.55111512312578E-16));
#8544=CARTESIAN_POINT('Ctrl Pts',(1.1802861081694,-0.79517479441724,-4.22592347788311E-16));
#8545=CARTESIAN_POINT('Ctrl Pts',(1.14852468994335,-0.831366862692395,-1.65660898229942E-15));
#8546=CARTESIAN_POINT('Ctrl Pts',(1.11500605367636,-0.865897589688669,-1.27675647831893E-15));
#8547=CARTESIAN_POINT('Ctrl Pts',(1.106788817097,-0.874362944625117,-1.34173175461127E-15));
#8548=CARTESIAN_POINT('Ctrl Pts',(1.09846592082978,-0.882728332671732,-1.4518904375016E-15));
#8549=CARTESIAN_POINT('Ctrl Pts',(1.09003827756787,-0.890990714153347,-6.93889390390723E-16));
#8550=CARTESIAN_POINT('Ctrl Pts',(1.08120696979645,-0.8996488444896,1.26881278685788E-16));
#8551=CARTESIAN_POINT('Ctrl Pts',(1.07226667800469,-0.908187904030433,-9.62861165954058E-16));
#8552=CARTESIAN_POINT('Ctrl Pts',(1.0632213738949,-0.916602560539565,-5.82867087928207E-16));
#8553=CARTESIAN_POINT('Ctrl Pts',(1.02245569976267,-0.95452601131826,1.67515078953523E-15));
#8554=CARTESIAN_POINT('Ctrl Pts',(0.979542146270061,-0.989942845515599,
-2.99196435015932E-16));
#8555=CARTESIAN_POINT('Ctrl Pts',(0.934596947466491,-1.02256508694638,5.82867087928207E-16));
#8556=CARTESIAN_POINT('Ctrl Pts',(0.889651748662921,-1.05518732837715,1.58939179805206E-15));
#8557=CARTESIAN_POINT('Ctrl Pts',(0.842674238566416,-1.08501566506116,-2.12027705394649E-16));
#8558=CARTESIAN_POINT('Ctrl Pts',(0.793764246391153,-1.11170783983522,-5.82867087928207E-16));
#8559=CARTESIAN_POINT('Origin',(0.,0.,8.66831010612084));
#8560=CARTESIAN_POINT('',(-2.72578406873475,-3.33812273494286E-16,8.66831010612084));
#8561=CARTESIAN_POINT('Origin',(0.,0.,8.66831010612084));
#8562=CARTESIAN_POINT('Origin',(1.80562831587628,0.,0.));
#8563=CARTESIAN_POINT('Origin',(3.51922397520286,0.,6.88122480138927));
#8564=CARTESIAN_POINT('',(-3.51922397520286,-4.30980637671481E-16,6.88122480138927));
#8565=CARTESIAN_POINT('Origin',(0.,0.,6.88122480138927));
#8566=CARTESIAN_POINT('Origin',(0.,0.,8.31887564143431));
#8567=CARTESIAN_POINT('',(-3.51922397520286,-4.30980637671481E-16,9.75652648147935));
#8568=CARTESIAN_POINT('Origin',(0.,0.,9.75652648147935));
#8569=CARTESIAN_POINT('',(-3.51922397520286,-4.30980637671481E-16,8.31887564143431));
#8570=CARTESIAN_POINT('Origin',(0.,0.,9.84316232611724));
#8571=CARTESIAN_POINT('',(-3.18037436229666,-3.8948352828769E-16,9.92979817075513));
#8572=CARTESIAN_POINT('',(-3.34979916874976,4.10232082979586E-16,9.84316232611724));
#8573=CARTESIAN_POINT('Origin',(0.,0.,9.92979817075513));
#8574=CARTESIAN_POINT('Origin',(0.,0.,10.7561296768773));
#8575=CARTESIAN_POINT('',(-3.18037436229666,-3.8948352828769E-16,11.5824611829994));
#8576=CARTESIAN_POINT('Origin',(0.,0.,11.5824611829994));
#8577=CARTESIAN_POINT('',(-3.18037436229666,-3.89483528287691E-16,10.7561296768773));
#8578=CARTESIAN_POINT('Origin',(3.71701820384649,0.,11.5824611829994));
#8579=CARTESIAN_POINT('',(-3.71701820384649,-4.55203444571304E-16,11.5824611829994));
#8580=CARTESIAN_POINT('Origin',(0.,0.,11.5824611829994));
#8581=CARTESIAN_POINT('Origin',(0.,0.,12.6961282806954));
#8582=CARTESIAN_POINT('',(-3.71701820384649,-4.55203444571304E-16,13.8097953783913));
#8583=CARTESIAN_POINT('Origin',(0.,0.,13.8097953783913));
#8584=CARTESIAN_POINT('',(-3.71701820384649,-4.55203444571305E-16,12.6961282806954));
#8585=CARTESIAN_POINT('Origin',(0.,0.,13.8097953783913));
#8586=CARTESIAN_POINT('',(-3.01701820384649,-3.6947816863099E-16,14.5097953783913));
#8587=CARTESIAN_POINT('Origin',(0.,0.,14.5097953783913));
#8588=CARTESIAN_POINT('Origin',(-3.01701820384648,-3.69478168630989E-16,
13.8097953783913));
#8589=CARTESIAN_POINT('Origin',(1.4890246697361,0.,14.5097953783913));
#8590=CARTESIAN_POINT('',(-1.4890246697361,-1.82352929564375E-16,14.5097953783913));
#8591=CARTESIAN_POINT('Origin',(0.,0.,14.5097953783913));
#8592=CARTESIAN_POINT('Origin',(0.,0.,14.1858997942285));
#8593=CARTESIAN_POINT('',(-1.4890246697361,-1.82352929564375E-16,13.8620042100656));
#8594=CARTESIAN_POINT('Origin',(0.,0.,13.8620042100656));
#8595=CARTESIAN_POINT('',(-1.4890246697361,-1.82352929564376E-16,14.1858997942285));
#8596=CARTESIAN_POINT('Origin',(2.72578406873475,0.,13.8620042100656));
#8597=CARTESIAN_POINT('',(-2.72578406873475,-3.33812273494286E-16,13.8620042100656));
#8598=CARTESIAN_POINT('Origin',(0.,0.,13.8620042100656));
#8599=CARTESIAN_POINT('Origin',(0.,0.,11.2651571580932));
#8600=CARTESIAN_POINT('',(-2.72578406873475,-3.33812273494286E-16,11.2651571580932));
#14531=UNCERTAINTY_MEASURE_WITH_UNIT(LENGTH_MEASURE(0.01),#14545,
'DISTANCE_ACCURACY_VALUE',
'Maximum model space distance between geometric entities at asserted c
onnectivities');
#14534=UNCERTAINTY_MEASURE_WITH_UNIT(LENGTH_MEASURE(0.01),#14545,
'DISTANCE_ACCURACY_VALUE',
'Maximum model space distance between geometric entities at asserted c
onnectivities');
#14541=(
GEOMETRIC_REPRESENTATION_CONTEXT(3)
GLOBAL_UNCERTAINTY_ASSIGNED_CONTEXT((#14531))
GLOBAL_UNIT_ASSIGNED_CONTEXT((#14545,#14547,#14548))
REPRESENTATION_CONTEXT('','3D')
);
#14544=(
GEOMETRIC_REPRESENTATION_CONTEXT(3)
GLOBAL_UNCERTAINTY_ASSIGNED_CONTEXT((#14534))
GLOBAL_UNIT_ASSIGNED_CONTEXT((#14545,#14547,#14548))
REPRESENTATION_CONTEXT('','3D')
);
#14545=(
LENGTH_UNIT()
NAMED_UNIT(*)
SI_UNIT(.MILLI.,.METRE.)
);
#14547=(
NAMED_UNIT(*)
PLANE_ANGLE_UNIT()
SI_UNIT($,.RADIAN.)
);
#14548=(
NAMED_UNIT(*)
SI_UNIT($,.STERADIAN.)
SOLID_ANGLE_UNIT()
);
#14555=SHAPE_DEFINITION_REPRESENTATION(#14564,#14581);
#14564=PRODUCT_DEFINITION_SHAPE('',$,#14591);
#14581=SHAPE_REPRESENTATION('',(#2004),#14541);
#14584=PRODUCT_DEFINITION_CONTEXT('part definition',#14613,'design');
#14591=PRODUCT_DEFINITION('Screw_01','Screw_01',#14600,#14584);
#14600=PRODUCT_DEFINITION_FORMATION('',$,#14621);
#14613=APPLICATION_CONTEXT(
'Core Data for Automotive Mechanical Design Process');
#14614=PRODUCT_CONTEXT('part definition',#14613,'mechanical');
#14621=PRODUCT('Screw_01','Screw_01',$,(#14614));
#14627=PRESENTATION_STYLE_ASSIGNMENT((#14631));
#14631=SURFACE_STYLE_USAGE(.BOTH.,#14635);
#14635=SURFACE_SIDE_STYLE('',(#14639));
#14639=SURFACE_STYLE_FILL_AREA(#14643);
#14643=FILL_AREA_STYLE('Opaque(203,203,203)',(#14647));
#14647=FILL_AREA_STYLE_COLOUR('Opaque(203,203,203)',#14651);
#14651=COLOUR_RGB('Opaque(203,203,203)', 0.31764706, 0.68627451, 0.89019608);
ENDSEC;
END-ISO-10303-21;
